ISO-10303-21;
HEADER;
FILE_DESCRIPTION (('STEP AP214'),
    '1' );
FILE_NAME ('spur gear_iso_ISO - Spur gear 2M 50T 20PA 18FW ---S50B22H150L15.0N.step',
    '2026-10-08T11:45:07',
    ( '' ),
    ( '' ),
    'SwSTEP 2.0',
    'SolidWorks 2026',
    '' );
FILE_SCHEMA (( 'AUTOMOTIVE_DESIGN' ));
ENDSEC;

DATA;
#6=CIRCLE ( 'NONE', #19608, 51.99999999999999289 ) ;
#12=CARTESIAN_POINT ( 'NONE',  ( 18.00000000000000355, 45.78515115856060191, -12.64416602183617577 ) ) ;
#14=CARTESIAN_POINT ( 'NONE',  ( 0.000000000000000000, -47.32430374665948136, 21.55018039121509688 ) ) ;
#15=DIRECTION ( 'NONE',  ( 0.000000000000000000, -0.8443279255020199603, 0.5358267949789887741 ) ) ;
#16=VERTEX_POINT ( 'NONE', #31754 ) ;
#17=DIRECTION ( 'NONE',  ( -1.000000000000000000, -0.000000000000000000, -0.000000000000000000 ) ) ;
#34=EDGE_LOOP ( 'NONE', ( #7797, #14411, #2119, #1925 ) ) ;
#40=EDGE_CURVE ( 'NONE', #21663, #37965, #25471, .T. ) ;
#55=DIRECTION ( 'NONE',  ( 1.000000000000000000, -0.000000000000000000, -0.000000000000000000 ) ) ;
#61=AXIS2_PLACEMENT_3D ( 'NONE', #7256, #13853, #27356 ) ;
#65=LINE ( 'NONE', #43070, #7397 ) ;
#68=DIRECTION ( 'NONE',  ( 0.000000000000000000, 0.000000000000000000, -1.000000000000000000 ) ) ;
#70=DIRECTION ( 'NONE',  ( -1.000000000000000000, 0.000000000000000000, 0.000000000000000000 ) ) ;
#76=DIRECTION ( 'NONE',  ( 0.000000000000000000, 0.000000000000000000, -1.000000000000000000 ) ) ;
#93=DIRECTION ( 'NONE',  ( 0.000000000000000000, -0.3681245526846853022, 0.9297764858882484607 ) ) ;
#106=DIRECTION ( 'NONE',  ( -1.000000000000000000, -0.000000000000000000, -0.000000000000000000 ) ) ;
#108=ADVANCED_FACE ( 'NONE', ( #34802 ), #31105, .T. ) ;
#118=LINE ( 'NONE', #13486, #30404 ) ;
#121=DIRECTION ( 'NONE',  ( -1.000000000000000000, -0.000000000000000000, -0.000000000000000000 ) ) ;
#124=CARTESIAN_POINT ( 'NONE',  ( 0.000000000000000000, 0.000000000000000000, 0.000000000000000000 ) ) ;
#133=EDGE_CURVE ( 'NONE', #32336, #24871, #39498, .T. ) ;
#137=EDGE_LOOP ( 'NONE', ( #388, #32106, #23613, #3341 ) ) ;
#151=DIRECTION ( 'NONE',  ( 0.000000000000000000, 0.000000000000000000, -1.000000000000000000 ) ) ;
#167=DIRECTION ( 'NONE',  ( 0.000000000000000000, 0.000000000000000000, 1.000000000000000000 ) ) ;
#170=VERTEX_POINT ( 'NONE', #16346 ) ;
#178=CARTESIAN_POINT ( 'NONE',  ( 18.00000000000000355, 20.99948489194481738, -42.60488980472760545 ) ) ;
#192=VERTEX_POINT ( 'NONE', #36012 ) ;
#199=CARTESIAN_POINT ( 'NONE',  ( 9.000000000000001776, -30.03615769709704608, -42.44795908869020451 ) ) ;
#202=ORIENTED_EDGE ( 'NONE', *, *, #13580, .T. ) ;
#204=LINE ( 'NONE', #34053, #4600 ) ;
#207=CYLINDRICAL_SURFACE ( 'NONE', #17131, 20.00000000000000355 ) ;
#217=ORIENTED_EDGE ( 'NONE', *, *, #22395, .F. ) ;
#225=DIRECTION ( 'NONE',  ( -1.000000000000000000, 0.000000000000000000, 0.000000000000000000 ) ) ;
#229=ORIENTED_EDGE ( 'NONE', *, *, #13847, .F. ) ;
#235=VERTEX_POINT ( 'NONE', #20345 ) ;
#240=CYLINDRICAL_SURFACE ( 'NONE', #4769, 20.00000000000000355 ) ;
#253=ORIENTED_EDGE ( 'NONE', *, *, #22562, .T. ) ;
#254=DIRECTION ( 'NONE',  ( 0.000000000000000000, -6.938893903907226011E-15, 1.000000000000000000 ) ) ;
#255=VERTEX_POINT ( 'NONE', #36433 ) ;
#259=LINE ( 'NONE', #7052, #31169 ) ;
#262=DIRECTION ( 'NONE',  ( 0.000000000000000000, -0.9980267284282708928, -0.06279051952932436509 ) ) ;
#266=CIRCLE ( 'NONE', #34432, 20.00000000000000711 ) ;
#269=DIRECTION ( 'NONE',  ( 0.000000000000000000, 0.000000000000000000, 1.000000000000000000 ) ) ;
#283=ADVANCED_FACE ( 'NONE', ( #13571 ), #32962, .T. ) ;
#285=EDGE_LOOP ( 'NONE', ( #5183, #4420, #32510, #24970 ) ) ;
#286=CARTESIAN_POINT ( 'NONE',  ( -10.00000000000000000, 0.000000000000000000, 0.000000000000000000 ) ) ;
#291=VERTEX_POINT ( 'NONE', #33181 ) ;
#296=EDGE_CURVE ( 'NONE', #640, #8463, #3270, .T. ) ;
#307=CARTESIAN_POINT ( 'NONE',  ( 0.000000000000000000, -18.53613841426822972, 48.58406706613896375 ) ) ;
#311=ORIENTED_EDGE ( 'NONE', *, *, #38978, .F. ) ;
#316=DIRECTION ( 'NONE',  ( 0.000000000000000000, 0.000000000000000000, -1.000000000000000000 ) ) ;
#322=EDGE_CURVE ( 'NONE', #29751, #6854, #14213, .T. ) ;
#332=AXIS2_PLACEMENT_3D ( 'NONE', #8992, #29286, #42557 ) ;
#347=DIRECTION ( 'NONE',  ( -1.000000000000000000, -0.000000000000000000, -0.000000000000000000 ) ) ;
#352=ORIENTED_EDGE ( 'NONE', *, *, #296, .F. ) ;
#354=ORIENTED_EDGE ( 'NONE', *, *, #6008, .F. ) ;
#355=DIRECTION ( 'NONE',  ( 0.000000000000000000, 0.7705132427757904745, -0.6374239897486881912 ) ) ;
#359=ORIENTED_EDGE ( 'NONE', *, *, #32192, .T. ) ;
#361=EDGE_CURVE ( 'NONE', #10268, #41981, #3126, .T. ) ;
#363=VECTOR ( 'NONE', #4205, 1000.000000000000000 ) ;
#367=VECTOR ( 'NONE', #17531, 1000.000000000000000 ) ;
#373=CARTESIAN_POINT ( 'NONE',  ( 18.00000000000000355, -36.34385289850569478, -29.77717097092114429 ) ) ;
#381=DIRECTION ( 'NONE',  ( 0.000000000000000000, 0.000000000000000000, 1.000000000000000000 ) ) ;
#388=ORIENTED_EDGE ( 'NONE', *, *, #3051, .T. ) ;
#400=EDGE_CURVE ( 'NONE', #17108, #12372, #25504, .T. ) ;
#402=CARTESIAN_POINT ( 'NONE',  ( 0.000000000000000000, 0.000000000000000000, 0.000000000000000000 ) ) ;
#405=AXIS2_PLACEMENT_3D ( 'NONE', #124, #9763, #3187 ) ;
#406=CIRCLE ( 'NONE', #17897, 20.00000000000001066 ) ;
#407=EDGE_LOOP ( 'NONE', ( #6794, #8753, #34477, #34634 ) ) ;
#428=DIRECTION ( 'NONE',  ( 0.000000000000000000, 0.000000000000000000, 1.000000000000000000 ) ) ;
#429=AXIS2_PLACEMENT_3D ( 'NONE', #36616, #10454, #9000 ) ;
#437=DIRECTION ( 'NONE',  ( 0.000000000000000000, -0.9822872507286903865, 0.1873813145857150253 ) ) ;
#441=CARTESIAN_POINT ( 'NONE',  ( 18.00000000000000355, 46.19362259308835661, 8.585149169758654608 ) ) ;
#446=ORIENTED_EDGE ( 'NONE', *, *, #31372, .T. ) ;
#449=CARTESIAN_POINT ( 'NONE',  ( -10.00000000000000000, 0.000000000000000000, 0.000000000000000000 ) ) ;
#453=AXIS2_PLACEMENT_3D ( 'NONE', #35646, #23040, #19334 ) ;
#463=CYLINDRICAL_SURFACE ( 'NONE', #7099, 20.00000000000000711 ) ;
#470=CIRCLE ( 'NONE', #10341, 20.00000000000001421 ) ;
#476=CIRCLE ( 'NONE', #10987, 20.00000000000000355 ) ;
#478=DIRECTION ( 'NONE',  ( -1.000000000000000000, -0.000000000000000000, -0.000000000000000000 ) ) ;
#480=ORIENTED_EDGE ( 'NONE', *, *, #30811, .T. ) ;
#483=CIRCLE ( 'NONE', #29083, 47.49899999999998812 ) ;
#487=ORIENTED_EDGE ( 'NONE', *, *, #21055, .T. ) ;
#494=CARTESIAN_POINT ( 'NONE',  ( 9.000000000000001776, 47.32430374665931794, 21.55018039121544504 ) ) ;
#498=EDGE_LOOP ( 'NONE', ( #22590, #14533, #15559, #34141 ) ) ;
#501=VERTEX_POINT ( 'NONE', #18171 ) ;
#520=DIRECTION ( 'NONE',  ( -1.000000000000000000, 0.000000000000000000, 0.000000000000000000 ) ) ;
#522=CARTESIAN_POINT ( 'NONE',  ( 0.000000000000000000, -11.90021268425586953, 45.45261810511210143 ) ) ;
#525=ORIENTED_EDGE ( 'NONE', *, *, #4876, .F. ) ;
#527=AXIS2_PLACEMENT_3D ( 'NONE', #22171, #5544, #35427 ) ;
#531=ADVANCED_FACE ( 'NONE', ( #5457 ), #18378, .T. ) ;
#533=CARTESIAN_POINT ( 'NONE',  ( 18.00000000000000355, -46.77034588191318676, 22.72740077717213580 ) ) ;
#536=DIRECTION ( 'NONE',  ( 0.000000000000000000, 0.000000000000000000, 1.000000000000000000 ) ) ;
#538=AXIS2_PLACEMENT_3D ( 'NONE', #40650, #40443, #37179 ) ;
#545=EDGE_LOOP ( 'NONE', ( #30373, #28462, #5069, #8099 ) ) ;
#549=CIRCLE ( 'NONE', #35355, 47.49900000000000944 ) ;
#554=CARTESIAN_POINT ( 'NONE',  ( 0.000000000000000000, -42.03146605346771025, -22.12489237027361000 ) ) ;
#563=ADVANCED_FACE ( 'NONE', ( #31437 ), #1736, .T. ) ;
#569=EDGE_CURVE ( 'NONE', #10925, #32031, #2158, .T. ) ;
#570=ORIENTED_EDGE ( 'NONE', *, *, #29147, .T. ) ;
#575=DIRECTION ( 'NONE',  ( -1.000000000000000000, 0.000000000000000000, -0.000000000000000000 ) ) ;
#577=DIRECTION ( 'NONE',  ( 0.000000000000000000, 0.000000000000000000, 1.000000000000000000 ) ) ;
#595=DIRECTION ( 'NONE',  ( -1.000000000000000000, 0.000000000000000000, -0.000000000000000000 ) ) ;
#597=CYLINDRICAL_SURFACE ( 'NONE', #2515, 51.99999999999999289 ) ;
#599=DIRECTION ( 'NONE',  ( -1.000000000000000000, 0.000000000000000000, 0.000000000000000000 ) ) ;
#605=EDGE_CURVE ( 'NONE', #28014, #24263, #266, .T. ) ;
#628=DIRECTION ( 'NONE',  ( -1.000000000000000000, 0.000000000000000000, 0.000000000000000000 ) ) ;
#631=VERTEX_POINT ( 'NONE', #9583 ) ;
#638=DIRECTION ( 'NONE',  ( 0.000000000000000000, 0.000000000000000000, 1.000000000000000000 ) ) ;
#640=VERTEX_POINT ( 'NONE', #32493 ) ;
#643=ORIENTED_EDGE ( 'NONE', *, *, #1416, .F. ) ;
#650=EDGE_CURVE ( 'NONE', #9771, #35135, #17755, .T. ) ;
#653=CYLINDRICAL_SURFACE ( 'NONE', #7831, 20.00000000000000355 ) ;
#662=EDGE_CURVE ( 'NONE', #4953, #16239, #15652, .T. ) ;
#663=DIRECTION ( 'NONE',  ( -1.000000000000000000, -0.000000000000000000, -0.000000000000000000 ) ) ;
#672=DIRECTION ( 'NONE',  ( -1.000000000000000000, 0.000000000000000000, 0.000000000000000000 ) ) ;
#674=CARTESIAN_POINT ( 'NONE',  ( -132.0000507999999968, 0.000000000000000000, 0.000000000000000000 ) ) ;
#676=ORIENTED_EDGE ( 'NONE', *, *, #42452, .F. ) ;
#680=CARTESIAN_POINT ( 'NONE',  ( 18.00000000000000355, 46.87740477351712798, 3.172455868806036694 ) ) ;
#688=EDGE_LOOP ( 'NONE', ( #1604, #9388, #4620, #28390 ) ) ;
#692=ORIENTED_EDGE ( 'NONE', *, *, #322, .F. ) ;
#697=ORIENTED_EDGE ( 'NONE', *, *, #24466, .T. ) ;
#701=ORIENTED_EDGE ( 'NONE', *, *, #14583, .F. ) ;
#708=DIRECTION ( 'NONE',  ( -1.000000000000000000, -0.000000000000000000, -0.000000000000000000 ) ) ;
#712=EDGE_CURVE ( 'NONE', #40198, #14972, #29447, .T. ) ;
#729=ORIENTED_EDGE ( 'NONE', *, *, #41298, .T. ) ;
#730=LINE ( 'NONE', #25424, #7530 ) ;
#741=CARTESIAN_POINT ( 'NONE',  ( 18.00000000000000355, -39.55064067543046491, -25.36340625197400200 ) ) ;
#742=CARTESIAN_POINT ( 'NONE',  ( 0.000000000000000000, -49.25004636492399612, 16.68630974939742018 ) ) ;
#750=CYLINDRICAL_SURFACE ( 'NONE', #21678, 51.99999999999999289 ) ;
#755=VERTEX_POINT ( 'NONE', #6502 ) ;
#762=AXIS2_PLACEMENT_3D ( 'NONE', #975, #19125, #22610 ) ;
#783=CARTESIAN_POINT ( 'NONE',  ( 0.000000000000000000, 44.75336757549799671, -14.30704879393557150 ) ) ;
#784=ORIENTED_EDGE ( 'NONE', *, *, #32544, .F. ) ;
#786=ORIENTED_EDGE ( 'NONE', *, *, #29435, .T. ) ;
#792=EDGE_CURVE ( 'NONE', #22999, #28679, #30309, .T. ) ;
#806=ORIENTED_EDGE ( 'NONE', *, *, #39159, .T. ) ;
#812=ADVANCED_FACE ( 'NONE', ( #40957 ), #1260, .T. ) ;
#818=ORIENTED_EDGE ( 'NONE', *, *, #20409, .F. ) ;
#819=CARTESIAN_POINT ( 'NONE',  ( 9.000000000000001776, -40.47821179127690527, -32.64221760512803172 ) ) ;
#837=DIRECTION ( 'NONE',  ( 0.000000000000000000, 0.000000000000000000, 1.000000000000000000 ) ) ;
#841=CARTESIAN_POINT ( 'NONE',  ( 9.000000000000001776, 49.65209126885763169, 15.44894276735568006 ) ) ;
#846=CARTESIAN_POINT ( 'NONE',  ( 0.000000000000000000, -19.74581912682875284, 48.10512059033386123 ) ) ;
#865=CARTESIAN_POINT ( 'NONE',  ( 18.00000000000000355, -19.44205635905511897, -43.33776004284629124 ) ) ;
#876=CARTESIAN_POINT ( 'NONE',  ( 0.000000000000000000, -20.99948489194451540, 42.60488980472774045 ) ) ;
#879=DIRECTION ( 'NONE',  ( -1.000000000000000000, -0.000000000000000000, 0.000000000000000000 ) ) ;
#881=CARTESIAN_POINT ( 'NONE',  ( 18.00000000000000355, 11.46872990052381880, 45.56340405422447049 ) ) ;
#891=EDGE_CURVE ( 'NONE', #14013, #31709, #31171, .T. ) ;
#900=ORIENTED_EDGE ( 'NONE', *, *, #42670, .F. ) ;
#902=EDGE_LOOP ( 'NONE', ( #20737, #30290, #24579, #39196 ) ) ;
#909=VERTEX_POINT ( 'NONE', #37689 ) ;
#911=AXIS2_PLACEMENT_3D ( 'NONE', #21019, #9699, #10718 ) ;
#914=ORIENTED_EDGE ( 'NONE', *, *, #37764, .T. ) ;
#915=VECTOR ( 'NONE', #26629, 1000.000000000000000 ) ;
#919=CARTESIAN_POINT ( 'NONE',  ( 0.000000000000000000, -44.47301969247456555, 16.68249143361894582 ) ) ;
#923=DIRECTION ( 'NONE',  ( -1.000000000000000000, 0.000000000000000000, -0.000000000000000000 ) ) ;
#926=EDGE_CURVE ( 'NONE', #27914, #34568, #8609, .T. ) ;
#933=AXIS2_PLACEMENT_3D ( 'NONE', #39544, #9680, #23024 ) ;
#944=ORIENTED_EDGE ( 'NONE', *, *, #37002, .T. ) ;
#952=VERTEX_POINT ( 'NONE', #8894 ) ;
#956=EDGE_CURVE ( 'NONE', #20569, #39944, #24280, .T. ) ;
#958=AXIS2_PLACEMENT_3D ( 'NONE', #18288, #37644, #21128 ) ;
#964=CARTESIAN_POINT ( 'NONE',  ( 18.00000000000000355, 0.000000000000000000, 0.000000000000000000 ) ) ;
#966=CARTESIAN_POINT ( 'NONE',  ( 18.00000000000000355, 2.123073309835852296, -47.45152853935331905 ) ) ;
#974=ORIENTED_EDGE ( 'NONE', *, *, #40589, .F. ) ;
#975=CARTESIAN_POINT ( 'NONE',  ( 18.00000000000000355, 0.000000000000000000, 0.000000000000000000 ) ) ;
#976=VERTEX_POINT ( 'NONE', #15272 ) ;
#978=DIRECTION ( 'NONE',  ( -1.000000000000000000, 0.000000000000000000, -0.000000000000000000 ) ) ;
#983=FACE_OUTER_BOUND ( 'NONE', #36703, .T. ) ;
#997=DIRECTION ( 'NONE',  ( -1.000000000000000000, 0.000000000000000000, 0.000000000000000000 ) ) ;
#998=AXIS2_PLACEMENT_3D ( 'NONE', #24641, #24427, #14162 ) ;
#1000=ORIENTED_EDGE ( 'NONE', *, *, #14875, .T. ) ;
#1010=ORIENTED_EDGE ( 'NONE', *, *, #30191, .T. ) ;
#1014=ORIENTED_EDGE ( 'NONE', *, *, #35545, .F. ) ;
#1016=DIRECTION ( 'NONE',  ( -1.000000000000000000, -0.000000000000000000, -0.000000000000000000 ) ) ;
#1020=VERTEX_POINT ( 'NONE', #41166 ) ;
#1021=CARTESIAN_POINT ( 'NONE',  ( 0.000000000000000000, 45.78515115856060191, -12.64416602183617577 ) ) ;
#1032=ORIENTED_EDGE ( 'NONE', *, *, #22720, .T. ) ;
#1033=AXIS2_PLACEMENT_3D ( 'NONE', #6274, #5845, #19201 ) ;
#1066=FACE_OUTER_BOUND ( 'NONE', #10074, .T. ) ;
#1067=AXIS2_PLACEMENT_3D ( 'NONE', #24112, #32133, #25203 ) ;
#1077=ORIENTED_EDGE ( 'NONE', *, *, #32254, .F. ) ;
#1095=CARTESIAN_POINT ( 'NONE',  ( 18.00000000000000355, 46.87740477351718482, 16.82754413119463166 ) ) ;
#1097=ORIENTED_EDGE ( 'NONE', *, *, #35883, .F. ) ;
#1103=VERTEX_POINT ( 'NONE', #43106 ) ;
#1105=EDGE_CURVE ( 'NONE', #15611, #25329, #26347, .T. ) ;
#1111=AXIS2_PLACEMENT_3D ( 'NONE', #4135, #21442, #27296 ) ;
#1115=LINE ( 'NONE', #41249, #32972 ) ;
#1116=CARTESIAN_POINT ( 'NONE',  ( 0.000000000000000000, 0.000000000000000000, 0.000000000000000000 ) ) ;
#1119=ORIENTED_EDGE ( 'NONE', *, *, #1105, .F. ) ;
#1121=LINE ( 'NONE', #5270, #14511 ) ;
#1124=DIRECTION ( 'NONE',  ( -1.000000000000000000, 0.000000000000000000, 0.000000000000000000 ) ) ;
#1125=CARTESIAN_POINT ( 'NONE',  ( 18.00000000000000355, 0.6505223195683098592, 51.99593080916757515 ) ) ;
#1131=EDGE_CURVE ( 'NONE', #1479, #25103, #35694, .T. ) ;
#1132=AXIS2_PLACEMENT_3D ( 'NONE', #26513, #40223, #10359 ) ;
#1133=EDGE_CURVE ( 'NONE', #20337, #15352, #38862, .T. ) ;
#1134=EDGE_LOOP ( 'NONE', ( #26701, #6464, #26573, #27044 ) ) ;
#1144=AXIS2_PLACEMENT_3D ( 'NONE', #30578, #20557, #14211 ) ;
#1148=CARTESIAN_POINT ( 'NONE',  ( 0.000000000000000000, -46.87740477351715640, -3.172455868805708956 ) ) ;
#1150=DIRECTION ( 'NONE',  ( -1.000000000000000000, -0.000000000000000000, -0.000000000000000000 ) ) ;
#1158=ORIENTED_EDGE ( 'NONE', *, *, #7222, .F. ) ;
#1159=AXIS2_PLACEMENT_3D ( 'NONE', #11232, #4885, #21301 ) ;
#1163=EDGE_LOOP ( 'NONE', ( #23182, #25027, #39890, #38508 ) ) ;
#1176=DIRECTION ( 'NONE',  ( 0.000000000000000000, -0.6845471059286952764, 0.7289686274214054462 ) ) ;
#1179=CARTESIAN_POINT ( 'NONE',  ( 0.000000000000000000, 27.79676263918187118, 37.88001506494779846 ) ) ;
#1190=CARTESIAN_POINT ( 'NONE',  ( -10.00000000000000000, 0.000000000000000000, 0.000000000000000000 ) ) ;
#1191=AXIS2_PLACEMENT_3D ( 'NONE', #21747, #1610, #28494 ) ;
#1194=LINE ( 'NONE', #27849, #32826 ) ;
#1204=CARTESIAN_POINT ( 'NONE',  ( -10.00000000000000000, 0.000000000000000000, 0.000000000000000000 ) ) ;
#1205=ORIENTED_EDGE ( 'NONE', *, *, #13432, .T. ) ;
#1217=ORIENTED_EDGE ( 'NONE', *, *, #19654, .T. ) ;
#1220=ORIENTED_EDGE ( 'NONE', *, *, #33956, .F. ) ;
#1221=DIRECTION ( 'NONE',  ( 1.000000000000000000, 0.000000000000000000, 0.000000000000000000 ) ) ;
#1223=DIRECTION ( 'NONE',  ( -1.000000000000000000, -0.000000000000000000, -0.000000000000000000 ) ) ;
#1229=ORIENTED_EDGE ( 'NONE', *, *, #25180, .F. ) ;
#1238=EDGE_LOOP ( 'NONE', ( #38806, #1010, #34766, #20779 ) ) ;
#1247=CARTESIAN_POINT ( 'NONE',  ( 18.00000000000000355, 0.000000000000000000, 0.000000000000000000 ) ) ;
#1253=EDGE_LOOP ( 'NONE', ( #40270, #15926, #15655, #30488 ) ) ;
#1260=CYLINDRICAL_SURFACE ( 'NONE', #17092, 47.49900000000000233 ) ;
#1278=EDGE_CURVE ( 'NONE', #11061, #11670, #23587, .T. ) ;
#1279=ORIENTED_EDGE ( 'NONE', *, *, #36562, .F. ) ;
#1284=DIRECTION ( 'NONE',  ( -1.000000000000000000, -0.000000000000000000, -0.000000000000000000 ) ) ;
#1286=VECTOR ( 'NONE', #26797, 1000.000000000000000 ) ;
#1300=EDGE_CURVE ( 'NONE', #42289, #32276, #30248, .T. ) ;
#1305=CARTESIAN_POINT ( 'NONE',  ( 18.00000000000000355, -39.78933988720132220, 24.98727647984988920 ) ) ;
#1307=DIRECTION ( 'NONE',  ( -1.000000000000000000, 0.000000000000000000, 0.000000000000000000 ) ) ;
#1324=CARTESIAN_POINT ( 'NONE',  ( 9.000000000000001776, 30.03615769709792360, -42.44795908868958634 ) ) ;
#1331=CARTESIAN_POINT ( 'NONE',  ( 18.00000000000000355, -43.83938735307280865, 18.28286404005783083 ) ) ;
#1338=ORIENTED_EDGE ( 'NONE', *, *, #20817, .F. ) ;
#1341=CARTESIAN_POINT ( 'NONE',  ( 0.000000000000000000, 39.64889472655730884, 33.64468972902522381 ) ) ;
#1345=CIRCLE ( 'NONE', #25774, 47.49900000000000944 ) ;
#1374=CIRCLE ( 'NONE', #17434, 20.00000000000000711 ) ;
#1385=CARTESIAN_POINT ( 'NONE',  ( 0.000000000000000000, 0.000000000000000000, 0.000000000000000000 ) ) ;
#1391=ORIENTED_EDGE ( 'NONE', *, *, #30943, .F. ) ;
#1396=VERTEX_POINT ( 'NONE', #26758 ) ;
#1397=ORIENTED_EDGE ( 'NONE', *, *, #35387, .T. ) ;
#1399=PLANE ( 'NONE',  #19376 ) ;
#1403=ORIENTED_EDGE ( 'NONE', *, *, #24830, .F. ) ;
#1404=AXIS2_PLACEMENT_3D ( 'NONE', #10594, #6881, #3377 ) ;
#1413=LINE ( 'NONE', #4915, #35985 ) ;
#1416=EDGE_CURVE ( 'NONE', #42813, #631, #22192, .T. ) ;
#1418=VERTEX_POINT ( 'NONE', #8834 ) ;
#1423=CARTESIAN_POINT ( 'NONE',  ( 9.000000000000001776, -13.56094713063538038, -50.20060470671754160 ) ) ;
#1427=ORIENTED_EDGE ( 'NONE', *, *, #7222, .T. ) ;
#1440=DIRECTION ( 'NONE',  ( -1.000000000000000000, 0.000000000000000000, 0.000000000000000000 ) ) ;
#1441=VERTEX_POINT ( 'NONE', #7969 ) ;
#1447=ORIENTED_EDGE ( 'NONE', *, *, #10542, .F. ) ;
#1464=FACE_OUTER_BOUND ( 'NONE', #33238, .T. ) ;
#1471=ORIENTED_EDGE ( 'NONE', *, *, #31671, .F. ) ;
#1479=VERTEX_POINT ( 'NONE', #41978 ) ;
#1480=DIRECTION ( 'NONE',  ( 0.000000000000000000, -0.9822872507286903865, 0.1873813145857149975 ) ) ;
#1483=CIRCLE ( 'NONE', #31467, 47.49900000000000233 ) ;
#1498=AXIS2_PLACEMENT_3D ( 'NONE', #12904, #5900, #29925 ) ;
#1503=ORIENTED_EDGE ( 'NONE', *, *, #25146, .T. ) ;
#1532=CARTESIAN_POINT ( 'NONE',  ( 0.000000000000000000, 12.30077720129167851, -50.52416135122069107 ) ) ;
#1536=DIRECTION ( 'NONE',  ( 1.000000000000000000, -0.000000000000000000, 0.000000000000000000 ) ) ;
#1537=CARTESIAN_POINT ( 'NONE',  ( 9.000000000000001776, 18.53613841426788511, 48.58406706613909876 ) ) ;
#1538=DIRECTION ( 'NONE',  ( 0.000000000000000000, -0.2486898871648415832, -0.9685831611286344067 ) ) ;
#1547=ADVANCED_BREP_SHAPE_REPRESENTATION ( '', ( #14024, #13552 ), #23928 ) ;
#1550=EDGE_CURVE ( 'NONE', #42889, #32412, #38089, .T. ) ;
#1553=VECTOR ( 'NONE', #41674, 1000.000000000000000 ) ;
#1554=ORIENTED_EDGE ( 'NONE', *, *, #26625, .F. ) ;
#1556=VERTEX_POINT ( 'NONE', #2685 ) ;
#1559=VECTOR ( 'NONE', #8751, 1000.000000000000000 ) ;
#1560=ORIENTED_EDGE ( 'NONE', *, *, #1735, .F. ) ;
#1565=CARTESIAN_POINT ( 'NONE',  ( 0.000000000000000000, 7.162210897276451327, -51.50439529848821252 ) ) ;
#1574=FACE_OUTER_BOUND ( 'NONE', #28406, .T. ) ;
#1584=ORIENTED_EDGE ( 'NONE', *, *, #35545, .T. ) ;
#1597=ORIENTED_EDGE ( 'NONE', *, *, #33469, .T. ) ;
#1599=DIRECTION ( 'NONE',  ( 0.000000000000000000, 0.000000000000000000, 1.000000000000000000 ) ) ;
#1600=CARTESIAN_POINT ( 'NONE',  ( 9.000000000000001776, -44.25018368420724357, -27.31155879685227106 ) ) ;
#1602=DIRECTION ( 'NONE',  ( -1.000000000000000000, -0.000000000000000000, -0.000000000000000000 ) ) ;
#1604=ORIENTED_EDGE ( 'NONE', *, *, #24927, .F. ) ;
#1605=DIRECTION ( 'NONE',  ( -1.000000000000000000, 0.000000000000000000, -0.000000000000000000 ) ) ;
#1606=VERTEX_POINT ( 'NONE', #5979 ) ;
#1610=DIRECTION ( 'NONE',  ( -1.000000000000000000, -0.000000000000000000, 0.000000000000000000 ) ) ;
#1614=LINE ( 'NONE', #25028, #22451 ) ;
#1619=VERTEX_POINT ( 'NONE', #19753 ) ;
#1624=FACE_OUTER_BOUND ( 'NONE', #41541, .T. ) ;
#1632=VERTEX_POINT ( 'NONE', #42825 ) ;
#1637=DIRECTION ( 'NONE',  ( 0.000000000000000000, 0.000000000000000000, 1.000000000000000000 ) ) ;
#1641=DIRECTION ( 'NONE',  ( -1.000000000000000000, -0.000000000000000000, 0.000000000000000000 ) ) ;
#1643=AXIS2_PLACEMENT_3D ( 'NONE', #34065, #36296, #17735 ) ;
#1644=EDGE_CURVE ( 'NONE', #36379, #2044, #19323, .T. ) ;
#1650=DIRECTION ( 'NONE',  ( -1.000000000000000000, 0.000000000000000000, 0.000000000000000000 ) ) ;
#1653=FACE_OUTER_BOUND ( 'NONE', #7306, .T. ) ;
#1655=VERTEX_POINT ( 'NONE', #33020 ) ;
#1668=DIRECTION ( 'NONE',  ( -1.000000000000000000, -0.000000000000000000, -0.000000000000000000 ) ) ;
#1672=DIRECTION ( 'NONE',  ( -1.000000000000000000, 0.000000000000000000, 0.000000000000000000 ) ) ;
#1691=CIRCLE ( 'NONE', #6532, 20.00000000000000711 ) ;
#1711=EDGE_CURVE ( 'NONE', #14485, #3869, #3242, .T. ) ;
#1713=DIRECTION ( 'NONE',  ( 0.000000000000000000, 0.000000000000000000, 1.000000000000000000 ) ) ;
#1716=CARTESIAN_POINT ( 'NONE',  ( 18.00000000000000355, -30.93515269692137792, 36.04401931830242489 ) ) ;
#1735=EDGE_CURVE ( 'NONE', #14587, #36747, #28482, .T. ) ;
#1736=CYLINDRICAL_SURFACE ( 'NONE', #17061, 51.99999999999999289 ) ;
#1747=EDGE_CURVE ( 'NONE', #10605, #21443, #549, .T. ) ;
#1751=VERTEX_POINT ( 'NONE', #27579 ) ;
#1752=DIRECTION ( 'NONE',  ( -1.000000000000000000, 0.000000000000000000, 0.000000000000000000 ) ) ;
#1753=DIRECTION ( 'NONE',  ( -1.000000000000000000, 0.000000000000000000, 0.000000000000000000 ) ) ;
#1765=LINE ( 'NONE', #32517, #6772 ) ;
#1767=CIRCLE ( 'NONE', #21326, 20.00000000000000711 ) ;
#1773=ORIENTED_EDGE ( 'NONE', *, *, #5212, .F. ) ;
#1791=EDGE_CURVE ( 'NONE', #5484, #37859, #483, .T. ) ;
#1800=AXIS2_PLACEMENT_3D ( 'NONE', #38039, #25013, #7935 ) ;
#1802=CARTESIAN_POINT ( 'NONE',  ( 18.00000000000000355, 50.95304419620824632, 10.38206564895679307 ) ) ;
#1808=DIRECTION ( 'NONE',  ( -1.000000000000000000, 0.000000000000000000, -0.000000000000000000 ) ) ;
#1818=FACE_OUTER_BOUND ( 'NONE', #13046, .T. ) ;
#1821=VECTOR ( 'NONE', #36180, 1000.000000000000000 ) ;
#1824=ORIENTED_EDGE ( 'NONE', *, *, #37060, .F. ) ;
#1832=CARTESIAN_POINT ( 'NONE',  ( 0.000000000000000000, 38.92705108641732181, 27.21837053747810486 ) ) ;
#1837=CARTESIAN_POINT ( 'NONE',  ( 18.00000000000000355, 0.000000000000000000, 0.000000000000000000 ) ) ;
#1845=CIRCLE ( 'NONE', #26244, 52.00000000000000000 ) ;
#1847=EDGE_CURVE ( 'NONE', #28966, #22227, #259, .T. ) ;
#1849=EDGE_CURVE ( 'NONE', #13721, #23787, #23523, .T. ) ;
#1853=EDGE_CURVE ( 'NONE', #23198, #41127, #30420, .T. ) ;
#1859=AXIS2_PLACEMENT_3D ( 'NONE', #12679, #347, #35759 ) ;
#1876=EDGE_LOOP ( 'NONE', ( #31239, #28384, #15885, #12832 ) ) ;
#1880=CIRCLE ( 'NONE', #41625, 20.00000000000000711 ) ;
#1882=ORIENTED_EDGE ( 'NONE', *, *, #1133, .F. ) ;
#1887=CARTESIAN_POINT ( 'NONE',  ( 18.00000000000000355, -45.78515115856051665, 12.64416602183649374 ) ) ;
#1892=CIRCLE ( 'NONE', #7469, 47.49900000000000233 ) ;
#1897=CYLINDRICAL_SURFACE ( 'NONE', #19187, 20.00000000000000711 ) ;
#1898=ORIENTED_EDGE ( 'NONE', *, *, #38041, .T. ) ;
#1909=LINE ( 'NONE', #17682, #19718 ) ;
#1916=CIRCLE ( 'NONE', #30499, 20.00000000000000000 ) ;
#1920=AXIS2_PLACEMENT_3D ( 'NONE', #13229, #22634, #26102 ) ;
#1925=ORIENTED_EDGE ( 'NONE', *, *, #28284, .T. ) ;
#1930=DIRECTION ( 'NONE',  ( 1.000000000000000000, 0.000000000000000000, 0.000000000000000000 ) ) ;
#1940=CARTESIAN_POINT ( 'NONE',  ( 0.000000000000000000, 0.000000000000000000, 0.000000000000000000 ) ) ;
#1963=CARTESIAN_POINT ( 'NONE',  ( 0.000000000000000000, 0.000000000000000000, 0.000000000000000000 ) ) ;
#1972=AXIS2_PLACEMENT_3D ( 'NONE', #17498, #27288, #14422 ) ;
#1979=EDGE_CURVE ( 'NONE', #33515, #30585, #22847, .T. ) ;
#1987=ORIENTED_EDGE ( 'NONE', *, *, #38485, .T. ) ;
#1990=CARTESIAN_POINT ( 'NONE',  ( 18.00000000000000355, 38.92705108641770551, -27.21837053747755419 ) ) ;
#1993=VERTEX_POINT ( 'NONE', #31925 ) ;
#1997=DIRECTION ( 'NONE',  ( -1.000000000000000000, 0.000000000000000000, 0.000000000000000000 ) ) ;
#2001=AXIS2_PLACEMENT_3D ( 'NONE', #29527, #25426, #41960 ) ;
#2002=ORIENTED_EDGE ( 'NONE', *, *, #29349, .T. ) ;
#2011=DIRECTION ( 'NONE',  ( -1.000000000000000000, -0.000000000000000000, -0.000000000000000000 ) ) ;
#2035=DIRECTION ( 'NONE',  ( 1.000000000000000000, 0.000000000000000000, 0.000000000000000000 ) ) ;
#2038=DIRECTION ( 'NONE',  ( 0.000000000000000000, 0.000000000000000000, 1.000000000000000000 ) ) ;
#2039=CARTESIAN_POINT ( 'NONE',  ( 18.00000000000000355, 43.83938735307268075, 18.28286404005813637 ) ) ;
#2043=CARTESIAN_POINT ( 'NONE',  ( 18.00000000000000355, 15.49408907645172206, 44.90087086784598824 ) ) ;
#2044=VERTEX_POINT ( 'NONE', #39279 ) ;
#2048=ORIENTED_EDGE ( 'NONE', *, *, #20310, .T. ) ;
#2058=CARTESIAN_POINT ( 'NONE',  ( 18.00000000000000355, -0.2227391519113303131, -46.98410307550732057 ) ) ;
#2062=SURFACE_STYLE_FILL_AREA ( #12134 ) ;
#2063=FACE_OUTER_BOUND ( 'NONE', #34647, .T. ) ;
#2069=ORIENTED_EDGE ( 'NONE', *, *, #42044, .F. ) ;
#2075=EDGE_CURVE ( 'NONE', #17062, #41964, #18621, .T. ) ;
#2086=EDGE_LOOP ( 'NONE', ( #5203, #36771, #19499, #3248 ) ) ;
#2089=ORIENTED_EDGE ( 'NONE', *, *, #42452, .T. ) ;
#2098=CARTESIAN_POINT ( 'NONE',  ( 0.000000000000000000, -11.90021268425522827, -45.45261810511227907 ) ) ;
#2117=AXIS2_PLACEMENT_3D ( 'NONE', #13517, #40309, #26601 ) ;
#2119=ORIENTED_EDGE ( 'NONE', *, *, #17419, .F. ) ;
#2120=CARTESIAN_POINT ( 'NONE',  ( 18.00000000000000355, 0.000000000000000000, 0.000000000000000000 ) ) ;
#2121=ORIENTED_EDGE ( 'NONE', *, *, #21743, .F. ) ;
#2132=DIRECTION ( 'NONE',  ( 0.000000000000000000, 0.000000000000000000, 1.000000000000000000 ) ) ;
#2133=DIRECTION ( 'NONE',  ( -1.000000000000000000, -0.000000000000000000, -0.000000000000000000 ) ) ;
#2136=DIRECTION ( 'NONE',  ( 0.000000000000000000, 0.000000000000000000, 1.000000000000000000 ) ) ;
#2148=AXIS2_PLACEMENT_3D ( 'NONE', #35048, #41148, #41810 ) ;
#2149=EDGE_CURVE ( 'NONE', #15934, #34314, #5196, .T. ) ;
#2158=LINE ( 'NONE', #18600, #37229 ) ;
#2160=CYLINDRICAL_SURFACE ( 'NONE', #40106, 20.00000000000000355 ) ;
#2170=ORIENTED_EDGE ( 'NONE', *, *, #3727, .F. ) ;
#2195=ORIENTED_EDGE ( 'NONE', *, *, #27318, .T. ) ;
#2196=DIRECTION ( 'NONE',  ( -1.000000000000000000, 0.000000000000000000, 0.000000000000000000 ) ) ;
#2203=EDGE_LOOP ( 'NONE', ( #23105, #31689, #40551, #10405 ) ) ;
#2206=EDGE_CURVE ( 'NONE', #37256, #39541, #6562, .T. ) ;
#2213=LINE ( 'NONE', #42135, #39522 ) ;
#2218=CYLINDRICAL_SURFACE ( 'NONE', #26867, 20.00000000000000355 ) ;
#2220=ORIENTED_EDGE ( 'NONE', *, *, #24907, .F. ) ;
#2227=CARTESIAN_POINT ( 'NONE',  ( 0.000000000000000000, 43.83938735307293655, -18.28286404005752530 ) ) ;
#2230=ADVANCED_FACE ( 'NONE', ( #9844 ), #207, .T. ) ;
#2231=LINE ( 'NONE', #29316, #4872 ) ;
#2234=ORIENTED_EDGE ( 'NONE', *, *, #5925, .T. ) ;
#2240=CARTESIAN_POINT ( 'NONE',  ( 0.000000000000000000, -34.03046037009231384, -33.13733193845841640 ) ) ;
#2260=VERTEX_POINT ( 'NONE', #6790 ) ;
#2263=( NAMED_UNIT ( * ) PLANE_ANGLE_UNIT ( ) SI_UNIT ( $, .RADIAN. ) );
#2287=VERTEX_POINT ( 'NONE', #27920 ) ;
#2297=CYLINDRICAL_SURFACE ( 'NONE', #36237, 20.00000000000000355 ) ;
#2304=ADVANCED_FACE ( 'NONE', ( #23196 ), #24887, .T. ) ;
#2308=EDGE_CURVE ( 'NONE', #27480, #2459, #14313, .T. ) ;
#2309=AXIS2_PLACEMENT_3D ( 'NONE', #22613, #32612, #16054 ) ;
#2310=CARTESIAN_POINT ( 'NONE',  ( 18.00000000000000355, -17.50309955389580452, -43.60271849949383949 ) ) ;
#2312=CARTESIAN_POINT ( 'NONE',  ( 18.00000000000000355, -35.11945359308136716, 38.34871548466002622 ) ) ;
#2313=ORIENTED_EDGE ( 'NONE', *, *, #16329, .T. ) ;
#2314=VECTOR ( 'NONE', #37076, 1000.000000000000000 ) ;
#2328=DIRECTION ( 'NONE',  ( 0.000000000000000000, 0.000000000000000000, -1.000000000000000000 ) ) ;
#2330=ORIENTED_EDGE ( 'NONE', *, *, #12459, .F. ) ;
#2334=AXIS2_PLACEMENT_3D ( 'NONE', #13533, #7608, #20969 ) ;
#2336=ORIENTED_EDGE ( 'NONE', *, *, #26033, .T. ) ;
#2338=DIRECTION ( 'NONE',  ( -1.000000000000000000, -0.000000000000000000, -0.000000000000000000 ) ) ;
#2340=ORIENTED_EDGE ( 'NONE', *, *, #9156, .T. ) ;
#2344=DIRECTION ( 'NONE',  ( -1.000000000000000000, -0.000000000000000000, 0.000000000000000000 ) ) ;
#2363=ORIENTED_EDGE ( 'NONE', *, *, #23969, .T. ) ;
#2379=CIRCLE ( 'NONE', #26804, 20.00000000000000711 ) ;
#2383=EDGE_CURVE ( 'NONE', #27751, #5537, #31391, .T. ) ;
#2389=CARTESIAN_POINT ( 'NONE',  ( 18.00000000000000355, 46.11014828289844303, -9.022736828080878624 ) ) ;
#2390=DIRECTION ( 'NONE',  ( 0.000000000000000000, 0.1253332335643046747, -0.9921147013144777649 ) ) ;
#2392=EDGE_LOOP ( 'NONE', ( #15895, #35412, #42434, #41583 ) ) ;
#2397=VECTOR ( 'NONE', #29588, 1000.000000000000000 ) ;
#2398=ORIENTED_EDGE ( 'NONE', *, *, #14492, .T. ) ;
#2399=DIRECTION ( 'NONE',  ( 0.000000000000000000, 0.000000000000000000, 1.000000000000000000 ) ) ;
#2404=LINE ( 'NONE', #15771, #10100 ) ;
#2405=VERTEX_POINT ( 'NONE', #8261 ) ;
#2416=VECTOR ( 'NONE', #25982, 1000.000000000000000 ) ;
#2446=EDGE_CURVE ( 'NONE', #10863, #6408, #42035, .T. ) ;
#2459=VERTEX_POINT ( 'NONE', #29845 ) ;
#2466=DIRECTION ( 'NONE',  ( 0.000000000000000000, 0.000000000000000000, 1.000000000000000000 ) ) ;
#2467=AXIS2_PLACEMENT_3D ( 'NONE', #19428, #19850, #29227 ) ;
#2468=ORIENTED_EDGE ( 'NONE', *, *, #17099, .F. ) ;
#2470=CARTESIAN_POINT ( 'NONE',  ( 0.000000000000000000, 0.000000000000000000, 0.000000000000000000 ) ) ;
#2474=CARTESIAN_POINT ( 'NONE',  ( 0.000000000000000000, 0.000000000000000000, 0.000000000000000000 ) ) ;
#2479=DIRECTION ( 'NONE',  ( -1.000000000000000000, -0.000000000000000000, 0.000000000000000000 ) ) ;
#2481=CARTESIAN_POINT ( 'NONE',  ( 18.00000000000000355, -36.34385289850609979, 29.77717097092063270 ) ) ;
#2488=AXIS2_PLACEMENT_3D ( 'NONE', #1385, #25416, #38035 ) ;
#2491=VECTOR ( 'NONE', #15224, 1000.000000000000000 ) ;
#2492=CARTESIAN_POINT ( 'NONE',  ( 18.00000000000000355, -18.53613841426756537, -48.58406706613921955 ) ) ;
#2515=AXIS2_PLACEMENT_3D ( 'NONE', #13950, #27245, #24216 ) ;
#2517=AXIS2_PLACEMENT_3D ( 'NONE', #4483, #1223, #25066 ) ;
#2519=FACE_OUTER_BOUND ( 'NONE', #5497, .T. ) ;
#2525=STYLED_ITEM ( 'NONE', ( #13382 ), #14024 ) ;
#2532=AXIS2_PLACEMENT_3D ( 'NONE', #18376, #11584, #18814 ) ;
#2542=VECTOR ( 'NONE', #36090, 1000.000000000000000 ) ;
#2543=PRODUCT_DEFINITION_SHAPE ( 'NONE', 'NONE',  #15380 ) ;
#2552=CIRCLE ( 'NONE', #1159, 20.00000000000000711 ) ;
#2553=ORIENTED_EDGE ( 'NONE', *, *, #2795, .T. ) ;
#2559=CIRCLE ( 'NONE', #26982, 52.00000000000000000 ) ;
#2561=ADVANCED_FACE ( 'NONE', ( #6461 ), #19815, .T. ) ;
#2565=DIRECTION ( 'NONE',  ( 0.000000000000000000, 0.000000000000000000, 1.000000000000000000 ) ) ;
#2572=FACE_OUTER_BOUND ( 'NONE', #34341, .T. ) ;
#2574=ORIENTED_EDGE ( 'NONE', *, *, #25288, .F. ) ;
#2575=EDGE_LOOP ( 'NONE', ( #10483, #23882, #32202, #22823 ) ) ;
#2577=VERTEX_POINT ( 'NONE', #29407 ) ;
#2585=VECTOR ( 'NONE', #39909, 1000.000000000000000 ) ;
#2591=EDGE_LOOP ( 'NONE', ( #15301, #13878, #36634, #3742 ) ) ;
#2604=AXIS2_PLACEMENT_3D ( 'NONE', #18901, #12109, #12325 ) ;
#2611=ORIENTED_EDGE ( 'NONE', *, *, #15356, .F. ) ;
#2614=CARTESIAN_POINT ( 'NONE',  ( 9.000000000000001776, 7.162210897275726573, 51.50439529848830489 ) ) ;
#2615=AXIS2_PLACEMENT_3D ( 'NONE', #7940, #20878, #10365 ) ;
#2617=LINE ( 'NONE', #29275, #23163 ) ;
#2619=DIRECTION ( 'NONE',  ( 0.000000000000000000, -0.9048270524660145808, -0.4257792915650830956 ) ) ;
#2621=CARTESIAN_POINT ( 'NONE',  ( -10.00000000000000000, 0.000000000000000000, 0.000000000000000000 ) ) ;
#2664=AXIS2_PLACEMENT_3D ( 'NONE', #30080, #22922, #32692 ) ;
#2671=ADVANCED_FACE ( 'NONE', ( #16973 ), #30257, .T. ) ;
#2677=EDGE_LOOP ( 'NONE', ( #35857, #1584, #37806, #13347 ) ) ;
#2684=CYLINDRICAL_SURFACE ( 'NONE', #5681, 20.00000000000000711 ) ;
#2685=CARTESIAN_POINT ( 'NONE',  ( 0.000000000000000000, -8.053585752062225822, 46.81126742072019908 ) ) ;
#2690=SURFACE_SIDE_STYLE ('',( #2062 ) ) ;
#2697=CYLINDRICAL_SURFACE ( 'NONE', #34608, 20.00000000000000711 ) ;
#2698=VERTEX_POINT ( 'NONE', #24393 ) ;
#2700=CARTESIAN_POINT ( 'NONE',  ( 0.000000000000000000, 17.08890430202814059, -43.76671000081927332 ) ) ;
#2729=ORIENTED_EDGE ( 'NONE', *, *, #39408, .T. ) ;
#2732=CYLINDRICAL_SURFACE ( 'NONE', #23156, 20.00000000000000355 ) ;
#2736=DIRECTION ( 'NONE',  ( -1.000000000000000000, 0.000000000000000000, 0.000000000000000000 ) ) ;
#2747=VERTEX_POINT ( 'NONE', #33518 ) ;
#2755=ORIENTED_EDGE ( 'NONE', *, *, #4486, .F. ) ;
#2761=CYLINDRICAL_SURFACE ( 'NONE', #8935, 51.99999999999999289 ) ;
#2766=CARTESIAN_POINT ( 'NONE',  ( -10.00000000000000000, 0.000000000000000000, 0.000000000000000000 ) ) ;
#2769=CARTESIAN_POINT ( 'NONE',  ( 0.000000000000000000, -45.78515115856033901, -12.64416602183713856 ) ) ;
#2774=ORIENTED_EDGE ( 'NONE', *, *, #15826, .T. ) ;
#2780=CARTESIAN_POINT ( 'NONE',  ( 0.000000000000000000, -44.61570720899084819, -14.73072383765613047 ) ) ;
#2783=AXIS2_PLACEMENT_3D ( 'NONE', #2780, #15513, #25962 ) ;
#2786=DIRECTION ( 'NONE',  ( -1.000000000000000000, 0.000000000000000000, -0.000000000000000000 ) ) ;
#2795=EDGE_CURVE ( 'NONE', #34535, #18339, #15424, .T. ) ;
#2797=DIRECTION ( 'NONE',  ( 0.000000000000000000, -6.982962677686265922E-15, 1.000000000000000000 ) ) ;
#2801=AXIS2_PLACEMENT_3D ( 'NONE', #22721, #9598, #2797 ) ;
#2808=DIRECTION ( 'NONE',  ( 0.000000000000000000, 0.000000000000000000, 1.000000000000000000 ) ) ;
#2825=ORIENTED_EDGE ( 'NONE', *, *, #10355, .F. ) ;
#2834=ORIENTED_EDGE ( 'NONE', *, *, #5212, .T. ) ;
#2835=DIRECTION ( 'NONE',  ( -1.000000000000000000, 0.000000000000000000, 0.000000000000000000 ) ) ;
#2836=LINE ( 'NONE', #20515, #32471 ) ;
#2848=EDGE_CURVE ( 'NONE', #14923, #25035, #4710, .T. ) ;
#2850=VECTOR ( 'NONE', #32606, 1000.000000000000000 ) ;
#2868=CIRCLE ( 'NONE', #26589, 20.00000000000000711 ) ;
#2871=CYLINDRICAL_SURFACE ( 'NONE', #42323, 20.00000000000000355 ) ;
#2875=CARTESIAN_POINT ( 'NONE',  ( -10.00000000000000000, 0.000000000000000000, 0.000000000000000000 ) ) ;
#2878=VECTOR ( 'NONE', #18435, 1000.000000000000000 ) ;
#2883=ORIENTED_EDGE ( 'NONE', *, *, #20947, .T. ) ;
#2885=ORIENTED_EDGE ( 'NONE', *, *, #7704, .T. ) ;
#2890=CARTESIAN_POINT ( 'NONE',  ( 0.000000000000000000, -36.34385289850609979, 29.77717097092063270 ) ) ;
#2894=VERTEX_POINT ( 'NONE', #36297 ) ;
#2900=AXIS2_PLACEMENT_3D ( 'NONE', #38184, #31229, #17728 ) ;
#2908=ADVANCED_FACE ( 'NONE', ( #22406 ), #15841, .T. ) ;
#2909=FACE_OUTER_BOUND ( 'NONE', #3989, .T. ) ;
#2930=AXIS2_PLACEMENT_3D ( 'NONE', #9324, #2963, #35932 ) ;
#2932=VERTEX_POINT ( 'NONE', #36505 ) ;
#2945=DIRECTION ( 'NONE',  ( -1.000000000000000000, 0.000000000000000000, -0.000000000000000000 ) ) ;
#2952=DIRECTION ( 'NONE',  ( -1.000000000000000000, 0.000000000000000000, -0.000000000000000000 ) ) ;
#2954=EDGE_CURVE ( 'NONE', #20442, #13064, #5771, .T. ) ;
#2963=DIRECTION ( 'NONE',  ( -1.000000000000000000, 0.000000000000000000, 0.000000000000000000 ) ) ;
#2971=ORIENTED_EDGE ( 'NONE', *, *, #29004, .T. ) ;
#2982=ADVANCED_FACE ( 'NONE', ( #25881 ), #22837, .T. ) ;
#2985=ORIENTED_EDGE ( 'NONE', *, *, #29586, .T. ) ;
#2991=CARTESIAN_POINT ( 'NONE',  ( 18.00000000000000355, 3.840921266750508156, -47.34345070675165346 ) ) ;
#2996=CARTESIAN_POINT ( 'NONE',  ( 9.000000000000001776, 13.56094713063571433, 50.20060470671744213 ) ) ;
#2999=CARTESIAN_POINT ( 'NONE',  ( 0.000000000000000000, -39.55064067543082018, 25.36340625197346199 ) ) ;
#3001=LINE ( 'NONE', #6307, #5089 ) ;
#3005=EDGE_CURVE ( 'NONE', #27946, #17810, #34479, .T. ) ;
#3008=EDGE_CURVE ( 'NONE', #23020, #21806, #5211, .T. ) ;
#3009=VERTEX_POINT ( 'NONE', #12774 ) ;
#3013=CARTESIAN_POINT ( 'NONE',  ( 18.00000000000000355, 30.93515269692163017, -36.04401931830219752 ) ) ;
#3026=LINE ( 'NONE', #22969, #13149 ) ;
#3028=ORIENTED_EDGE ( 'NONE', *, *, #8866, .T. ) ;
#3051=EDGE_CURVE ( 'NONE', #21806, #33051, #29789, .T. ) ;
#3056=CARTESIAN_POINT ( 'NONE',  ( 18.00000000000000355, 5.667686777402355602, -46.64153600743599526 ) ) ;
#3057=EDGE_CURVE ( 'NONE', #8971, #16736, #14291, .T. ) ;
#3059=VERTEX_POINT ( 'NONE', #17792 ) ;
#3060=CARTESIAN_POINT ( 'NONE',  ( 18.00000000000000355, 49.25004636492411692, -16.68630974939707556 ) ) ;
#3069=DIRECTION ( 'NONE',  ( -1.000000000000000000, -0.000000000000000000, -0.000000000000000000 ) ) ;
#3074=DIRECTION ( 'NONE',  ( -1.000000000000000000, -0.000000000000000000, -0.000000000000000000 ) ) ;
#3078=EDGE_CURVE ( 'NONE', #4859, #12278, #2379, .T. ) ;
#3081=CARTESIAN_POINT ( 'NONE',  ( 18.00000000000000355, 17.50309955389674954, -43.60271849949345579 ) ) ;
#3082=ADVANCED_FACE ( 'NONE', ( #24343 ), #10350, .T. ) ;
#3090=AXIS2_PLACEMENT_3D ( 'NONE', #25677, #7270, #26935 ) ;
#3114=DIRECTION ( 'NONE',  ( -1.000000000000000000, -0.000000000000000000, -0.000000000000000000 ) ) ;
#3121=ORIENTED_EDGE ( 'NONE', *, *, #24456, .F. ) ;
#3126=CIRCLE ( 'NONE', #5254, 20.00000000000000711 ) ;
#3133=DIRECTION ( 'NONE',  ( -1.000000000000000000, 0.000000000000000000, -0.000000000000000000 ) ) ;
#3136=AXIS2_PLACEMENT_3D ( 'NONE', #40057, #20708, #4063 ) ;
#3138=CARTESIAN_POINT ( 'NONE',  ( 18.00000000000000355, 9.744342220503391161, 46.48873837489801275 ) ) ;
#3141=CARTESIAN_POINT ( 'NONE',  ( 18.00000000000000355, 0.000000000000000000, 0.000000000000000000 ) ) ;
#3145=ADVANCED_FACE ( 'NONE', ( #17367 ), #17578, .T. ) ;
#3153=EDGE_LOOP ( 'NONE', ( #6838, #19531, #20948, #13257 ) ) ;
#3154=VERTEX_POINT ( 'NONE', #14279 ) ;
#3159=EDGE_CURVE ( 'NONE', #7094, #4717, #13866, .T. ) ;
#3161=DIRECTION ( 'NONE',  ( 1.000000000000000000, -0.000000000000000000, -0.000000000000000000 ) ) ;
#3162=DIRECTION ( 'NONE',  ( -1.000000000000000000, 0.000000000000000000, 0.000000000000000000 ) ) ;
#3176=CARTESIAN_POINT ( 'NONE',  ( 0.000000000000000000, -47.00885577955416039, 6.806061952192135500 ) ) ;
#3180=CYLINDRICAL_SURFACE ( 'NONE', #12967, 47.49900000000000233 ) ;
#3185=ORIENTED_EDGE ( 'NONE', *, *, #3193, .T. ) ;
#3187=DIRECTION ( 'NONE',  ( 0.000000000000000000, -0.4817536741017223179, 0.8763066800438596982 ) ) ;
#3189=CARTESIAN_POINT ( 'NONE',  ( 0.000000000000000000, -5.871425383721176061, -51.66745943012289644 ) ) ;
#3192=VERTEX_POINT ( 'NONE', #26715 ) ;
#3193=EDGE_CURVE ( 'NONE', #909, #17108, #12888, .T. ) ;
#3200=CARTESIAN_POINT ( 'NONE',  ( 18.00000000000000355, 47.00885577955412487, 6.806061952192453468 ) ) ;
#3205=CARTESIAN_POINT ( 'NONE',  ( 0.000000000000000000, 44.61570720899074161, 14.73072383765644133 ) ) ;
#3223=VERTEX_POINT ( 'NONE', #23468 ) ;
#3226=AXIS2_PLACEMENT_3D ( 'NONE', #4499, #35044, #4735 ) ;
#3231=AXIS2_PLACEMENT_3D ( 'NONE', #12731, #26035, #16224 ) ;
#3234=ADVANCED_FACE ( 'NONE', ( #6850 ), #20204, .T. ) ;
#3242=CIRCLE ( 'NONE', #8242, 47.49899999999999523 ) ;
#3245=DIRECTION ( 'NONE',  ( 0.000000000000000000, 0.000000000000000000, -1.000000000000000000 ) ) ;
#3248=ORIENTED_EDGE ( 'NONE', *, *, #42169, .T. ) ;
#3253=DIRECTION ( 'NONE',  ( -1.000000000000000000, 0.000000000000000000, 0.000000000000000000 ) ) ;
#3256=DIRECTION ( 'NONE',  ( 0.000000000000000000, 0.000000000000000000, 1.000000000000000000 ) ) ;
#3267=ORIENTED_EDGE ( 'NONE', *, *, #28812, .F. ) ;
#3270=LINE ( 'NONE', #16648, #20612 ) ;
#3284=LINE ( 'NONE', #1537, #32337 ) ;
#3295=ORIENTED_EDGE ( 'NONE', *, *, #42552, .T. ) ;
#3300=CARTESIAN_POINT ( 'NONE',  ( 0.000000000000000000, 0.000000000000000000, 0.000000000000000000 ) ) ;
#3322=EDGE_CURVE ( 'NONE', #291, #30171, #8788, .T. ) ;
#3323=ORIENTED_EDGE ( 'NONE', *, *, #21761, .F. ) ;
#3341=ORIENTED_EDGE ( 'NONE', *, *, #3008, .T. ) ;
#3344=EDGE_CURVE ( 'NONE', #1751, #29967, #21275, .T. ) ;
#3347=CARTESIAN_POINT ( 'NONE',  ( -10.00000000000000000, 0.000000000000000000, 0.000000000000000000 ) ) ;
#3349=ORIENTED_EDGE ( 'NONE', *, *, #5609, .T. ) ;
#3354=EDGE_LOOP ( 'NONE', ( #2825, #40400, #8127, #15878 ) ) ;
#3359=CARTESIAN_POINT ( 'NONE',  ( 0.000000000000000000, -36.34385289850569478, -29.77717097092114429 ) ) ;
#3360=CIRCLE ( 'NONE', #40302, 20.00000000000000711 ) ;
#3364=DIRECTION ( 'NONE',  ( 1.000000000000000000, -0.000000000000000000, -0.000000000000000000 ) ) ;
#3373=CYLINDRICAL_SURFACE ( 'NONE', #11096, 20.00000000000000355 ) ;
#3374=ORIENTED_EDGE ( 'NONE', *, *, #38041, .F. ) ;
#3377=DIRECTION ( 'NONE',  ( 0.000000000000000000, 0.000000000000000000, -1.000000000000000000 ) ) ;
#3379=ORIENTED_EDGE ( 'NONE', *, *, #31376, .T. ) ;
#3380=ORIENTED_EDGE ( 'NONE', *, *, #1979, .F. ) ;
#3386=CIRCLE ( 'NONE', #38964, 20.00000000000000355 ) ;
#3388=CARTESIAN_POINT ( 'NONE',  ( 150.0000507999999968, 0.000000000000000000, 0.000000000000000000 ) ) ;
#3393=CARTESIAN_POINT ( 'NONE',  ( 0.000000000000000000, 0.000000000000000000, 0.000000000000000000 ) ) ;
#3397=DIRECTION ( 'NONE',  ( -1.000000000000000000, -0.000000000000000000, -0.000000000000000000 ) ) ;
#3399=ADVANCED_FACE ( 'NONE', ( #22147 ), #5520, .T. ) ;
#3409=EDGE_CURVE ( 'NONE', #38711, #28617, #26241, .T. ) ;
#3422=ORIENTED_EDGE ( 'NONE', *, *, #3879, .T. ) ;
#3424=AXIS2_PLACEMENT_3D ( 'NONE', #17051, #23172, #13551 ) ;
#3426=CARTESIAN_POINT ( 'NONE',  ( 9.000000000000001776, -49.65209126885773827, 15.44894276735532834 ) ) ;
#3428=DIRECTION ( 'NONE',  ( -1.000000000000000000, 0.000000000000000000, 0.000000000000000000 ) ) ;
#3434=ORIENTED_EDGE ( 'NONE', *, *, #3548, .T. ) ;
#3446=AXIS2_PLACEMENT_3D ( 'NONE', #33041, #16278, #25692 ) ;
#3449=VERTEX_POINT ( 'NONE', #9422 ) ;
#3475=VECTOR ( 'NONE', #5005, 1000.000000000000000 ) ;
#3486=ORIENTED_EDGE ( 'NONE', *, *, #29791, .F. ) ;
#3492=ADVANCED_FACE ( 'NONE', ( #38888 ), #2218, .T. ) ;
#3500=LINE ( 'NONE', #37329, #22695 ) ;
#3502=CARTESIAN_POINT ( 'NONE',  ( 18.00000000000000355, 24.72041153920732981, 40.55929306992697292 ) ) ;
#3504=AXIS2_PLACEMENT_3D ( 'NONE', #10199, #13722, #40503 ) ;
#3505=DIRECTION ( 'NONE',  ( 0.000000000000000000, 0.000000000000000000, -1.000000000000000000 ) ) ;
#3509=ORIENTED_EDGE ( 'NONE', *, *, #16971, .F. ) ;
#3516=VERTEX_POINT ( 'NONE', #26452 ) ;
#3529=ORIENTED_EDGE ( 'NONE', *, *, #39408, .F. ) ;
#3540=ORIENTED_EDGE ( 'NONE', *, *, #22669, .T. ) ;
#3543=DIRECTION ( 'NONE',  ( -1.000000000000000000, 0.000000000000000000, 0.000000000000000000 ) ) ;
#3548=EDGE_CURVE ( 'NONE', #36864, #31070, #34513, .T. ) ;
#3551=DIRECTION ( 'NONE',  ( 0.000000000000000000, 0.000000000000000000, 1.000000000000000000 ) ) ;
#3562=EDGE_CURVE ( 'NONE', #20877, #28679, #3500, .T. ) ;
#3573=DIRECTION ( 'NONE',  ( -1.000000000000000000, 0.000000000000000000, 0.000000000000000000 ) ) ;
#3575=ORIENTED_EDGE ( 'NONE', *, *, #20808, .T. ) ;
#3578=CARTESIAN_POINT ( 'NONE',  ( 18.00000000000000355, 42.03146605346785947, 22.12489237027331512 ) ) ;
#3583=DIRECTION ( 'NONE',  ( 0.000000000000000000, -0.2486898871648415832, -0.9685831611286344067 ) ) ;
#3587=ORIENTED_EDGE ( 'NONE', *, *, #35757, .F. ) ;
#3601=CIRCLE ( 'NONE', #28048, 51.99999999999999289 ) ;
#3608=DIRECTION ( 'NONE',  ( 0.000000000000000000, -0.9822872507286903865, 0.1873813145857150808 ) ) ;
#3609=ORIENTED_EDGE ( 'NONE', *, *, #22877, .T. ) ;
#3617=DIRECTION ( 'NONE',  ( -1.000000000000000000, 0.000000000000000000, 0.000000000000000000 ) ) ;
#3620=EDGE_LOOP ( 'NONE', ( #39500, #12729, #22297, #202 ) ) ;
#3622=AXIS2_PLACEMENT_3D ( 'NONE', #36254, #23426, #36686 ) ;
#3631=CARTESIAN_POINT ( 'NONE',  ( 9.000000000000001776, 50.95304419620838843, -10.38206564895608786 ) ) ;
#3639=ADVANCED_FACE ( 'NONE', ( #13586 ), #26884, .T. ) ;
#3649=CARTESIAN_POINT ( 'NONE',  ( 18.00000000000000355, 39.78933988720149273, -24.98727647984960498 ) ) ;
#3651=CARTESIAN_POINT ( 'NONE',  ( 0.000000000000000000, 32.32520163883584274, 34.09746168776050013 ) ) ;
#3656=DIRECTION ( 'NONE',  ( -1.000000000000000000, 0.000000000000000000, 0.000000000000000000 ) ) ;
#3657=EDGE_LOOP ( 'NONE', ( #35777, #16401, #31053, #6724 ) ) ;
#3665=DIRECTION ( 'NONE',  ( -1.000000000000000000, 0.000000000000000000, 0.000000000000000000 ) ) ;
#3668=CARTESIAN_POINT ( 'NONE',  ( 0.000000000000000000, -36.06787431788649911, -37.45808914225526820 ) ) ;
#3669=DIRECTION ( 'NONE',  ( 0.000000000000000000, 0.3681245526846786964, -0.9297764858882511252 ) ) ;
#3673=CARTESIAN_POINT ( 'NONE',  ( 18.00000000000000355, -31.08872492059927595, -41.68322423723131465 ) ) ;
#3680=ORIENTED_EDGE ( 'NONE', *, *, #27734, .F. ) ;
#3682=VERTEX_POINT ( 'NONE', #17318 ) ;
#3683=EDGE_CURVE ( 'NONE', #37859, #17810, #27317, .T. ) ;
#3691=DIRECTION ( 'NONE',  ( -1.000000000000000000, 0.000000000000000000, 0.000000000000000000 ) ) ;
#3702=ORIENTED_EDGE ( 'NONE', *, *, #7845, .T. ) ;
#3706=ORIENTED_EDGE ( 'NONE', *, *, #5925, .F. ) ;
#3717=LINE ( 'NONE', #40389, #37065 ) ;
#3727=EDGE_CURVE ( 'NONE', #37240, #9333, #3284, .T. ) ;
#3740=EDGE_CURVE ( 'NONE', #23341, #33051, #24724, .T. ) ;
#3742=ORIENTED_EDGE ( 'NONE', *, *, #12506, .T. ) ;
#3750=DIRECTION ( 'NONE',  ( -1.000000000000000000, 0.000000000000000000, 0.000000000000000000 ) ) ;
#3751=DIRECTION ( 'NONE',  ( 0.000000000000000000, 0.000000000000000000, 1.000000000000000000 ) ) ;
#3758=CIRCLE ( 'NONE', #28208, 51.99999999999999289 ) ;
#3765=ADVANCED_FACE ( 'NONE', ( #41686 ), #18620, .T. ) ;
#3768=FACE_OUTER_BOUND ( 'NONE', #42830, .T. ) ;
#3772=AXIS2_PLACEMENT_3D ( 'NONE', #29357, #38933, #26299 ) ;
#3774=CYLINDRICAL_SURFACE ( 'NONE', #2615, 20.00000000000000355 ) ;
#3776=DIRECTION ( 'NONE',  ( 0.000000000000000000, 0.2486898871648483278, 0.9685831611286327414 ) ) ;
#3778=CLOSED_SHELL ( 'NONE', ( #7954, #24081, #17418, #24457, #27680, #30678, #2671, #16076, #28476, #9225, #26608, #42376, #37307, #31574, #5546, #42553, #283, #26396, #18331, #39239, #7829, #16380, #14380, #11847, #11276, #2304, #34821, #38037, #31679, #2982, #9918, #6212, #40968, #22931, #33695, #25396, #13267, #21109, #19532, #27393, #42922, #563, #16597, #15431, #17980, #10109, #29291, #14900, #23573, #12951, #39893, #15630, #33486, #18889, #4184, #25779, #13943, #39286, #15114, #28698, #16842, #33136, #11785, #33174, #31853, #40136, #16028, #40026, #13483, #28829, #23018, #12091, #23135, #23053, #3399, #6296, #23307, #30240, #3492, #32937, #22449, #33340, #11448, #2561, #24265, #3082, #9817, #2908, #20072, #35055, #14937, #41537, #28118, #22490, #531, #25266, #16497, #41096, #17462, #40730, #12025, #26822, #32770, #40985, #13293, #25972, #35332, #35827, #32249, #29799, #24494, #40365, #6575, #16636, #25350, #39529, #32711, #21846, #30865, #28535, #5590, #27656, #3234, #17190, #35867, #6131, #8629, #22174, #16923, #36362, #32186, #23940, #31596, #26335, #9187, #11405, #42607, #20190, #23748, #18714, #3639, #7100, #42844, #13798, #23091, #9250, #23870, #12845, #27801, #10175, #24284, #31200, #12882, #39112, #10546, #28090, #26037, #23126, #33929, #41933, #21955, #39603, #15760, #15959, #17473, #14269, #17026, #13501, #14829, #22057, #14880, #2230, #17925, #42704, #3145, #11491, #42318, #14681, #27420, #25162, #31833, #5522, #20876, #11174, #11945, #40083, #41646, #3765, #33509, #42994, #42097, #812, #7703, #36587, #19934, #32959, #20547, #38095, #108, #35500, #37219, #3916, #26627, #24146, #39629, #15537, #10613, #40556, #24607, #33344 ) ) ;
#3779=CARTESIAN_POINT ( 'NONE',  ( 18.00000000000000355, 0.000000000000000000, 0.000000000000000000 ) ) ;
#3783=VECTOR ( 'NONE', #40726, 1000.000000000000000 ) ;
#3793=CIRCLE ( 'NONE', #9392, 20.00000000000000711 ) ;
#3808=ORIENTED_EDGE ( 'NONE', *, *, #10827, .F. ) ;
#3816=CIRCLE ( 'NONE', #28274, 20.00000000000000355 ) ;
#3817=DIRECTION ( 'NONE',  ( -1.000000000000000000, -0.000000000000000000, 0.000000000000000000 ) ) ;
#3818=VERTEX_POINT ( 'NONE', #38406 ) ;
#3830=CIRCLE ( 'NONE', #26180, 20.00000000000000000 ) ;
#3834=DIRECTION ( 'NONE',  ( -1.000000000000000000, 0.000000000000000000, -0.000000000000000000 ) ) ;
#3835=FACE_OUTER_BOUND ( 'NONE', #10840, .T. ) ;
#3843=ORIENTED_EDGE ( 'NONE', *, *, #33671, .F. ) ;
#3852=CARTESIAN_POINT ( 'NONE',  ( 0.000000000000000000, 0.000000000000000000, 0.000000000000000000 ) ) ;
#3864=CIRCLE ( 'NONE', #31785, 20.00000000000000711 ) ;
#3867=CARTESIAN_POINT ( 'NONE',  ( 0.000000000000000000, -44.47301969247432396, -16.68249143361957465 ) ) ;
#3869=VERTEX_POINT ( 'NONE', #7660 ) ;
#3872=ORIENTED_EDGE ( 'NONE', *, *, #29001, .F. ) ;
#3874=CYLINDRICAL_SURFACE ( 'NONE', #5633, 20.00000000000000355 ) ;
#3879=EDGE_CURVE ( 'NONE', #39306, #38951, #26166, .T. ) ;
#3881=ORIENTED_EDGE ( 'NONE', *, *, #27541, .T. ) ;
#3884=EDGE_CURVE ( 'NONE', #8604, #13205, #21463, .T. ) ;
#3888=AXIS2_PLACEMENT_3D ( 'NONE', #23696, #30215, #27596 ) ;
#3893=LINE ( 'NONE', #43178, #915 ) ;
#3899=ORIENTED_EDGE ( 'NONE', *, *, #36187, .F. ) ;
#3904=CARTESIAN_POINT ( 'NONE',  ( 18.00000000000000355, -15.49408907645202937, 44.90087086784588166 ) ) ;
#3915=AXIS2_PLACEMENT_3D ( 'NONE', #15112, #5250, #28416 ) ;
#3916=ADVANCED_FACE ( 'NONE', ( #39037 ), #22308, .T. ) ;
#3920=AXIS2_PLACEMENT_3D ( 'NONE', #6424, #520, #36517 ) ;
#3938=DIRECTION ( 'NONE',  ( 0.000000000000000000, 0.000000000000000000, -1.000000000000000000 ) ) ;
#3944=DIRECTION ( 'NONE',  ( -1.000000000000000000, -0.000000000000000000, -0.000000000000000000 ) ) ;
#3952=ORIENTED_EDGE ( 'NONE', *, *, #5296, .F. ) ;
#3954=CARTESIAN_POINT ( 'NONE',  ( 18.00000000000000355, 34.03046037009303149, -33.13733193845768454 ) ) ;
#3967=ORIENTED_EDGE ( 'NONE', *, *, #18558, .F. ) ;
#3981=CARTESIAN_POINT ( 'NONE',  ( 18.00000000000000355, 0.000000000000000000, 0.000000000000000000 ) ) ;
#3983=DIRECTION ( 'NONE',  ( -1.000000000000000000, 0.000000000000000000, 0.000000000000000000 ) ) ;
#3989=EDGE_LOOP ( 'NONE', ( #17339, #7233, #33464, #23683 ) ) ;
#3990=DIRECTION ( 'NONE',  ( -1.000000000000000000, 0.000000000000000000, 0.000000000000000000 ) ) ;
#3994=ORIENTED_EDGE ( 'NONE', *, *, #30132, .T. ) ;
#3996=CYLINDRICAL_SURFACE ( 'NONE', #35884, 20.00000000000001066 ) ;
#3998=AXIS2_PLACEMENT_3D ( 'NONE', #13953, #17675, #6939 ) ;
#4001=CARTESIAN_POINT ( 'NONE',  ( 0.000000000000000000, 35.11945359308111136, 38.34871548466026070 ) ) ;
#4003=DIRECTION ( 'NONE',  ( -1.000000000000000000, 0.000000000000000000, 0.000000000000000000 ) ) ;
#4017=DIRECTION ( 'NONE',  ( -1.000000000000000000, -0.000000000000000000, -0.000000000000000000 ) ) ;
#4020=DIRECTION ( 'NONE',  ( 0.000000000000000000, -0.9822872507286865007, -0.1873813145857355367 ) ) ;
#4024=CIRCLE ( 'NONE', #38890, 20.00000000000001066 ) ;
#4046=FACE_OUTER_BOUND ( 'NONE', #37576, .T. ) ;
#4049=CIRCLE ( 'NONE', #34036, 20.00000000000000000 ) ;
#4050=ORIENTED_EDGE ( 'NONE', *, *, #28300, .T. ) ;
#4056=CYLINDRICAL_SURFACE ( 'NONE', #4875, 20.00000000000000355 ) ;
#4058=VERTEX_POINT ( 'NONE', #38535 ) ;
#4060=VERTEX_POINT ( 'NONE', #28338 ) ;
#4061=CARTESIAN_POINT ( 'NONE',  ( 18.00000000000000355, 15.49408907645172206, 44.90087086784598824 ) ) ;
#4063=DIRECTION ( 'NONE',  ( 0.000000000000000000, 0.000000000000000000, 1.000000000000000000 ) ) ;
#4065=ORIENTED_EDGE ( 'NONE', *, *, #9204, .F. ) ;
#4068=VERTEX_POINT ( 'NONE', #21601 ) ;
#4072=ORIENTED_EDGE ( 'NONE', *, *, #1416, .T. ) ;
#4078=CIRCLE ( 'NONE', #2001, 20.00000000000001066 ) ;
#4080=ORIENTED_EDGE ( 'NONE', *, *, #25929, .T. ) ;
#4081=DIRECTION ( 'NONE',  ( -1.000000000000000000, -0.000000000000000000, -0.000000000000000000 ) ) ;
#4097=CARTESIAN_POINT ( 'NONE',  ( 18.00000000000000355, 5.667686777401707232, 46.64153600743607342 ) ) ;
#4103=AXIS2_PLACEMENT_3D ( 'NONE', #14756, #21322, #41318 ) ;
#4135=CARTESIAN_POINT ( 'NONE',  ( 0.000000000000000000, -6.109652351742118626, 46.58570277113506819 ) ) ;
#4140=EDGE_CURVE ( 'NONE', #1441, #16, #17883, .T. ) ;
#4141=DIRECTION ( 'NONE',  ( 0.000000000000000000, 0.000000000000000000, -1.000000000000000000 ) ) ;
#4144=DIRECTION ( 'NONE',  ( 0.000000000000000000, 0.7705132427757904745, -0.6374239897486881912 ) ) ;
#4153=CARTESIAN_POINT ( 'NONE',  ( 18.00000000000000355, 43.83938735307292944, -18.28286404005752175 ) ) ;
#4164=CARTESIAN_POINT ( 'NONE',  ( 18.00000000000000355, -36.05989434073635636, 30.12041790338605551 ) ) ;
#4165=EDGE_CURVE ( 'NONE', #19555, #15934, #30362, .T. ) ;
#4168=CYLINDRICAL_SURFACE ( 'NONE', #33577, 20.00000000000000355 ) ;
#4184=ADVANCED_FACE ( 'NONE', ( #26600 ), #597, .T. ) ;
#4188=DIRECTION ( 'NONE',  ( -1.000000000000000000, -0.000000000000000000, -0.000000000000000000 ) ) ;
#4194=LINE ( 'NONE', #7484, #39108 ) ;
#4196=ORIENTED_EDGE ( 'NONE', *, *, #39192, .F. ) ;
#4201=CARTESIAN_POINT ( 'NONE',  ( 18.00000000000000355, 47.32430374665931794, 21.55018039121543438 ) ) ;
#4203=AXIS2_PLACEMENT_3D ( 'NONE', #22737, #32303, #3245 ) ;
#4205=DIRECTION ( 'NONE',  ( -1.000000000000000000, -0.000000000000000000, 0.000000000000000000 ) ) ;
#4208=CYLINDRICAL_SURFACE ( 'NONE', #22731, 47.49900000000000233 ) ;
#4212=ORIENTED_EDGE ( 'NONE', *, *, #40417, .F. ) ;
#4213=CIRCLE ( 'NONE', #15848, 51.99999999999999289 ) ;
#4217=VERTEX_POINT ( 'NONE', #21916 ) ;
#4230=DIRECTION ( 'NONE',  ( -1.000000000000000000, 0.000000000000000000, 0.000000000000000000 ) ) ;
#4235=CARTESIAN_POINT ( 'NONE',  ( 18.00000000000001421, 0.000000000000000000, 7.500000000000000000 ) ) ;
#4243=DIRECTION ( 'NONE',  ( -1.000000000000000000, 0.000000000000000000, -0.000000000000000000 ) ) ;
#4245=EDGE_CURVE ( 'NONE', #25151, #20337, #33182, .T. ) ;
#4247=VERTEX_POINT ( 'NONE', #31696 ) ;
#4258=AXIS2_PLACEMENT_3D ( 'NONE', #19063, #2835, #29080 ) ;
#4260=DIRECTION ( 'NONE',  ( -1.000000000000000000, -0.000000000000000000, -0.000000000000000000 ) ) ;
#4261=VECTOR ( 'NONE', #19912, 1000.000000000000000 ) ;
#4266=LINE ( 'NONE', #17202, #10048 ) ;
#4276=ORIENTED_EDGE ( 'NONE', *, *, #29821, .F. ) ;
#4283=CARTESIAN_POINT ( 'NONE',  ( 18.00000000000000355, 0.000000000000000000, 0.000000000000000000 ) ) ;
#4284=EDGE_LOOP ( 'NONE', ( #39949, #32196, #8791, #40838 ) ) ;
#4295=DIRECTION ( 'NONE',  ( 0.000000000000000000, 0.5877852522924742473, -0.8090169943749466741 ) ) ;
#4307=EDGE_CURVE ( 'NONE', #22785, #42289, #8122, .T. ) ;
#4322=AXIS2_PLACEMENT_3D ( 'NONE', #42064, #12014, #12222 ) ;
#4330=FACE_OUTER_BOUND ( 'NONE', #41752, .T. ) ;
#4331=CARTESIAN_POINT ( 'NONE',  ( 0.000000000000000000, -7.162210897276078292, 51.50439529848826226 ) ) ;
#4338=CARTESIAN_POINT ( 'NONE',  ( 18.00000000000000355, 0.000000000000000000, 0.000000000000000000 ) ) ;
#4347=DIRECTION ( 'NONE',  ( -1.000000000000000000, -0.000000000000000000, 0.000000000000000000 ) ) ;
#4350=DIRECTION ( 'NONE',  ( 0.000000000000000000, 0.000000000000000000, -1.000000000000000000 ) ) ;
#4356=CARTESIAN_POINT ( 'NONE',  ( 9.000000000000001776, -51.19683565102437939, -9.104066087303991139 ) ) ;
#4357=EDGE_CURVE ( 'NONE', #28923, #17108, #2836, .T. ) ;
#4363=ORIENTED_EDGE ( 'NONE', *, *, #10593, .T. ) ;
#4370=CARTESIAN_POINT ( 'NONE',  ( 18.00000000000000355, -46.87740477351715640, 16.82754413119429771 ) ) ;
#4375=CIRCLE ( 'NONE', #9960, 47.49900000000000233 ) ;
#4383=MECHANICAL_DESIGN_GEOMETRIC_PRESENTATION_REPRESENTATION('',(#23250),#7887);
#4386=VERTEX_POINT ( 'NONE', #34212 ) ;
#4392=CARTESIAN_POINT ( 'NONE',  ( 18.00000000000000355, -27.43636312076348815, 38.14186064215142835 ) ) ;
#4395=CARTESIAN_POINT ( 'NONE',  ( 0.000000000000000000, 0.000000000000000000, 0.000000000000000000 ) ) ;
#4400=ORIENTED_EDGE ( 'NONE', *, *, #650, .T. ) ;
#4403=CARTESIAN_POINT ( 'NONE',  ( 0.000000000000000000, -11.46872990052349550, -45.56340405422456286 ) ) ;
#4405=ORIENTED_EDGE ( 'NONE', *, *, #14189, .F. ) ;
#4407=EDGE_CURVE ( 'NONE', #1396, #33317, #24863, .T. ) ;
#4414=CARTESIAN_POINT ( 'NONE',  ( 18.00000000000000355, 0.000000000000000000, 0.000000000000000000 ) ) ;
#4417=VERTEX_POINT ( 'NONE', #10659 ) ;
#4418=FACE_OUTER_BOUND ( 'NONE', #13049, .T. ) ;
#4420=ORIENTED_EDGE ( 'NONE', *, *, #14189, .T. ) ;
#4431=EDGE_CURVE ( 'NONE', #1632, #1619, #36019, .T. ) ;
#4446=DIRECTION ( 'NONE',  ( 0.000000000000000000, 0.000000000000000000, 1.000000000000000000 ) ) ;
#4458=CARTESIAN_POINT ( 'NONE',  ( 0.000000000000000000, 2.123073309835184386, 47.45152853935334747 ) ) ;
#4459=AXIS2_PLACEMENT_3D ( 'NONE', #16810, #30098, #9998 ) ;
#4476=ORIENTED_EDGE ( 'NONE', *, *, #31522, .F. ) ;
#4482=CARTESIAN_POINT ( 'NONE',  ( 0.000000000000000000, 36.06787431788731624, -37.45808914225450081 ) ) ;
#4483=CARTESIAN_POINT ( 'NONE',  ( 0.000000000000000000, 0.000000000000000000, 0.000000000000000000 ) ) ;
#4486=EDGE_CURVE ( 'NONE', #5452, #37135, #38546, .T. ) ;
#4497=CARTESIAN_POINT ( 'NONE',  ( -132.0000507999999968, 0.000000000000000000, 7.500000000000000000 ) ) ;
#4499=CARTESIAN_POINT ( 'NONE',  ( 0.000000000000000000, 36.34385289850590794, 29.77717097092089205 ) ) ;
#4517=DIRECTION ( 'NONE',  ( -1.000000000000000000, -0.000000000000000000, 0.000000000000000000 ) ) ;
#4520=DIRECTION ( 'NONE',  ( 0.000000000000000000, 0.000000000000000000, 1.000000000000000000 ) ) ;
#4522=EDGE_CURVE ( 'NONE', #19733, #30654, #9487, .T. ) ;
#4535=CIRCLE ( 'NONE', #8037, 51.99999999999999289 ) ;
#4550=ORIENTED_EDGE ( 'NONE', *, *, #26397, .F. ) ;
#4559=DIRECTION ( 'NONE',  ( 0.000000000000000000, 0.000000000000000000, -1.000000000000000000 ) ) ;
#4561=EDGE_LOOP ( 'NONE', ( #10273, #28524, #17345, #37937 ) ) ;
#4563=DIRECTION ( 'NONE',  ( -1.000000000000000000, 0.000000000000000000, 0.000000000000000000 ) ) ;
#4565=CIRCLE ( 'NONE', #28990, 47.49900000000000233 ) ;
#4571=CARTESIAN_POINT ( 'NONE',  ( 18.00000000000000355, 0.000000000000000000, 0.000000000000000000 ) ) ;
#4581=CARTESIAN_POINT ( 'NONE',  ( 9.000000000000001776, -12.30077720129131613, 50.52416135122077634 ) ) ;
#4582=AXIS2_PLACEMENT_3D ( 'NONE', #40626, #1150, #20199 ) ;
#4584=CARTESIAN_POINT ( 'NONE',  ( 18.00000000000000355, 29.60891106212788415, 37.14118181634774629 ) ) ;
#4588=AXIS2_PLACEMENT_3D ( 'NONE', #32830, #29804, #10127 ) ;
#4590=CYLINDRICAL_SURFACE ( 'NONE', #21882, 51.99999999999999289 ) ;
#4593=AXIS2_PLACEMENT_3D ( 'NONE', #38661, #21515, #8567 ) ;
#4595=DIRECTION ( 'NONE',  ( -1.000000000000000000, -0.000000000000000000, 0.000000000000000000 ) ) ;
#4600=VECTOR ( 'NONE', #30152, 1000.000000000000000 ) ;
#4620=ORIENTED_EDGE ( 'NONE', *, *, #15356, .T. ) ;
#4621=DIRECTION ( 'NONE',  ( -1.000000000000000000, 0.000000000000000000, 0.000000000000000000 ) ) ;
#4623=ORIENTED_EDGE ( 'NONE', *, *, #15965, .F. ) ;
#4630=VERTEX_POINT ( 'NONE', #5821 ) ;
#4631=DIRECTION ( 'NONE',  ( 0.000000000000000000, 0.000000000000000000, -1.000000000000000000 ) ) ;
#4641=EDGE_CURVE ( 'NONE', #6919, #6443, #6288, .T. ) ;
#4647=EDGE_LOOP ( 'NONE', ( #23298, #15444, #34694, #34797 ) ) ;
#4665=CARTESIAN_POINT ( 'NONE',  ( 0.000000000000000000, -47.32430374665916162, -21.55018039121577544 ) ) ;
#4669=AXIS2_PLACEMENT_3D ( 'NONE', #674, #19565, #20006 ) ;
#4674=LINE ( 'NONE', #14296, #37485 ) ;
#4684=DIRECTION ( 'NONE',  ( 0.000000000000000000, 0.000000000000000000, 1.000000000000000000 ) ) ;
#4690=CARTESIAN_POINT ( 'NONE',  ( 18.00000000000000355, 0.000000000000000000, 0.000000000000000000 ) ) ;
#4693=CARTESIAN_POINT ( 'NONE',  ( 0.000000000000000000, 44.47301969247445186, 16.68249143361925135 ) ) ;
#4710=LINE ( 'NONE', #14776, #40807 ) ;
#4717=VERTEX_POINT ( 'NONE', #2312 ) ;
#4735=DIRECTION ( 'NONE',  ( 0.000000000000000000, 0.9048270524660205760, -0.4257792915650702170 ) ) ;
#4736=ORIENTED_EDGE ( 'NONE', *, *, #3057, .T. ) ;
#4738=ORIENTED_EDGE ( 'NONE', *, *, #35387, .F. ) ;
#4749=ORIENTED_EDGE ( 'NONE', *, *, #10761, .F. ) ;
#4750=CYLINDRICAL_SURFACE ( 'NONE', #35144, 20.00000000000000355 ) ;
#4756=EDGE_CURVE ( 'NONE', #6092, #17062, #9782, .T. ) ;
#4765=AXIS2_PLACEMENT_3D ( 'NONE', #39578, #13222, #16723 ) ;
#4766=EDGE_CURVE ( 'NONE', #3059, #33656, #26551, .T. ) ;
#4767=ORIENTED_EDGE ( 'NONE', *, *, #37855, .T. ) ;
#4769=AXIS2_PLACEMENT_3D ( 'NONE', #29327, #9677, #9879 ) ;
#4773=ORIENTED_EDGE ( 'NONE', *, *, #13432, .F. ) ;
#4783=ORIENTED_EDGE ( 'NONE', *, *, #37907, .F. ) ;
#4788=CIRCLE ( 'NONE', #8962, 20.00000000000000000 ) ;
#4789=CARTESIAN_POINT ( 'NONE',  ( 9.000000000000001776, 43.55304910509446614, -28.41006711799937889 ) ) ;
#4796=CYLINDRICAL_SURFACE ( 'NONE', #18080, 20.00000000000000711 ) ;
#4804=ORIENTED_EDGE ( 'NONE', *, *, #28043, .T. ) ;
#4813=EDGE_CURVE ( 'NONE', #40202, #31882, #18217, .T. ) ;
#4815=CIRCLE ( 'NONE', #10390, 51.99999999999999289 ) ;
#4821=EDGE_CURVE ( 'NONE', #36379, #34535, #34164, .T. ) ;
#4823=LINE ( 'NONE', #24710, #28856 ) ;
#4825=VERTEX_POINT ( 'NONE', #554 ) ;
#4829=DIRECTION ( 'NONE',  ( -1.000000000000000000, 0.000000000000000000, -0.000000000000000000 ) ) ;
#4834=CARTESIAN_POINT ( 'NONE',  ( 18.00000000000000355, 7.162210897276454880, -51.50439529848820541 ) ) ;
#4838=ORIENTED_EDGE ( 'NONE', *, *, #12506, .F. ) ;
#4841=CYLINDRICAL_SURFACE ( 'NONE', #30622, 51.99999999999999289 ) ;
#4843=VERTEX_POINT ( 'NONE', #17411 ) ;
#4850=VERTEX_POINT ( 'NONE', #10397 ) ;
#4859=VERTEX_POINT ( 'NONE', #10831 ) ;
#4872=VECTOR ( 'NONE', #25843, 1000.000000000000000 ) ;
#4873=ORIENTED_EDGE ( 'NONE', *, *, #35271, .F. ) ;
#4875=AXIS2_PLACEMENT_3D ( 'NONE', #30496, #3617, #16987 ) ;
#4876=EDGE_CURVE ( 'NONE', #14923, #31429, #40441, .T. ) ;
#4878=CIRCLE ( 'NONE', #41104, 47.49900000000000233 ) ;
#4884=DIRECTION ( 'NONE',  ( -1.000000000000000000, 0.000000000000000000, 0.000000000000000000 ) ) ;
#4885=DIRECTION ( 'NONE',  ( -1.000000000000000000, 0.000000000000000000, 0.000000000000000000 ) ) ;
#4915=CARTESIAN_POINT ( 'NONE',  ( 9.000000000000001776, 30.03615769709733740, 42.44795908868999135 ) ) ;
#4917=CARTESIAN_POINT ( 'NONE',  ( 18.00000000000000355, 29.60891106212838508, -37.14118181634735549 ) ) ;
#4918=FACE_OUTER_BOUND ( 'NONE', #19978, .T. ) ;
#4928=DIRECTION ( 'NONE',  ( -1.000000000000000000, 0.000000000000000000, -0.000000000000000000 ) ) ;
#4933=CIRCLE ( 'NONE', #29332, 20.00000000000000711 ) ;
#4936=DIRECTION ( 'NONE',  ( -1.000000000000000000, 0.000000000000000000, -0.000000000000000000 ) ) ;
#4937=CIRCLE ( 'NONE', #13928, 20.00000000000000355 ) ;
#4945=ORIENTED_EDGE ( 'NONE', *, *, #15192, .T. ) ;
#4946=CYLINDRICAL_SURFACE ( 'NONE', #17928, 20.00000000000000355 ) ;
#4950=CARTESIAN_POINT ( 'NONE',  ( 18.00000000000000355, 37.91532898920922889, 28.61088654061651937 ) ) ;
#4953=VERTEX_POINT ( 'NONE', #34812 ) ;
#4964=ORIENTED_EDGE ( 'NONE', *, *, #31671, .T. ) ;
#4965=DIRECTION ( 'NONE',  ( -1.000000000000000000, 0.000000000000000000, 0.000000000000000000 ) ) ;
#4979=AXIS2_PLACEMENT_3D ( 'NONE', #19226, #29450, #19020 ) ;
#4987=AXIS2_PLACEMENT_3D ( 'NONE', #29919, #25991, #19250 ) ;
#4990=ORIENTED_EDGE ( 'NONE', *, *, #26453, .T. ) ;
#4993=ORIENTED_EDGE ( 'NONE', *, *, #7710, .T. ) ;
#5004=CARTESIAN_POINT ( 'NONE',  ( 0.000000000000000000, -18.53613841426756892, -48.58406706613922665 ) ) ;
#5005=DIRECTION ( 'NONE',  ( -1.000000000000000000, 0.000000000000000000, 0.000000000000000000 ) ) ;
#5008=CARTESIAN_POINT ( 'NONE',  ( 18.00000000000000355, 0.000000000000000000, 0.000000000000000000 ) ) ;
#5014=ORIENTED_EDGE ( 'NONE', *, *, #27318, .F. ) ;
#5021=ORIENTED_EDGE ( 'NONE', *, *, #24000, .T. ) ;
#5022=DIRECTION ( 'NONE',  ( -1.000000000000000000, 0.000000000000000000, 0.000000000000000000 ) ) ;
#5025=AXIS2_PLACEMENT_3D ( 'NONE', #21038, #34078, #17539 ) ;
#5029=CARTESIAN_POINT ( 'NONE',  ( 18.00000000000000355, -44.47301969247456555, 16.68249143361894582 ) ) ;
#5031=CARTESIAN_POINT ( 'NONE',  ( 18.00000000000000355, 0.000000000000000000, 0.000000000000000000 ) ) ;
#5054=CYLINDRICAL_SURFACE ( 'NONE', #32573, 20.00000000000000711 ) ;
#5061=CIRCLE ( 'NONE', #36378, 52.00000000000000000 ) ;
#5068=DIRECTION ( 'NONE',  ( 0.000000000000000000, -6.982962677686265922E-15, 1.000000000000000000 ) ) ;
#5069=ORIENTED_EDGE ( 'NONE', *, *, #14033, .T. ) ;
#5071=ORIENTED_EDGE ( 'NONE', *, *, #35615, .F. ) ;
#5087=COLOUR_RGB ( '', 0.72549020, 0.75294118, 0.79215686) ;
#5089=VECTOR ( 'NONE', #19656, 1000.000000000000000 ) ;
#5092=CARTESIAN_POINT ( 'NONE',  ( -10.00000000000000000, 0.000000000000000000, 0.000000000000000000 ) ) ;
#5097=ORIENTED_EDGE ( 'NONE', *, *, #38098, .T. ) ;
#5105=DIRECTION ( 'NONE',  ( 1.000000000000000000, 0.000000000000000000, 0.000000000000000000 ) ) ;
#5108=CARTESIAN_POINT ( 'NONE',  ( 9.000000000000001776, -51.19683565102450018, 9.104066087303291255 ) ) ;
#5110=EDGE_CURVE ( 'NONE', #15819, #18858, #41155, .T. ) ;
#5112=ORIENTED_EDGE ( 'NONE', *, *, #26850, .T. ) ;
#5121=ORIENTED_EDGE ( 'NONE', *, *, #30559, .F. ) ;
#5122=DIRECTION ( 'NONE',  ( -1.000000000000000000, 0.000000000000000000, 0.000000000000000000 ) ) ;
#5126=CARTESIAN_POINT ( 'NONE',  ( 18.00000000000001421, 9.184850993605147944E-16, -7.500000000000000000 ) ) ;
#5139=CIRCLE ( 'NONE', #18457, 52.00000000000000000 ) ;
#5151=AXIS2_PLACEMENT_3D ( 'NONE', #34819, #7555, #31552 ) ;
#5161=EDGE_CURVE ( 'NONE', #13064, #38711, #19626, .T. ) ;
#5162=CARTESIAN_POINT ( 'NONE',  ( 18.00000000000000355, -42.60732521687558005, -19.80331771201703006 ) ) ;
#5163=CIRCLE ( 'NONE', #37202, 20.00000000000000711 ) ;
#5172=DIRECTION ( 'NONE',  ( 0.000000000000000000, 0.000000000000000000, 1.000000000000000000 ) ) ;
#5182=AXIS2_PLACEMENT_3D ( 'NONE', #20362, #33623, #40156 ) ;
#5183=ORIENTED_EDGE ( 'NONE', *, *, #34113, .T. ) ;
#5196=CIRCLE ( 'NONE', #38634, 52.00000000000000000 ) ;
#5203=ORIENTED_EDGE ( 'NONE', *, *, #1131, .T. ) ;
#5206=FACE_OUTER_BOUND ( 'NONE', #26391, .T. ) ;
#5211=CIRCLE ( 'NONE', #8699, 20.00000000000000355 ) ;
#5212=EDGE_CURVE ( 'NONE', #33622, #16464, #8837, .T. ) ;
#5215=DIRECTION ( 'NONE',  ( 0.000000000000000000, 0.000000000000000000, 1.000000000000000000 ) ) ;
#5228=AXIS2_PLACEMENT_3D ( 'NONE', #11343, #14846, #18146 ) ;
#5229=DIRECTION ( 'NONE',  ( 1.000000000000000000, 0.000000000000000000, 0.000000000000000000 ) ) ;
#5232=VECTOR ( 'NONE', #17854, 1000.000000000000000 ) ;
#5234=CARTESIAN_POINT ( 'NONE',  ( 18.00000000000000355, 0.000000000000000000, 0.000000000000000000 ) ) ;
#5240=ORIENTED_EDGE ( 'NONE', *, *, #22433, .T. ) ;
#5246=DIRECTION ( 'NONE',  ( 0.000000000000000000, 0.000000000000000000, 1.000000000000000000 ) ) ;
#5250=DIRECTION ( 'NONE',  ( -1.000000000000000000, 0.000000000000000000, 0.000000000000000000 ) ) ;
#5251=APPLICATION_CONTEXT ( 'automotive_design' ) ;
#5254=AXIS2_PLACEMENT_3D ( 'NONE', #21445, #37534, #4141 ) ;
#5260=CARTESIAN_POINT ( 'NONE',  ( 18.00000000000000355, -39.55064067543082018, 25.36340625197346199 ) ) ;
#5263=CARTESIAN_POINT ( 'NONE',  ( 18.00000000000000355, 51.85248208264516734, 3.914090171286377817 ) ) ;
#5266=ORIENTED_EDGE ( 'NONE', *, *, #2308, .T. ) ;
#5270=CARTESIAN_POINT ( 'NONE',  ( 9.000000000000001776, 46.77034588191335018, -22.72740077717179830 ) ) ;
#5277=ORIENTED_EDGE ( 'NONE', *, *, #27912, .T. ) ;
#5278=VERTEX_POINT ( 'NONE', #19984 ) ;
#5279=FACE_OUTER_BOUND ( 'NONE', #34037, .T. ) ;
#5287=AXIS2_PLACEMENT_3D ( 'NONE', #21788, #27657, #41794 ) ;
#5293=EDGE_CURVE ( 'NONE', #192, #24364, #26931, .T. ) ;
#5296=EDGE_CURVE ( 'NONE', #24285, #16293, #39750, .T. ) ;
#5298=CIRCLE ( 'NONE', #10888, 47.49900000000000233 ) ;
#5307=DIRECTION ( 'NONE',  ( -1.000000000000000000, 0.000000000000000000, -0.000000000000000000 ) ) ;
#5312=ORIENTED_EDGE ( 'NONE', *, *, #1747, .T. ) ;
#5324=DIRECTION ( 'NONE',  ( 0.000000000000000000, 0.000000000000000000, -1.000000000000000000 ) ) ;
#5329=AXIS2_PLACEMENT_3D ( 'NONE', #8779, #6355, #22138 ) ;
#5330=EDGE_CURVE ( 'NONE', #32585, #37461, #29999, .T. ) ;
#5331=CIRCLE ( 'NONE', #17200, 52.00000000000000000 ) ;
#5333=CARTESIAN_POINT ( 'NONE',  ( 18.00000000000000355, -46.90537658765333617, 2.727856614654147638 ) ) ;
#5338=ORIENTED_EDGE ( 'NONE', *, *, #10542, .T. ) ;
#5340=ORIENTED_EDGE ( 'NONE', *, *, #13057, .F. ) ;
#5365=LINE ( 'NONE', #37861, #5232 ) ;
#5377=DIRECTION ( 'NONE',  ( -1.000000000000000000, 0.000000000000000000, -0.000000000000000000 ) ) ;
#5390=DIRECTION ( 'NONE',  ( -1.000000000000000000, 0.000000000000000000, -0.000000000000000000 ) ) ;
#5393=CARTESIAN_POINT ( 'NONE',  ( 0.000000000000000000, -43.55304910509386218, -28.41006711800032392 ) ) ;
#5396=LINE ( 'NONE', #35484, #24470 ) ;
#5399=DIRECTION ( 'NONE',  ( -1.000000000000000000, 0.000000000000000000, -0.000000000000000000 ) ) ;
#5409=EDGE_LOOP ( 'NONE', ( #26215, #4736, #32992, #16953 ) ) ;
#5430=AXIS2_PLACEMENT_3D ( 'NONE', #22888, #2736, #42666 ) ;
#5432=DIRECTION ( 'NONE',  ( 0.000000000000000000, 0.000000000000000000, 1.000000000000000000 ) ) ;
#5435=CARTESIAN_POINT ( 'NONE',  ( 18.00000000000000355, 6.109652351742432153, -46.58570277113501845 ) ) ;
#5439=DIRECTION ( 'NONE',  ( -1.000000000000000000, 0.000000000000000000, 0.000000000000000000 ) ) ;
#5452=VERTEX_POINT ( 'NONE', #1802 ) ;
#5457=FACE_OUTER_BOUND ( 'NONE', #19641, .T. ) ;
#5460=DIRECTION ( 'NONE',  ( -1.000000000000000000, -0.000000000000000000, 0.000000000000000000 ) ) ;
#5469=FACE_OUTER_BOUND ( 'NONE', #18237, .T. ) ;
#5479=VECTOR ( 'NONE', #42976, 1000.000000000000000 ) ;
#5484=VERTEX_POINT ( 'NONE', #37591 ) ;
#5490=VERTEX_POINT ( 'NONE', #21283 ) ;
#5497=EDGE_LOOP ( 'NONE', ( #16247, #39511, #36391, #34067 ) ) ;
#5510=DIRECTION ( 'NONE',  ( 0.000000000000000000, -0.2486898871648622333, 0.9685831611286292997 ) ) ;
#5520=CYLINDRICAL_SURFACE ( 'NONE', #7318, 47.49900000000000233 ) ;
#5522=ADVANCED_FACE ( 'NONE', ( #34319 ), #30847, .T. ) ;
#5528=ORIENTED_EDGE ( 'NONE', *, *, #5609, .F. ) ;
#5529=LINE ( 'NONE', #8164, #19998 ) ;
#5535=VECTOR ( 'NONE', #11351, 1000.000000000000000 ) ;
#5537=VERTEX_POINT ( 'NONE', #11007 ) ;
#5544=DIRECTION ( 'NONE',  ( -1.000000000000000000, -0.000000000000000000, -0.000000000000000000 ) ) ;
#5546=ADVANCED_FACE ( 'NONE', ( #32333 ), #41729, .T. ) ;
#5547=DIRECTION ( 'NONE',  ( -1.000000000000000000, 0.000000000000000000, -0.000000000000000000 ) ) ;
#5551=EDGE_CURVE ( 'NONE', #13205, #16464, #22221, .T. ) ;
#5552=ORIENTED_EDGE ( 'NONE', *, *, #14770, .F. ) ;
#5554=EDGE_LOOP ( 'NONE', ( #21862, #20945, #24916, #2774 ) ) ;
#5563=DIRECTION ( 'NONE',  ( -1.000000000000000000, 0.000000000000000000, 0.000000000000000000 ) ) ;
#5568=ORIENTED_EDGE ( 'NONE', *, *, #29222, .T. ) ;
#5573=CARTESIAN_POINT ( 'NONE',  ( 18.00000000000000355, 42.41764978026606769, 20.20639853260304619 ) ) ;
#5578=DIRECTION ( 'NONE',  ( 0.000000000000000000, 0.000000000000000000, 1.000000000000000000 ) ) ;
#5590=ADVANCED_FACE ( 'NONE', ( #22555 ), #5923, .T. ) ;
#5593=VERTEX_POINT ( 'NONE', #42567 ) ;
#5603=ORIENTED_EDGE ( 'NONE', *, *, #12813, .F. ) ;
#5604=ORIENTED_EDGE ( 'NONE', *, *, #21562, .F. ) ;
#5605=CARTESIAN_POINT ( 'NONE',  ( 18.00000000000000355, 22.82995208772746665, -41.06517797613638976 ) ) ;
#5609=EDGE_CURVE ( 'NONE', #28896, #40202, #32633, .T. ) ;
#5617=DIRECTION ( 'NONE',  ( 0.000000000000000000, 0.9510565162951523099, 0.3090169943749515591 ) ) ;
#5619=VECTOR ( 'NONE', #18121, 1000.000000000000000 ) ;
#5632=FACE_OUTER_BOUND ( 'NONE', #15385, .T. ) ;
#5633=AXIS2_PLACEMENT_3D ( 'NONE', #14177, #10899, #17259 ) ;
#5634=FACE_OUTER_BOUND ( 'NONE', #19999, .T. ) ;
#5640=VECTOR ( 'NONE', #3983, 1000.000000000000000 ) ;
#5651=ORIENTED_EDGE ( 'NONE', *, *, #25524, .T. ) ;
#5656=DIRECTION ( 'NONE',  ( -1.000000000000000000, -0.000000000000000000, 0.000000000000000000 ) ) ;
#5659=DIRECTION ( 'NONE',  ( 0.000000000000000000, 0.000000000000000000, -1.000000000000000000 ) ) ;
#5664=AXIS2_PLACEMENT_3D ( 'NONE', #33162, #19466, #29473 ) ;
#5668=DIRECTION ( 'NONE',  ( -1.000000000000000000, 0.000000000000000000, 0.000000000000000000 ) ) ;
#5670=DIRECTION ( 'NONE',  ( -1.000000000000000000, -0.000000000000000000, -0.000000000000000000 ) ) ;
#5672=CIRCLE ( 'NONE', #11269, 20.00000000000000711 ) ;
#5681=AXIS2_PLACEMENT_3D ( 'NONE', #9692, #35645, #19980 ) ;
#5686=EDGE_CURVE ( 'NONE', #16407, #1606, #2213, .T. ) ;
#5707=DIRECTION ( 'NONE',  ( 0.000000000000000000, 0.000000000000000000, 1.000000000000000000 ) ) ;
#5708=EDGE_LOOP ( 'NONE', ( #40977, #28777, #13448, #25033 ) ) ;
#5709=DIRECTION ( 'NONE',  ( -1.000000000000000000, 0.000000000000000000, -0.000000000000000000 ) ) ;
#5716=CARTESIAN_POINT ( 'NONE',  ( 18.00000000000000355, 39.78933988720115877, 24.98727647985016276 ) ) ;
#5723=DIRECTION ( 'NONE',  ( -1.000000000000000000, -0.000000000000000000, 0.000000000000000000 ) ) ;
#5732=CARTESIAN_POINT ( 'NONE',  ( 0.000000000000000000, -46.21320724403656044, 10.97699764141937173 ) ) ;
#5738=ORIENTED_EDGE ( 'NONE', *, *, #6612, .T. ) ;
#5742=AXIS2_PLACEMENT_3D ( 'NONE', #29942, #7952, #41446 ) ;
#5744=DIRECTION ( 'NONE',  ( -1.000000000000000000, 0.000000000000000000, 0.000000000000000000 ) ) ;
#5745=DIRECTION ( 'NONE',  ( 0.000000000000000000, 0.000000000000000000, 1.000000000000000000 ) ) ;
#5759=ORIENTED_EDGE ( 'NONE', *, *, #34742, .F. ) ;
#5771=LINE ( 'NONE', #32395, #14998 ) ;
#5775=FACE_OUTER_BOUND ( 'NONE', #39175, .T. ) ;
#5779=EDGE_CURVE ( 'NONE', #19793, #12073, #34688, .T. ) ;
#5788=CIRCLE ( 'NONE', #38514, 47.49900000000000233 ) ;
#5795=ORIENTED_EDGE ( 'NONE', *, *, #41227, .T. ) ;
#5808=CARTESIAN_POINT ( 'NONE',  ( 0.000000000000000000, 3.840921266750508156, -47.34345070675165346 ) ) ;
#5821=CARTESIAN_POINT ( 'NONE',  ( 18.00000000000000355, 19.74581912682909035, -48.10512059033371912 ) ) ;
#5827=ORIENTED_EDGE ( 'NONE', *, *, #37104, .F. ) ;
#5842=CARTESIAN_POINT ( 'NONE',  ( 18.00000000000000355, -7.162210897275384625, -51.50439529848835463 ) ) ;
#5845=DIRECTION ( 'NONE',  ( -1.000000000000000000, -0.000000000000000000, -0.000000000000000000 ) ) ;
#5861=EDGE_LOOP ( 'NONE', ( #9888, #29025, #5866, #17663, #33632, #2883, #15285, #14965, #11068, #21017, #14636, #31968, #34644, #26739, #24899, #20985, #10597, #17857, #12493, #24025, #3609, #7439, #2340, #7771, #19177, #4080, #38224, #11326, #38416, #11989, #7759, #23096, #6700, #31297, #18169, #9717, #35060, #35677, #13259, #17066, #19691, #15400, #1205, #34130, #13559, #40054, #32215, #29386, #1229, #24819, #16915, #3994, #31718, #30401, #10083, #15416, #4065, #914, #253, #38547, #14045, #18268, #1427, #28216, #20852, #16271, #7023, #24622, #28517, #20040, #34349, #6873, #36105, #9858, #3185, #15139, #16037, #43034, #25562, #16451, #7965, #22937, #34559, #9541, #19857, #40289, #15627, #37043, #10149, #5312, #11200, #21590, #43065, #28689, #43057, #5568, #23807, #4945, #34197, #40586, #37127, #3422, #34903, #33186, #25376, #42543, #9019, #27737, #27831, #18622, #28439, #24769, #21284, #30834, #5240, #8304, #10126, #24330, #32650, #19305, #42640, #6829, #37418, #19967, #1447, #3028, #30340, #1032, #11173, #40868, #41042, #13420, #9007, #26243, #24030, #2002, #25760, #42934, #2985, #12265, #11198, #10547, #35662, #34148, #18861, #28666, #10455, #4767, #13193, #35326, #23652, #33879, #21370, #30776, #6534, #33022, #23703, #39876, #29740, #32803, #6329, #570, #34137, #36331, #3380, #18085, #29850, #43172, #10868, #32569, #16001, #28365, #25185, #30517, #8035, #32953, #15029, #7654, #17452, #19427, #26326, #22462, #8263, #4993, #24665, #9818, #17540, #28147, #10905, #21431, #32535, #5021, #27390, #37829, #5266, #41011, #27510, #11779, #24803, #5112, #697, #26447, #4050 ) ) ;
#5864=DIRECTION ( 'NONE',  ( -1.000000000000000000, 0.000000000000000000, -0.000000000000000000 ) ) ;
#5866=ORIENTED_EDGE ( 'NONE', *, *, #11477, .T. ) ;
#5871=CIRCLE ( 'NONE', #39264, 20.00000000000000000 ) ;
#5874=FACE_OUTER_BOUND ( 'NONE', #9990, .T. ) ;
#5875=AXIS2_PLACEMENT_3D ( 'NONE', #36353, #16551, #12416 ) ;
#5892=CARTESIAN_POINT ( 'NONE',  ( 9.000000000000001776, -40.47821179127736713, 32.64221760512746329 ) ) ;
#5900=DIRECTION ( 'NONE',  ( -1.000000000000000000, -0.000000000000000000, 0.000000000000000000 ) ) ;
#5903=ORIENTED_EDGE ( 'NONE', *, *, #8793, .F. ) ;
#5907=CIRCLE ( 'NONE', #9396, 47.49900000000000233 ) ;
#5913=DIRECTION ( 'NONE',  ( 0.000000000000000000, 0.000000000000000000, 1.000000000000000000 ) ) ;
#5914=DIRECTION ( 'NONE',  ( 0.000000000000000000, 0.2486898871648553500, -0.9685831611286310761 ) ) ;
#5923=CYLINDRICAL_SURFACE ( 'NONE', #16631, 20.00000000000000355 ) ;
#5925=EDGE_CURVE ( 'NONE', #31919, #28896, #8412, .T. ) ;
#5932=AXIS2_PLACEMENT_3D ( 'NONE', #41991, #16061, #23052 ) ;
#5936=AXIS2_PLACEMENT_3D ( 'NONE', #14531, #18049, #20885 ) ;
#5940=EDGE_CURVE ( 'NONE', #6854, #40629, #6995, .T. ) ;
#5944=CARTESIAN_POINT ( 'NONE',  ( 0.000000000000000000, 50.95304419620838843, -10.38206564895608786 ) ) ;
#5946=ORIENTED_EDGE ( 'NONE', *, *, #30217, .T. ) ;
#5947=DIRECTION ( 'NONE',  ( 1.000000000000000000, -0.000000000000000000, -0.000000000000000000 ) ) ;
#5951=AXIS2_PLACEMENT_3D ( 'NONE', #40207, #708, #7261 ) ;
#5957=ORIENTED_EDGE ( 'NONE', *, *, #40387, .F. ) ;
#5958=CIRCLE ( 'NONE', #35910, 7.500000000000000000 ) ;
#5959=CYLINDRICAL_SURFACE ( 'NONE', #35776, 20.00000000000000711 ) ;
#5960=AXIS2_PLACEMENT_3D ( 'NONE', #881, #21237, #34072 ) ;
#5965=ORIENTED_EDGE ( 'NONE', *, *, #12721, .F. ) ;
#5976=ORIENTED_EDGE ( 'NONE', *, *, #2308, .F. ) ;
#5979=CARTESIAN_POINT ( 'NONE',  ( 0.000000000000000000, 8.053585752061904302, 46.81126742072025593 ) ) ;
#5985=( NAMED_UNIT ( * ) PLANE_ANGLE_UNIT ( ) SI_UNIT ( $, .RADIAN. ) );
#5995=CIRCLE ( 'NONE', #38045, 20.00000000000000711 ) ;
#6008=EDGE_CURVE ( 'NONE', #31470, #13399, #16796, .T. ) ;
#6011=ORIENTED_EDGE ( 'NONE', *, *, #39788, .F. ) ;
#6019=CARTESIAN_POINT ( 'NONE',  ( 18.00000000000000355, -11.90021268425522827, -45.45261810511227907 ) ) ;
#6026=EDGE_CURVE ( 'NONE', #27822, #13721, #31408, .T. ) ;
#6032=ORIENTED_EDGE ( 'NONE', *, *, #35082, .T. ) ;
#6060=CARTESIAN_POINT ( 'NONE',  ( 0.000000000000000000, -5.667686777401384823, -46.64153600743609474 ) ) ;
#6064=VECTOR ( 'NONE', #42646, 1000.000000000000000 ) ;
#6072=CIRCLE ( 'NONE', #41606, 47.49899999999998812 ) ;
#6075=AXIS2_PLACEMENT_3D ( 'NONE', #1148, #31284, #28458 ) ;
#6079=DIRECTION ( 'NONE',  ( 0.000000000000000000, -0.7705132427757817037, -0.6374239897486988493 ) ) ;
#6090=CARTESIAN_POINT ( 'NONE',  ( 9.000000000000001776, 25.61928775981106554, -45.25098998563450436 ) ) ;
#6092=VERTEX_POINT ( 'NONE', #38831 ) ;
#6093=VECTOR ( 'NONE', #17330, 1000.000000000000000 ) ;
#6096=ORIENTED_EDGE ( 'NONE', *, *, #15351, .F. ) ;
#6110=FACE_OUTER_BOUND ( 'NONE', #5409, .T. ) ;
#6121=DIRECTION ( 'NONE',  ( -1.000000000000000000, 0.000000000000000000, -0.000000000000000000 ) ) ;
#6123=ORIENTED_EDGE ( 'NONE', *, *, #25337, .T. ) ;
#6124=DIRECTION ( 'NONE',  ( -1.000000000000000000, 0.000000000000000000, -0.000000000000000000 ) ) ;
#6126=DIRECTION ( 'NONE',  ( 1.000000000000000000, 0.000000000000000000, 0.000000000000000000 ) ) ;
#6129=LINE ( 'NONE', #9394, #5479 ) ;
#6131=ADVANCED_FACE ( 'NONE', ( #25776 ), #9157, .T. ) ;
#6136=DIRECTION ( 'NONE',  ( 0.000000000000000000, -0.4817536741017222623, 0.8763066800438598092 ) ) ;
#6139=CARTESIAN_POINT ( 'NONE',  ( 18.00000000000000355, 24.72041153920788403, -40.55929306992662475 ) ) ;
#6143=DIRECTION ( 'NONE',  ( -1.000000000000000000, 0.000000000000000000, 0.000000000000000000 ) ) ;
#6150=AXIS2_PLACEMENT_3D ( 'NONE', #32255, #28791, #2132 ) ;
#6153=AXIS2_PLACEMENT_3D ( 'NONE', #2875, #6390, #29538 ) ;
#6155=DIRECTION ( 'NONE',  ( -1.000000000000000000, 0.000000000000000000, 0.000000000000000000 ) ) ;
#6156=DIRECTION ( 'NONE',  ( 0.000000000000000000, -0.7705132427757817037, -0.6374239897486988493 ) ) ;
#6174=CIRCLE ( 'NONE', #1972, 52.00000000000000000 ) ;
#6176=DIRECTION ( 'NONE',  ( -1.000000000000000000, -0.000000000000000000, 0.000000000000000000 ) ) ;
#6212=ADVANCED_FACE ( 'NONE', ( #23359 ), #9365, .T. ) ;
#6214=EDGE_CURVE ( 'NONE', #23500, #10758, #33473, .T. ) ;
#6224=CARTESIAN_POINT ( 'NONE',  ( 18.00000000000000355, 32.00046193115198179, -34.40241257139653186 ) ) ;
#6232=DIRECTION ( 'NONE',  ( 0.000000000000000000, 0.9822872507286879440, 0.1873813145857285145 ) ) ;
#6234=CIRCLE ( 'NONE', #13960, 51.99999999999999289 ) ;
#6243=EDGE_LOOP ( 'NONE', ( #28817, #31999, #34736, #38345 ) ) ;
#6248=DIRECTION ( 'NONE',  ( 0.000000000000000000, 0.9980267284282717810, -0.06279051952930990443 ) ) ;
#6251=CARTESIAN_POINT ( 'NONE',  ( 0.000000000000000000, -50.95304419620830316, 10.38206564895644313 ) ) ;
#6263=AXIS2_PLACEMENT_3D ( 'NONE', #29281, #2196, #2399 ) ;
#6273=CARTESIAN_POINT ( 'NONE',  ( 9.000000000000001776, 19.74581912682909390, -48.10512059033372623 ) ) ;
#6274=CARTESIAN_POINT ( 'NONE',  ( 18.00000000000000355, 0.000000000000000000, 0.000000000000000000 ) ) ;
#6279=DIRECTION ( 'NONE',  ( 0.000000000000000000, 0.5877852522924742473, -0.8090169943749465631 ) ) ;
#6282=DIRECTION ( 'NONE',  ( 0.000000000000000000, -0.9980267284282708928, -0.06279051952932446223 ) ) ;
#6288=CIRCLE ( 'NONE', #35558, 20.00000000000000355 ) ;
#6296=ADVANCED_FACE ( 'NONE', ( #34429 ), #3874, .T. ) ;
#6298=CIRCLE ( 'NONE', #42510, 47.49900000000000233 ) ;
#6300=ORIENTED_EDGE ( 'NONE', *, *, #15296, .F. ) ;
#6302=UNCERTAINTY_MEASURE_WITH_UNIT (LENGTH_MEASURE( 1.000000000000000082E-05 ), #25879, 'distance_accuracy_value', 'NONE');
#6304=DIRECTION ( 'NONE',  ( 0.000000000000000000, 0.000000000000000000, 1.000000000000000000 ) ) ;
#6307=CARTESIAN_POINT ( 'NONE',  ( 9.000000000000001776, -50.95304419620832448, 10.38206564895643957 ) ) ;
#6309=SHAPE_DEFINITION_REPRESENTATION ( #2543, #13509 ) ;
#6321=AXIS2_PLACEMENT_3D ( 'NONE', #13035, #9734, #42235 ) ;
#6322=AXIS2_PLACEMENT_3D ( 'NONE', #12977, #33242, #14058 ) ;
#6327=DIRECTION ( 'NONE',  ( 0.000000000000000000, -0.1253332335642905193, -0.9921147013144796523 ) ) ;
#6329=ORIENTED_EDGE ( 'NONE', *, *, #30217, .F. ) ;
#6333=AXIS2_PLACEMENT_3D ( 'NONE', #8722, #9589, #22077 ) ;
#6335=DIRECTION ( 'NONE',  ( -1.000000000000000000, 0.000000000000000000, 0.000000000000000000 ) ) ;
#6338=FACE_OUTER_BOUND ( 'NONE', #7420, .T. ) ;
#6350=ORIENTED_EDGE ( 'NONE', *, *, #8955, .F. ) ;
#6353=DIRECTION ( 'NONE',  ( -1.000000000000000000, 0.000000000000000000, 0.000000000000000000 ) ) ;
#6355=DIRECTION ( 'NONE',  ( -1.000000000000000000, 0.000000000000000000, 0.000000000000000000 ) ) ;
#6361=ORIENTED_EDGE ( 'NONE', *, *, #26526, .F. ) ;
#6374=LINE ( 'NONE', #23217, #42109 ) ;
#6377=ORIENTED_EDGE ( 'NONE', *, *, #16253, .F. ) ;
#6385=VERTEX_POINT ( 'NONE', #7820 ) ;
#6389=ORIENTED_EDGE ( 'NONE', *, *, #22877, .F. ) ;
#6390=DIRECTION ( 'NONE',  ( -1.000000000000000000, -0.000000000000000000, -0.000000000000000000 ) ) ;
#6396=ORIENTED_EDGE ( 'NONE', *, *, #41089, .F. ) ;
#6398=ORIENTED_EDGE ( 'NONE', *, *, #19618, .F. ) ;
#6406=DIRECTION ( 'NONE',  ( 1.000000000000000000, 0.000000000000000000, 0.000000000000000000 ) ) ;
#6408=VERTEX_POINT ( 'NONE', #30749 ) ;
#6416=CARTESIAN_POINT ( 'NONE',  ( 0.000000000000000000, -22.43957647427189528, 41.27978878573620847 ) ) ;
#6423=CARTESIAN_POINT ( 'NONE',  ( 0.000000000000000000, 20.99948489194422763, 42.60488980472788256 ) ) ;
#6424=CARTESIAN_POINT ( 'NONE',  ( 0.000000000000000000, -32.00046193115174731, 34.40241257139675923 ) ) ;
#6429=DIRECTION ( 'NONE',  ( 0.000000000000000000, 0.8443279255020161855, -0.5358267949789946583 ) ) ;
#6434=EDGE_CURVE ( 'NONE', #33305, #19546, #15121, .T. ) ;
#6443=VERTEX_POINT ( 'NONE', #15626 ) ;
#6447=VERTEX_POINT ( 'NONE', #15845 ) ;
#6448=ORIENTED_EDGE ( 'NONE', *, *, #24907, .T. ) ;
#6450=EDGE_CURVE ( 'NONE', #11670, #7587, #28131, .T. ) ;
#6452=AXIS2_PLACEMENT_3D ( 'NONE', #4097, #9799, #10456 ) ;
#6460=DIRECTION ( 'NONE',  ( -1.000000000000000000, 0.000000000000000000, -0.000000000000000000 ) ) ;
#6461=FACE_OUTER_BOUND ( 'NONE', #24266, .T. ) ;
#6464=ORIENTED_EDGE ( 'NONE', *, *, #19880, .F. ) ;
#6481=CARTESIAN_POINT ( 'NONE',  ( 18.00000000000000355, -34.03046037009231384, -33.13733193845841640 ) ) ;
#6488=CARTESIAN_POINT ( 'NONE',  ( 18.00000000000000355, 22.82995208772746665, -41.06517797613638976 ) ) ;
#6502=CARTESIAN_POINT ( 'NONE',  ( 18.00000000000000355, 20.99948489194481738, -42.60488980472760545 ) ) ;
#6510=DIRECTION ( 'NONE',  ( -1.000000000000000000, 0.000000000000000000, -0.000000000000000000 ) ) ;
#6532=AXIS2_PLACEMENT_3D ( 'NONE', #7801, #11101, #4295 ) ;
#6534=ORIENTED_EDGE ( 'NONE', *, *, #11617, .T. ) ;
#6538=CYLINDRICAL_SURFACE ( 'NONE', #19404, 51.99999999999999289 ) ;
#6544=DIRECTION ( 'NONE',  ( -1.000000000000000000, -0.000000000000000000, -0.000000000000000000 ) ) ;
#6560=DIRECTION ( 'NONE',  ( -1.000000000000000000, 0.000000000000000000, 0.000000000000000000 ) ) ;
#6562=LINE ( 'NONE', #13152, #36569 ) ;
#6575=ADVANCED_FACE ( 'NONE', ( #22204 ), #2697, .T. ) ;
#6579=SURFACE_STYLE_USAGE ( .BOTH. , #13169 ) ;
#6580=FACE_OUTER_BOUND ( 'NONE', #28729, .T. ) ;
#6583=CYLINDRICAL_SURFACE ( 'NONE', #41258, 19.99999999999999645 ) ;
#6585=AXIS2_PLACEMENT_3D ( 'NONE', #26737, #43085, #30227 ) ;
#6587=FACE_OUTER_BOUND ( 'NONE', #25710, .T. ) ;
#6590=DIRECTION ( 'NONE',  ( 0.000000000000000000, 0.1253332335643046747, -0.9921147013144777649 ) ) ;
#6595=CARTESIAN_POINT ( 'NONE',  ( 18.00000000000000355, -12.30077720129131791, 50.52416135122076923 ) ) ;
#6597=CARTESIAN_POINT ( 'NONE',  ( 18.00000000000000355, 0.2227391519123156360, -46.98410307550729215 ) ) ;
#6598=AXIS2_PLACEMENT_3D ( 'NONE', #14075, #13640, #27366 ) ;
#6605=EDGE_CURVE ( 'NONE', #22812, #39801, #1845, .T. ) ;
#6612=EDGE_CURVE ( 'NONE', #42150, #19793, #20011, .T. ) ;
#6613=ORIENTED_EDGE ( 'NONE', *, *, #27240, .T. ) ;
#6615=AXIS2_PLACEMENT_3D ( 'NONE', #28375, #1930, #35519 ) ;
#6616=CARTESIAN_POINT ( 'NONE',  ( 0.000000000000000000, 0.000000000000000000, 0.000000000000000000 ) ) ;
#6625=DIRECTION ( 'NONE',  ( -1.000000000000000000, -0.000000000000000000, -0.000000000000000000 ) ) ;
#6635=CARTESIAN_POINT ( 'NONE',  ( 18.00000000000000355, -19.74581912682808493, -48.10512059033413124 ) ) ;
#6645=FACE_OUTER_BOUND ( 'NONE', #14197, .T. ) ;
#6649=AXIS2_PLACEMENT_3D ( 'NONE', #402, #21189, #17924 ) ;
#6652=EDGE_LOOP ( 'NONE', ( #39273, #13375, #31887, #38445 ) ) ;
#6663=CARTESIAN_POINT ( 'NONE',  ( 0.000000000000000000, 0.000000000000000000, 0.000000000000000000 ) ) ;
#6669=LINE ( 'NONE', #40029, #30645 ) ;
#6670=CIRCLE ( 'NONE', #5951, 51.99999999999999289 ) ;
#6678=CIRCLE ( 'NONE', #4588, 20.00000000000001066 ) ;
#6680=CIRCLE ( 'NONE', #2488, 52.00000000000000000 ) ;
#6681=CARTESIAN_POINT ( 'NONE',  ( 18.00000000000000355, -46.87740477351720614, 3.172455868805039270 ) ) ;
#6682=CARTESIAN_POINT ( 'NONE',  ( 18.00000000000000355, 0.000000000000000000, 0.000000000000000000 ) ) ;
#6684=AXIS2_PLACEMENT_3D ( 'NONE', #9054, #12564, #33258 ) ;
#6686=CYLINDRICAL_SURFACE ( 'NONE', #21183, 51.99999999999999289 ) ;
#6690=DIRECTION ( 'NONE',  ( 0.000000000000000000, 0.000000000000000000, 1.000000000000000000 ) ) ;
#6699=DIRECTION ( 'NONE',  ( 1.000000000000000000, 0.000000000000000000, 0.000000000000000000 ) ) ;
#6700=ORIENTED_EDGE ( 'NONE', *, *, #31609, .T. ) ;
#6701=EDGE_LOOP ( 'NONE', ( #37988, #10263, #35275, #11956 ) ) ;
#6707=ORIENTED_EDGE ( 'NONE', *, *, #40336, .T. ) ;
#6715=ORIENTED_EDGE ( 'NONE', *, *, #39039, .F. ) ;
#6722=ORIENTED_EDGE ( 'NONE', *, *, #4307, .F. ) ;
#6724=ORIENTED_EDGE ( 'NONE', *, *, #19734, .T. ) ;
#6740=VERTEX_POINT ( 'NONE', #31713 ) ;
#6747=VERTEX_POINT ( 'NONE', #41292 ) ;
#6748=AXIS2_PLACEMENT_3D ( 'NONE', #8811, #8175, #38471 ) ;
#6752=EDGE_CURVE ( 'NONE', #34203, #42167, #30854, .T. ) ;
#6770=DIRECTION ( 'NONE',  ( 0.000000000000000000, 0.000000000000000000, 1.000000000000000000 ) ) ;
#6772=VECTOR ( 'NONE', #8323, 1000.000000000000000 ) ;
#6790=CARTESIAN_POINT ( 'NONE',  ( 18.00000000000000355, -46.77034588191287412, -22.72740077717278595 ) ) ;
#6794=ORIENTED_EDGE ( 'NONE', *, *, #31413, .F. ) ;
#6803=CIRCLE ( 'NONE', #43011, 20.00000000000000711 ) ;
#6811=AXIS2_PLACEMENT_3D ( 'NONE', #36916, #36471, #6590 ) ;
#6814=EDGE_LOOP ( 'NONE', ( #37903, #18960, #22455, #2363 ) ) ;
#6815=DIRECTION ( 'NONE',  ( -1.000000000000000000, 0.000000000000000000, 0.000000000000000000 ) ) ;
#6820=ORIENTED_EDGE ( 'NONE', *, *, #30353, .T. ) ;
#6823=ORIENTED_EDGE ( 'NONE', *, *, #34847, .F. ) ;
#6829=ORIENTED_EDGE ( 'NONE', *, *, #12813, .T. ) ;
#6834=VECTOR ( 'NONE', #37612, 1000.000000000000000 ) ;
#6838=ORIENTED_EDGE ( 'NONE', *, *, #18158, .T. ) ;
#6841=CIRCLE ( 'NONE', #18057, 47.49899999999999523 ) ;
#6844=CARTESIAN_POINT ( 'NONE',  ( 18.00000000000000355, 9.744342220504043084, -46.48873837489787064 ) ) ;
#6845=CARTESIAN_POINT ( 'NONE',  ( 0.000000000000000000, 0.000000000000000000, 0.000000000000000000 ) ) ;
#6850=FACE_OUTER_BOUND ( 'NONE', #25759, .T. ) ;
#6854=VERTEX_POINT ( 'NONE', #24345 ) ;
#6861=CARTESIAN_POINT ( 'NONE',  ( 18.00000000000000355, 51.19683565102456413, -9.104066087302928878 ) ) ;
#6862=AXIS2_PLACEMENT_3D ( 'NONE', #35101, #29225, #38580 ) ;
#6870=CARTESIAN_POINT ( 'NONE',  ( 0.000000000000000000, 0.000000000000000000, 0.000000000000000000 ) ) ;
#6871=CARTESIAN_POINT ( 'NONE',  ( 0.000000000000000000, 31.08872492059957793, 41.68322423723110148 ) ) ;
#6873=ORIENTED_EDGE ( 'NONE', *, *, #37104, .T. ) ;
#6877=DIRECTION ( 'NONE',  ( -1.000000000000000000, 0.000000000000000000, 0.000000000000000000 ) ) ;
#6881=DIRECTION ( 'NONE',  ( 1.000000000000000000, 0.000000000000000000, 0.000000000000000000 ) ) ;
#6886=DIRECTION ( 'NONE',  ( -1.000000000000000000, 0.000000000000000000, 0.000000000000000000 ) ) ;
#6895=CYLINDRICAL_SURFACE ( 'NONE', #32941, 20.00000000000000355 ) ;
#6900=DIRECTION ( 'NONE',  ( 0.000000000000000000, -0.4817536741017036661, -0.8763066800438700232 ) ) ;
#6909=CARTESIAN_POINT ( 'NONE',  ( 0.000000000000000000, 0.000000000000000000, 0.000000000000000000 ) ) ;
#6913=DIRECTION ( 'NONE',  ( 1.000000000000000000, -0.000000000000000000, -0.000000000000000000 ) ) ;
#6916=AXIS2_PLACEMENT_3D ( 'NONE', #41269, #28444, #21493 ) ;
#6918=DIRECTION ( 'NONE',  ( -1.000000000000000000, -0.000000000000000000, 0.000000000000000000 ) ) ;
#6919=VERTEX_POINT ( 'NONE', #35604 ) ;
#6930=CARTESIAN_POINT ( 'NONE',  ( 18.00000000000000355, -46.21320724403656044, 10.97699764141937173 ) ) ;
#6933=ORIENTED_EDGE ( 'NONE', *, *, #30191, .F. ) ;
#6939=DIRECTION ( 'NONE',  ( 0.000000000000000000, 0.000000000000000000, 1.000000000000000000 ) ) ;
#6948=CYLINDRICAL_SURFACE ( 'NONE', #38455, 20.00000000000000355 ) ;
#6953=DIRECTION ( 'NONE',  ( 0.000000000000000000, 0.6845471059286899473, -0.7289686274214103312 ) ) ;
#6964=EDGE_CURVE ( 'NONE', #4247, #33656, #39241, .T. ) ;
#6965=ORIENTED_EDGE ( 'NONE', *, *, #39822, .T. ) ;
#6966=LINE ( 'NONE', #178, #2314 ) ;
#6968=EDGE_CURVE ( 'NONE', #17810, #25329, #37856, .T. ) ;
#6973=CARTESIAN_POINT ( 'NONE',  ( 18.00000000000000355, -46.21320724403641833, -10.97699764142002188 ) ) ;
#6983=ORIENTED_EDGE ( 'NONE', *, *, #39345, .F. ) ;
#6988=DIRECTION ( 'NONE',  ( -1.000000000000000000, 0.000000000000000000, -0.000000000000000000 ) ) ;
#6995=CIRCLE ( 'NONE', #41121, 47.49899999999999523 ) ;
#7005=ORIENTED_EDGE ( 'NONE', *, *, #7327, .T. ) ;
#7009=DIRECTION ( 'NONE',  ( 0.000000000000000000, 0.000000000000000000, 1.000000000000000000 ) ) ;
#7014=EDGE_CURVE ( 'NONE', #7783, #14470, #39771, .T. ) ;
#7023=ORIENTED_EDGE ( 'NONE', *, *, #6968, .T. ) ;
#7024=DIRECTION ( 'NONE',  ( -1.000000000000000000, -0.000000000000000000, -0.000000000000000000 ) ) ;
#7031=DIRECTION ( 'NONE',  ( 0.000000000000000000, 0.000000000000000000, 1.000000000000000000 ) ) ;
#7033=AXIS2_PLACEMENT_3D ( 'NONE', #2474, #29145, #15618 ) ;
#7036=EDGE_LOOP ( 'NONE', ( #6389, #21781, #2234, #42687 ) ) ;
#7049=AXIS2_PLACEMENT_3D ( 'NONE', #24222, #5563, #32176 ) ;
#7050=EDGE_CURVE ( 'NONE', #13399, #40171, #30372, .T. ) ;
#7052=CARTESIAN_POINT ( 'NONE',  ( 9.000000000000001776, 5.871425383721550872, 51.66745943012283959 ) ) ;
#7055=DIRECTION ( 'NONE',  ( -1.000000000000000000, -0.000000000000000000, 0.000000000000000000 ) ) ;
#7062=EDGE_CURVE ( 'NONE', #31919, #9735, #10068, .T. ) ;
#7067=AXIS2_PLACEMENT_3D ( 'NONE', #36334, #19801, #42663 ) ;
#7070=DIRECTION ( 'NONE',  ( 0.000000000000000000, 0.000000000000000000, 1.000000000000000000 ) ) ;
#7072=CIRCLE ( 'NONE', #31487, 47.49900000000000233 ) ;
#7083=ORIENTED_EDGE ( 'NONE', *, *, #39545, .F. ) ;
#7094=VERTEX_POINT ( 'NONE', #32976 ) ;
#7097=LINE ( 'NONE', #23509, #33548 ) ;
#7099=AXIS2_PLACEMENT_3D ( 'NONE', #10971, #33429, #13601 ) ;
#7100=ADVANCED_FACE ( 'NONE', ( #40377 ), #17319, .T. ) ;
#7115=VERTEX_POINT ( 'NONE', #27319 ) ;
#7125=EDGE_CURVE ( 'NONE', #15611, #31395, #4213, .T. ) ;
#7146=CARTESIAN_POINT ( 'NONE',  ( 0.000000000000000000, 0.000000000000000000, 52.00000000000000711 ) ) ;
#7150=DIRECTION ( 'NONE',  ( -1.000000000000000000, 0.000000000000000000, 0.000000000000000000 ) ) ;
#7161=CARTESIAN_POINT ( 'NONE',  ( 0.000000000000000000, 0.000000000000000000, 0.000000000000000000 ) ) ;
#7167=DIRECTION ( 'NONE',  ( -1.000000000000000000, -0.000000000000000000, -0.000000000000000000 ) ) ;
#7181=VERTEX_POINT ( 'NONE', #31012 ) ;
#7189=DIRECTION ( 'NONE',  ( -1.000000000000000000, 0.000000000000000000, 0.000000000000000000 ) ) ;
#7193=VECTOR ( 'NONE', #23304, 1000.000000000000000 ) ;
#7194=ORIENTED_EDGE ( 'NONE', *, *, #17419, .T. ) ;
#7197=ORIENTED_EDGE ( 'NONE', *, *, #7062, .T. ) ;
#7201=AXIS2_PLACEMENT_3D ( 'NONE', #34044, #4347, #24268 ) ;
#7207=DIRECTION ( 'NONE',  ( -1.000000000000000000, 0.000000000000000000, 0.000000000000000000 ) ) ;
#7209=AXIS2_PLACEMENT_3D ( 'NONE', #38402, #31446, #5246 ) ;
#7212=EDGE_CURVE ( 'NONE', #16407, #35106, #13761, .T. ) ;
#7220=DIRECTION ( 'NONE',  ( -1.000000000000000000, 0.000000000000000000, 0.000000000000000000 ) ) ;
#7222=EDGE_CURVE ( 'NONE', #31709, #41179, #476, .T. ) ;
#7228=LINE ( 'NONE', #33856, #6093 ) ;
#7233=ORIENTED_EDGE ( 'NONE', *, *, #39803, .T. ) ;
#7235=EDGE_CURVE ( 'NONE', #4843, #33515, #14889, .T. ) ;
#7244=ORIENTED_EDGE ( 'NONE', *, *, #133, .F. ) ;
#7245=CARTESIAN_POINT ( 'NONE',  ( 18.00000000000000355, -13.85708833599999856, 45.43276465116660745 ) ) ;
#7251=ORIENTED_EDGE ( 'NONE', *, *, #38344, .F. ) ;
#7255=EDGE_LOOP ( 'NONE', ( #38382, #26897, #42841, #11842 ) ) ;
#7256=CARTESIAN_POINT ( 'NONE',  ( 0.000000000000000000, 0.000000000000000000, 0.000000000000000000 ) ) ;
#7259=CARTESIAN_POINT ( 'NONE',  ( 0.000000000000000000, 49.65209126885784485, -15.44894276735497485 ) ) ;
#7261=DIRECTION ( 'NONE',  ( 0.000000000000000000, 0.000000000000000000, 1.000000000000000000 ) ) ;
#7270=DIRECTION ( 'NONE',  ( -1.000000000000000000, -0.000000000000000000, -0.000000000000000000 ) ) ;
#7271=EDGE_CURVE ( 'NONE', #3192, #6092, #37426, .T. ) ;
#7276=EDGE_CURVE ( 'NONE', #23500, #26596, #13351, .T. ) ;
#7278=AXIS2_PLACEMENT_3D ( 'NONE', #10425, #30511, #8233 ) ;
#7282=DIRECTION ( 'NONE',  ( -1.000000000000000000, 0.000000000000000000, 0.000000000000000000 ) ) ;
#7286=EDGE_LOOP ( 'NONE', ( #29648, #41949, #311, #5827 ) ) ;
#7300=FACE_OUTER_BOUND ( 'NONE', #26915, .T. ) ;
#7306=EDGE_LOOP ( 'NONE', ( #6707, #24571, #7640, #5277 ) ) ;
#7313=CYLINDRICAL_SURFACE ( 'NONE', #35206, 51.99999999999999289 ) ;
#7317=EDGE_CURVE ( 'NONE', #21574, #36583, #23168, .T. ) ;
#7318=AXIS2_PLACEMENT_3D ( 'NONE', #21289, #1808, #41733 ) ;
#7320=CARTESIAN_POINT ( 'NONE',  ( -10.00000000000000000, 0.000000000000000000, 0.000000000000000000 ) ) ;
#7327=EDGE_CURVE ( 'NONE', #28038, #20877, #1483, .T. ) ;
#7328=AXIS2_PLACEMENT_3D ( 'NONE', #7874, #4595, #31241 ) ;
#7329=VECTOR ( 'NONE', #28651, 1000.000000000000000 ) ;
#7337=CARTESIAN_POINT ( 'NONE',  ( 18.00000000000000355, -44.25018368420762016, 27.31155879685165999 ) ) ;
#7339=AXIS2_PLACEMENT_3D ( 'NONE', #7510, #14088, #27381 ) ;
#7347=EDGE_CURVE ( 'NONE', #1606, #4068, #23823, .T. ) ;
#7350=EDGE_CURVE ( 'NONE', #9086, #1020, #16153, .T. ) ;
#7362=AXIS2_PLACEMENT_3D ( 'NONE', #21071, #20625, #23464 ) ;
#7368=DIRECTION ( 'NONE',  ( 0.000000000000000000, 0.000000000000000000, 1.000000000000000000 ) ) ;
#7371=CYLINDRICAL_SURFACE ( 'NONE', #34806, 47.49900000000000233 ) ;
#7374=DIRECTION ( 'NONE',  ( 0.000000000000000000, 0.4817536741017162671, -0.8763066800438630288 ) ) ;
#7392=ORIENTED_EDGE ( 'NONE', *, *, #30286, .F. ) ;
#7397=VECTOR ( 'NONE', #33911, 1000.000000000000000 ) ;
#7401=CARTESIAN_POINT ( 'NONE',  ( 18.00000000000000355, 0.000000000000000000, 0.000000000000000000 ) ) ;
#7402=EDGE_CURVE ( 'NONE', #20302, #32639, #37629, .T. ) ;
#7406=CARTESIAN_POINT ( 'NONE',  ( 0.000000000000000000, -12.30077720129131258, 50.52416135122076923 ) ) ;
#7408=DIRECTION ( 'NONE',  ( 0.000000000000000000, -0.9048270524660145808, -0.4257792915650830956 ) ) ;
#7411=CIRCLE ( 'NONE', #15786, 20.00000000000000711 ) ;
#7414=FACE_OUTER_BOUND ( 'NONE', #14579, .T. ) ;
#7418=CYLINDRICAL_SURFACE ( 'NONE', #15270, 20.00000000000000355 ) ;
#7420=EDGE_LOOP ( 'NONE', ( #8523, #35725, #39660, #33761 ) ) ;
#7439=ORIENTED_EDGE ( 'NONE', *, *, #24633, .T. ) ;
#7444=EDGE_LOOP ( 'NONE', ( #36460, #14540, #37342, #6032 ) ) ;
#7456=CARTESIAN_POINT ( 'NONE',  ( 18.00000000000000355, -5.871425383721897262, 51.66745943012279696 ) ) ;
#7464=DIRECTION ( 'NONE',  ( -1.000000000000000000, -0.000000000000000000, 0.000000000000000000 ) ) ;
#7469=AXIS2_PLACEMENT_3D ( 'NONE', #21744, #28692, #38685 ) ;
#7470=DIRECTION ( 'NONE',  ( 0.000000000000000000, 0.4817536741017100499, 0.8763066800438663595 ) ) ;
#7481=ORIENTED_EDGE ( 'NONE', *, *, #400, .F. ) ;
#7482=DIRECTION ( 'NONE',  ( 1.000000000000000000, 0.000000000000000000, 0.000000000000000000 ) ) ;
#7484=CARTESIAN_POINT ( 'NONE',  ( 18.00000000000000355, 46.21320724403663860, -10.97699764141904843 ) ) ;
#7487=CIRCLE ( 'NONE', #527, 52.00000000000000000 ) ;
#7510=CARTESIAN_POINT ( 'NONE',  ( 0.000000000000000000, -39.55064067543046491, -25.36340625197400200 ) ) ;
#7518=AXIS2_PLACEMENT_3D ( 'NONE', #32311, #35575, #2619 ) ;
#7519=LINE ( 'NONE', #24791, #27007 ) ;
#7520=FACE_OUTER_BOUND ( 'NONE', #30458, .T. ) ;
#7524=AXIS2_PLACEMENT_3D ( 'NONE', #18355, #18568, #38362 ) ;
#7527=AXIS2_PLACEMENT_3D ( 'NONE', #21787, #18294, #5578 ) ;
#7530=VECTOR ( 'NONE', #1605, 1000.000000000000000 ) ;
#7534=EDGE_CURVE ( 'NONE', #20186, #24437, #6298, .T. ) ;
#7537=CIRCLE ( 'NONE', #13826, 52.00000000000000000 ) ;
#7544=DIRECTION ( 'NONE',  ( 0.000000000000000000, 0.000000000000000000, 1.000000000000000000 ) ) ;
#7548=ORIENTED_EDGE ( 'NONE', *, *, #25557, .T. ) ;
#7555=DIRECTION ( 'NONE',  ( -1.000000000000000000, -0.000000000000000000, -0.000000000000000000 ) ) ;
#7559=ORIENTED_EDGE ( 'NONE', *, *, #20501, .T. ) ;
#7561=ORIENTED_EDGE ( 'NONE', *, *, #20810, .F. ) ;
#7569=CARTESIAN_POINT ( 'NONE',  ( 18.00000000000000355, 44.75336757549779776, 14.30704879393622164 ) ) ;
#7570=EDGE_LOOP ( 'NONE', ( #18173, #9826, #39455, #24551 ) ) ;
#7577=DIRECTION ( 'NONE',  ( -1.000000000000000000, -0.000000000000000000, 0.000000000000000000 ) ) ;
#7586=AXIS2_PLACEMENT_3D ( 'NONE', #26533, #39805, #35891 ) ;
#7587=VERTEX_POINT ( 'NONE', #23809 ) ;
#7591=LINE ( 'NONE', #30522, #3783 ) ;
#7605=DIRECTION ( 'NONE',  ( -1.000000000000000000, 0.000000000000000000, 0.000000000000000000 ) ) ;
#7608=DIRECTION ( 'NONE',  ( -1.000000000000000000, -0.000000000000000000, 0.000000000000000000 ) ) ;
#7616=DIRECTION ( 'NONE',  ( -1.000000000000000000, -0.000000000000000000, -0.000000000000000000 ) ) ;
#7622=LINE ( 'NONE', #17046, #16079 ) ;
#7627=DIRECTION ( 'NONE',  ( -1.000000000000000000, 0.000000000000000000, 0.000000000000000000 ) ) ;
#7632=ORIENTED_EDGE ( 'NONE', *, *, #14583, .T. ) ;
#7635=CYLINDRICAL_SURFACE ( 'NONE', #40637, 20.00000000000000711 ) ;
#7636=VECTOR ( 'NONE', #36336, 1000.000000000000000 ) ;
#7639=CYLINDRICAL_SURFACE ( 'NONE', #32487, 11.00000000000000000 ) ;
#7640=ORIENTED_EDGE ( 'NONE', *, *, #27370, .T. ) ;
#7645=DIRECTION ( 'NONE',  ( -1.000000000000000000, -0.000000000000000000, 0.000000000000000000 ) ) ;
#7647=EDGE_CURVE ( 'NONE', #6443, #9628, #7622, .T. ) ;
#7649=DIRECTION ( 'NONE',  ( -1.000000000000000000, -0.000000000000000000, -0.000000000000000000 ) ) ;
#7650=EDGE_CURVE ( 'NONE', #22785, #6740, #20118, .T. ) ;
#7654=ORIENTED_EDGE ( 'NONE', *, *, #16361, .F. ) ;
#7659=DIRECTION ( 'NONE',  ( -1.000000000000000000, 0.000000000000000000, 0.000000000000000000 ) ) ;
#7660=CARTESIAN_POINT ( 'NONE',  ( 0.000000000000000000, 46.21320724403648939, 10.97699764141968970 ) ) ;
#7676=ORIENTED_EDGE ( 'NONE', *, *, #17827, .F. ) ;
#7678=DIRECTION ( 'NONE',  ( -1.000000000000000000, 0.000000000000000000, 0.000000000000000000 ) ) ;
#7682=LINE ( 'NONE', #27135, #23419 ) ;
#7703=ADVANCED_FACE ( 'NONE', ( #24465 ), #35098, .T. ) ;
#7704=EDGE_CURVE ( 'NONE', #38773, #13970, #28379, .T. ) ;
#7710=EDGE_CURVE ( 'NONE', #32276, #37957, #32075, .T. ) ;
#7732=DIRECTION ( 'NONE',  ( -1.000000000000000000, 0.000000000000000000, 0.000000000000000000 ) ) ;
#7734=CYLINDRICAL_SURFACE ( 'NONE', #17982, 20.00000000000000711 ) ;
#7743=VECTOR ( 'NONE', #20514, 1000.000000000000000 ) ;
#7744=ORIENTED_EDGE ( 'NONE', *, *, #2075, .F. ) ;
#7759=ORIENTED_EDGE ( 'NONE', *, *, #31886, .T. ) ;
#7762=DIRECTION ( 'NONE',  ( 0.000000000000000000, 0.000000000000000000, 1.000000000000000000 ) ) ;
#7763=CIRCLE ( 'NONE', #25225, 20.00000000000000711 ) ;
#7771=ORIENTED_EDGE ( 'NONE', *, *, #8265, .F. ) ;
#7773=AXIS2_PLACEMENT_3D ( 'NONE', #9895, #12345, #26288 ) ;
#7782=CARTESIAN_POINT ( 'NONE',  ( 18.00000000000000355, -47.00885577955406802, -6.806061952192774989 ) ) ;
#7783=VERTEX_POINT ( 'NONE', #34888 ) ;
#7788=DIRECTION ( 'NONE',  ( 0.000000000000000000, 0.000000000000000000, 1.000000000000000000 ) ) ;
#7789=EDGE_LOOP ( 'NONE', ( #12020, #43015, #25810, #30858 ) ) ;
#7796=CIRCLE ( 'NONE', #32185, 47.49900000000000233 ) ;
#7797=ORIENTED_EDGE ( 'NONE', *, *, #4357, .T. ) ;
#7799=CARTESIAN_POINT ( 'NONE',  ( 18.00000000000000355, 0.2227391519123156360, -46.98410307550729215 ) ) ;
#7801=CARTESIAN_POINT ( 'NONE',  ( 18.00000000000000355, 46.19362259308835661, 8.585149169758654608 ) ) ;
#7803=CYLINDRICAL_SURFACE ( 'NONE', #28171, 20.00000000000000355 ) ;
#7804=ORIENTED_EDGE ( 'NONE', *, *, #39165, .F. ) ;
#7808=LINE ( 'NONE', #34415, #25194 ) ;
#7810=CYLINDRICAL_SURFACE ( 'NONE', #32505, 20.00000000000000711 ) ;
#7819=DIRECTION ( 'NONE',  ( 0.000000000000000000, -0.9510565162951565288, 0.3090169943749383474 ) ) ;
#7820=CARTESIAN_POINT ( 'NONE',  ( 18.00000000000000355, 47.00885577955412487, 6.806061952192453468 ) ) ;
#7829=ADVANCED_FACE ( 'NONE', ( #35523 ), #33109, .T. ) ;
#7831=AXIS2_PLACEMENT_3D ( 'NONE', #10950, #7207, #14221 ) ;
#7837=CARTESIAN_POINT ( 'NONE',  ( 18.00000000000000355, -46.19362259308839214, 8.585149169758333088 ) ) ;
#7838=DIRECTION ( 'NONE',  ( -1.000000000000000000, 0.000000000000000000, 0.000000000000000000 ) ) ;
#7844=EDGE_LOOP ( 'NONE', ( #25517, #10385, #1077, #35013 ) ) ;
#7845=EDGE_CURVE ( 'NONE', #34783, #19720, #18915, .T. ) ;
#7849=LINE ( 'NONE', #3904, #35366 ) ;
#7857=CIRCLE ( 'NONE', #39882, 47.49900000000000233 ) ;
#7859=CARTESIAN_POINT ( 'NONE',  ( 18.00000000000000355, 30.93515269692114344, 36.04401931830261674 ) ) ;
#7861=CARTESIAN_POINT ( 'NONE',  ( 18.00000000000000355, 0.000000000000000000, 0.000000000000000000 ) ) ;
#7864=DIRECTION ( 'NONE',  ( -1.000000000000000000, 0.000000000000000000, 0.000000000000000000 ) ) ;
#7869=EDGE_CURVE ( 'NONE', #9771, #22661, #29012, .T. ) ;
#7870=CARTESIAN_POINT ( 'NONE',  ( 0.000000000000000000, -30.03615769709704608, -42.44795908869020451 ) ) ;
#7874=CARTESIAN_POINT ( 'NONE',  ( 0.000000000000000000, 0.000000000000000000, 0.000000000000000000 ) ) ;
#7877=ORIENTED_EDGE ( 'NONE', *, *, #5940, .F. ) ;
#7879=EDGE_CURVE ( 'NONE', #14699, #41127, #6, .T. ) ;
#7880=CARTESIAN_POINT ( 'NONE',  ( 9.000000000000001776, 43.55304910509406113, 28.41006711800000062 ) ) ;
#7887=( GEOMETRIC_REPRESENTATION_CONTEXT ( 3 ) GLOBAL_UNCERTAINTY_ASSIGNED_CONTEXT ( ( #29032 ) ) GLOBAL_UNIT_ASSIGNED_CONTEXT ( ( #12352, #5985, #38498 ) ) REPRESENTATION_CONTEXT ( 'NONE', 'WORKASPACE' ) );
#7891=CARTESIAN_POINT ( 'NONE',  ( 18.00000000000000355, -8.053585752061598768, -46.81126742072031988 ) ) ;
#7894=EDGE_CURVE ( 'NONE', #21438, #33305, #17530, .T. ) ;
#7910=DIRECTION ( 'NONE',  ( 0.000000000000000000, 0.000000000000000000, -1.000000000000000000 ) ) ;
#7920=CARTESIAN_POINT ( 'NONE',  ( 18.00000000000000355, 0.000000000000000000, 0.000000000000000000 ) ) ;
#7935=DIRECTION ( 'NONE',  ( 0.000000000000000000, 0.000000000000000000, 1.000000000000000000 ) ) ;
#7937=CARTESIAN_POINT ( 'NONE',  ( 18.00000000000000355, 32.00046193115198179, -34.40241257139653186 ) ) ;
#7940=CARTESIAN_POINT ( 'NONE',  ( 18.00000000000000355, 42.41764978026606769, 20.20639853260304619 ) ) ;
#7941=ORIENTED_EDGE ( 'NONE', *, *, #19172, .T. ) ;
#7944=EDGE_CURVE ( 'NONE', #19546, #30887, #19843, .T. ) ;
#7948=CARTESIAN_POINT ( 'NONE',  ( 0.000000000000000000, 0.000000000000000000, 0.000000000000000000 ) ) ;
#7952=DIRECTION ( 'NONE',  ( -1.000000000000000000, -0.000000000000000000, -0.000000000000000000 ) ) ;
#7954=ADVANCED_FACE ( 'NONE', ( #9980 ), #37241, .F. ) ;
#7960=DIRECTION ( 'NONE',  ( 0.000000000000000000, 0.1253332335643045359, -0.9921147013144778759 ) ) ;
#7962=DIRECTION ( 'NONE',  ( -1.000000000000000000, -0.000000000000000000, -0.000000000000000000 ) ) ;
#7965=ORIENTED_EDGE ( 'NONE', *, *, #361, .F. ) ;
#7968=AXIS2_PLACEMENT_3D ( 'NONE', #3359, #20004, #20219 ) ;
#7969=CARTESIAN_POINT ( 'NONE',  ( 0.000000000000000000, 42.03146605346817921, -22.12489237027272893 ) ) ;
#7976=AXIS2_PLACEMENT_3D ( 'NONE', #28745, #9510, #35260 ) ;
#7981=ORIENTED_EDGE ( 'NONE', *, *, #29534, .T. ) ;
#7984=ORIENTED_EDGE ( 'NONE', *, *, #39941, .T. ) ;
#7992=CIRCLE ( 'NONE', #32379, 20.00000000000000711 ) ;
#7993=ORIENTED_EDGE ( 'NONE', *, *, #35383, .T. ) ;
#7995=VERTEX_POINT ( 'NONE', #33980 ) ;
#7999=VECTOR ( 'NONE', #38507, 1000.000000000000000 ) ;
#8004=ORIENTED_EDGE ( 'NONE', *, *, #37912, .T. ) ;
#8006=CIRCLE ( 'NONE', #6585, 52.00000000000000000 ) ;
#8010=DIRECTION ( 'NONE',  ( -1.000000000000000000, -0.000000000000000000, -0.000000000000000000 ) ) ;
#8014=DIRECTION ( 'NONE',  ( -1.000000000000000000, -0.000000000000000000, -0.000000000000000000 ) ) ;
#8021=CARTESIAN_POINT ( 'NONE',  ( 0.000000000000000000, -32.00046193115124282, -34.40241257139720688 ) ) ;
#8035=ORIENTED_EDGE ( 'NONE', *, *, #37553, .T. ) ;
#8037=AXIS2_PLACEMENT_3D ( 'NONE', #41744, #18041, #31512 ) ;
#8039=CARTESIAN_POINT ( 'NONE',  ( 0.000000000000000000, 15.49408907645171674, 44.90087086784597403 ) ) ;
#8046=DIRECTION ( 'NONE',  ( 0.000000000000000000, 0.9980267284282713369, 0.06279051952931692659 ) ) ;
#8051=EDGE_CURVE ( 'NONE', #11670, #32336, #22394, .T. ) ;
#8055=EDGE_CURVE ( 'NONE', #2747, #32585, #9110, .T. ) ;
#8056=AXIS2_PLACEMENT_3D ( 'NONE', #24720, #27115, #37554 ) ;
#8059=FACE_OUTER_BOUND ( 'NONE', #19741, .T. ) ;
#8065=AXIS2_PLACEMENT_3D ( 'NONE', #23802, #37711, #24243 ) ;
#8068=DIRECTION ( 'NONE',  ( 1.000000000000000000, 0.000000000000000000, 0.000000000000000000 ) ) ;
#8073=ORIENTED_EDGE ( 'NONE', *, *, #40077, .F. ) ;
#8074=DIRECTION ( 'NONE',  ( 0.000000000000000000, 0.5877852522924685852, 0.8090169943749507819 ) ) ;
#8077=ORIENTED_EDGE ( 'NONE', *, *, #42674, .F. ) ;
#8093=ORIENTED_EDGE ( 'NONE', *, *, #10290, .T. ) ;
#8099=ORIENTED_EDGE ( 'NONE', *, *, #35616, .T. ) ;
#8101=AXIS2_PLACEMENT_3D ( 'NONE', #23837, #37101, #14219 ) ;
#8102=CARTESIAN_POINT ( 'NONE',  ( 0.000000000000000000, -22.43957647427129842, -41.27978878573651400 ) ) ;
#8108=DIRECTION ( 'NONE',  ( -1.000000000000000000, 0.000000000000000000, -0.000000000000000000 ) ) ;
#8111=VERTEX_POINT ( 'NONE', #34839 ) ;
#8113=ORIENTED_EDGE ( 'NONE', *, *, #31886, .F. ) ;
#8122=CIRCLE ( 'NONE', #12313, 47.49900000000000233 ) ;
#8126=EDGE_CURVE ( 'NONE', #20431, #1556, #42532, .T. ) ;
#8127=ORIENTED_EDGE ( 'NONE', *, *, #31027, .T. ) ;
#8147=ORIENTED_EDGE ( 'NONE', *, *, #22989, .T. ) ;
#8150=ORIENTED_EDGE ( 'NONE', *, *, #37855, .F. ) ;
#8155=AXIS2_PLACEMENT_3D ( 'NONE', #18097, #14796, #28098 ) ;
#8156=ORIENTED_EDGE ( 'NONE', *, *, #8683, .F. ) ;
#8163=ORIENTED_EDGE ( 'NONE', *, *, #25337, .F. ) ;
#8164=CARTESIAN_POINT ( 'NONE',  ( 18.00000000000000355, -47.00885577955416039, 6.806061952192135500 ) ) ;
#8169=EDGE_CURVE ( 'NONE', #28304, #42969, #15254, .T. ) ;
#8173=EDGE_LOOP ( 'NONE', ( #7676, #13776, #19033, #38901 ) ) ;
#8175=DIRECTION ( 'NONE',  ( -1.000000000000000000, -0.000000000000000000, -0.000000000000000000 ) ) ;
#8179=ORIENTED_EDGE ( 'NONE', *, *, #36594, .T. ) ;
#8180=DIRECTION ( 'NONE',  ( -1.000000000000000000, 0.000000000000000000, 0.000000000000000000 ) ) ;
#8181=CARTESIAN_POINT ( 'NONE',  ( 18.00000000000000355, -27.79676263918213763, 37.88001506494759241 ) ) ;
#8189=AXIS2_PLACEMENT_3D ( 'NONE', #25480, #35470, #36112 ) ;
#8198=CIRCLE ( 'NONE', #34662, 20.00000000000000711 ) ;
#8200=CIRCLE ( 'NONE', #20130, 47.49900000000000944 ) ;
#8202=DIRECTION ( 'NONE',  ( 0.000000000000000000, 0.000000000000000000, 1.000000000000000000 ) ) ;
#8218=FACE_OUTER_BOUND ( 'NONE', #27298, .T. ) ;
#8220=CIRCLE ( 'NONE', #13094, 20.00000000000001066 ) ;
#8233=DIRECTION ( 'NONE',  ( 0.000000000000000000, 0.3681245526846719240, 0.9297764858882537897 ) ) ;
#8239=CYLINDRICAL_SURFACE ( 'NONE', #17203, 47.49900000000000233 ) ;
#8241=DIRECTION ( 'NONE',  ( -1.000000000000000000, 0.000000000000000000, 0.000000000000000000 ) ) ;
#8242=AXIS2_PLACEMENT_3D ( 'NONE', #23889, #37376, #20198 ) ;
#8261=CARTESIAN_POINT ( 'NONE',  ( 0.000000000000000000, -40.47821179127690527, -32.64221760512802462 ) ) ;
#8263=ORIENTED_EDGE ( 'NONE', *, *, #35615, .T. ) ;
#8265=EDGE_CURVE ( 'NONE', #8333, #35102, #11979, .T. ) ;
#8271=ORIENTED_EDGE ( 'NONE', *, *, #9156, .F. ) ;
#8274=ORIENTED_EDGE ( 'NONE', *, *, #4357, .F. ) ;
#8275=CARTESIAN_POINT ( 'NONE',  ( 18.00000000000000355, 0.000000000000000000, 0.000000000000000000 ) ) ;
#8279=AXIS2_PLACEMENT_3D ( 'NONE', #10479, #16639, #39692 ) ;
#8295=EDGE_LOOP ( 'NONE', ( #3872, #14424, #35773, #944 ) ) ;
#8303=CIRCLE ( 'NONE', #13901, 52.00000000000000000 ) ;
#8304=ORIENTED_EDGE ( 'NONE', *, *, #28285, .T. ) ;
#8314=LINE ( 'NONE', #41023, #27497 ) ;
#8323=DIRECTION ( 'NONE',  ( -1.000000000000000000, 0.000000000000000000, 0.000000000000000000 ) ) ;
#8332=DIRECTION ( 'NONE',  ( 0.000000000000000000, 0.000000000000000000, 1.000000000000000000 ) ) ;
#8333=VERTEX_POINT ( 'NONE', #39596 ) ;
#8334=CARTESIAN_POINT ( 'NONE',  ( 18.00000000000000355, 0.000000000000000000, 0.000000000000000000 ) ) ;
#8338=ORIENTED_EDGE ( 'NONE', *, *, #20951, .F. ) ;
#8355=DIRECTION ( 'NONE',  ( -1.000000000000000000, 0.000000000000000000, 0.000000000000000000 ) ) ;
#8370=VERTEX_POINT ( 'NONE', #42645 ) ;
#8376=ORIENTED_EDGE ( 'NONE', *, *, #18839, .T. ) ;
#8377=CARTESIAN_POINT ( 'NONE',  ( 18.00000000000000355, 0.000000000000000000, 0.000000000000000000 ) ) ;
#8384=VERTEX_POINT ( 'NONE', #22640 ) ;
#8386=DIRECTION ( 'NONE',  ( -1.000000000000000000, -0.000000000000000000, -0.000000000000000000 ) ) ;
#8387=DIRECTION ( 'NONE',  ( 0.000000000000000000, 0.9822872507286879440, 0.1873813145857285700 ) ) ;
#8390=VERTEX_POINT ( 'NONE', #29590 ) ;
#8395=CIRCLE ( 'NONE', #2783, 20.00000000000000355 ) ;
#8398=DIRECTION ( 'NONE',  ( 0.000000000000000000, 0.000000000000000000, 1.000000000000000000 ) ) ;
#8401=ORIENTED_EDGE ( 'NONE', *, *, #5110, .T. ) ;
#8402=CARTESIAN_POINT ( 'NONE',  ( 0.000000000000000000, 0.000000000000000000, 0.000000000000000000 ) ) ;
#8405=CARTESIAN_POINT ( 'NONE',  ( -10.00000000000000000, 0.000000000000000000, 0.000000000000000000 ) ) ;
#8412=CIRCLE ( 'NONE', #15397, 47.49900000000000233 ) ;
#8419=VECTOR ( 'NONE', #26751, 1000.000000000000000 ) ;
#8425=FACE_OUTER_BOUND ( 'NONE', #31387, .T. ) ;
#8429=CARTESIAN_POINT ( 'NONE',  ( 18.00000000000000355, -29.60891106212762125, -37.14118181634796656 ) ) ;
#8441=DIRECTION ( 'NONE',  ( 0.000000000000000000, 0.000000000000000000, 1.000000000000000000 ) ) ;
#8452=FACE_OUTER_BOUND ( 'NONE', #31586, .T. ) ;
#8453=CIRCLE ( 'NONE', #17556, 51.99999999999999289 ) ;
#8463=VERTEX_POINT ( 'NONE', #533 ) ;
#8473=EDGE_CURVE ( 'NONE', #31578, #28014, #26964, .T. ) ;
#8482=CYLINDRICAL_SURFACE ( 'NONE', #23377, 51.99999999999999289 ) ;
#8483=AXIS2_PLACEMENT_3D ( 'NONE', #42745, #3253, #15978 ) ;
#8497=CARTESIAN_POINT ( 'NONE',  ( 18.00000000000000355, -8.053585752062225822, 46.81126742072019908 ) ) ;
#8498=EDGE_LOOP ( 'NONE', ( #40453, #22772, #10731, #33358 ) ) ;
#8505=DIRECTION ( 'NONE',  ( 0.000000000000000000, 0.000000000000000000, 1.000000000000000000 ) ) ;
#8507=CARTESIAN_POINT ( 'NONE',  ( 0.000000000000000000, 0.000000000000000000, 0.000000000000000000 ) ) ;
#8510=AXIS2_PLACEMENT_3D ( 'NONE', #28175, #38395, #41880 ) ;
#8511=CIRCLE ( 'NONE', #2900, 47.49900000000000233 ) ;
#8513=CYLINDRICAL_SURFACE ( 'NONE', #8510, 47.49900000000000233 ) ;
#8523=ORIENTED_EDGE ( 'NONE', *, *, #9746, .F. ) ;
#8540=DIRECTION ( 'NONE',  ( 0.000000000000000000, 0.4817536741017162116, -0.8763066800438631399 ) ) ;
#8542=EDGE_CURVE ( 'NONE', #35135, #14587, #41894, .T. ) ;
#8544=EDGE_LOOP ( 'NONE', ( #11071, #4990, #41347, #14304 ) ) ;
#8553=CARTESIAN_POINT ( 'NONE',  ( 18.00000000000000355, 26.17370628620655637, 39.63700417846172286 ) ) ;
#8564=DIRECTION ( 'NONE',  ( 0.000000000000000000, 0.8443279255020161855, -0.5358267949789946583 ) ) ;
#8567=DIRECTION ( 'NONE',  ( 0.000000000000000000, -0.7705132427757949154, 0.6374239897486827511 ) ) ;
#8578=LINE ( 'NONE', #15386, #8775 ) ;
#8581=CARTESIAN_POINT ( 'NONE',  ( 0.000000000000000000, 51.19683565102443623, 9.104066087303637644 ) ) ;
#8584=DIRECTION ( 'NONE',  ( 0.000000000000000000, -0.9822872507286865007, -0.1873813145857356199 ) ) ;
#8587=FACE_OUTER_BOUND ( 'NONE', #36805, .T. ) ;
#8589=CIRCLE ( 'NONE', #1643, 20.00000000000000711 ) ;
#8603=DIRECTION ( 'NONE',  ( -1.000000000000000000, -0.000000000000000000, 0.000000000000000000 ) ) ;
#8604=VERTEX_POINT ( 'NONE', #4235 ) ;
#8609=CIRCLE ( 'NONE', #3998, 51.99999999999999289 ) ;
#8615=ORIENTED_EDGE ( 'NONE', *, *, #17777, .F. ) ;
#8625=VECTOR ( 'NONE', #42490, 1000.000000000000000 ) ;
#8629=ADVANCED_FACE ( 'NONE', ( #40886 ), #27617, .T. ) ;
#8642=DIRECTION ( 'NONE',  ( 0.000000000000000000, 0.000000000000000000, 1.000000000000000000 ) ) ;
#8643=ORIENTED_EDGE ( 'NONE', *, *, #9591, .F. ) ;
#8649=DIRECTION ( 'NONE',  ( -1.000000000000000000, 0.000000000000000000, -0.000000000000000000 ) ) ;
#8659=AXIS2_PLACEMENT_3D ( 'NONE', #12795, #39161, #26107 ) ;
#8662=ORIENTED_EDGE ( 'NONE', *, *, #39803, .F. ) ;
#8683=EDGE_CURVE ( 'NONE', #32974, #9752, #20888, .T. ) ;
#8684=ORIENTED_EDGE ( 'NONE', *, *, #7212, .F. ) ;
#8687=EDGE_CURVE ( 'NONE', #19812, #37957, #1614, .T. ) ;
#8688=AXIS2_PLACEMENT_3D ( 'NONE', #23528, #36794, #6900 ) ;
#8699=AXIS2_PLACEMENT_3D ( 'NONE', #42623, #39570, #9903 ) ;
#8702=LINE ( 'NONE', #11801, #10361 ) ;
#8705=DIRECTION ( 'NONE',  ( -1.000000000000000000, -0.000000000000000000, 0.000000000000000000 ) ) ;
#8709=AXIS2_PLACEMENT_3D ( 'NONE', #11642, #23508, #5068 ) ;
#8711=EDGE_LOOP ( 'NONE', ( #37111, #40231, #37215, #21577 ) ) ;
#8717=EDGE_CURVE ( 'NONE', #9333, #16003, #15497, .T. ) ;
#8722=CARTESIAN_POINT ( 'NONE',  ( 18.00000000000000355, 27.79676263918187118, 37.88001506494779846 ) ) ;
#8734=EDGE_CURVE ( 'NONE', #5484, #27946, #16637, .T. ) ;
#8736=CIRCLE ( 'NONE', #40760, 20.00000000000000711 ) ;
#8737=EDGE_LOOP ( 'NONE', ( #22044, #6398, #5795, #18832 ) ) ;
#8751=DIRECTION ( 'NONE',  ( 1.000000000000000000, 0.000000000000000000, -0.000000000000000000 ) ) ;
#8752=AXIS2_PLACEMENT_3D ( 'NONE', #5333, #28697, #41963 ) ;
#8753=ORIENTED_EDGE ( 'NONE', *, *, #6450, .F. ) ;
#8759=CYLINDRICAL_SURFACE ( 'NONE', #25688, 20.00000000000000711 ) ;
#8775=VECTOR ( 'NONE', #8799, 1000.000000000000000 ) ;
#8779=CARTESIAN_POINT ( 'NONE',  ( 18.00000000000000355, 0.2227391519116599106, 46.98410307550730636 ) ) ;
#8787=ORIENTED_EDGE ( 'NONE', *, *, #11673, .T. ) ;
#8788=LINE ( 'NONE', #21724, #28935 ) ;
#8790=CARTESIAN_POINT ( 'NONE',  ( 0.000000000000000000, 0.000000000000000000, 0.000000000000000000 ) ) ;
#8791=ORIENTED_EDGE ( 'NONE', *, *, #10999, .T. ) ;
#8793=EDGE_CURVE ( 'NONE', #37085, #21443, #2617, .T. ) ;
#8798=ORIENTED_EDGE ( 'NONE', *, *, #6450, .T. ) ;
#8799=DIRECTION ( 'NONE',  ( -1.000000000000000000, -0.000000000000000000, -0.000000000000000000 ) ) ;
#8802=LINE ( 'NONE', #35418, #39298 ) ;
#8804=EDGE_CURVE ( 'NONE', #27530, #40464, #12003, .T. ) ;
#8808=DIRECTION ( 'NONE',  ( 0.000000000000000000, 0.000000000000000000, 1.000000000000000000 ) ) ;
#8811=CARTESIAN_POINT ( 'NONE',  ( -10.00000000000000000, 0.000000000000000000, 0.000000000000000000 ) ) ;
#8813=EDGE_CURVE ( 'NONE', #631, #22812, #39116, .T. ) ;
#8816=FACE_OUTER_BOUND ( 'NONE', #38739, .T. ) ;
#8821=VERTEX_POINT ( 'NONE', #19257 ) ;
#8829=DIRECTION ( 'NONE',  ( 0.000000000000000000, 0.000000000000000000, 1.000000000000000000 ) ) ;
#8834=CARTESIAN_POINT ( 'NONE',  ( 0.000000000000000000, -24.72041153920759271, 40.55929306992679528 ) ) ;
#8837=LINE ( 'NONE', #25673, #32824 ) ;
#8851=DIRECTION ( 'NONE',  ( -1.000000000000000000, -0.000000000000000000, 0.000000000000000000 ) ) ;
#8856=CARTESIAN_POINT ( 'NONE',  ( 18.00000000000000355, -42.60732521687558005, -19.80331771201703006 ) ) ;
#8860=DIRECTION ( 'NONE',  ( -1.000000000000000000, 0.000000000000000000, 0.000000000000000000 ) ) ;
#8864=EDGE_LOOP ( 'NONE', ( #33847, #19282, #19456, #13647 ) ) ;
#8866=EDGE_CURVE ( 'NONE', #1655, #11213, #7072, .T. ) ;
#8874=CARTESIAN_POINT ( 'NONE',  ( 0.000000000000000000, 41.20225022064669673, -23.63323037071358357 ) ) ;
#8894=CARTESIAN_POINT ( 'NONE',  ( 0.000000000000000000, -8.053585752061598768, -46.81126742072031988 ) ) ;
#8897=CARTESIAN_POINT ( 'NONE',  ( 18.00000000000000355, 0.000000000000000000, 0.000000000000000000 ) ) ;
#8902=ORIENTED_EDGE ( 'NONE', *, *, #28716, .F. ) ;
#8904=VERTEX_POINT ( 'NONE', #24475 ) ;
#8907=AXIS2_PLACEMENT_3D ( 'NONE', #20697, #37443, #27655 ) ;
#8911=CIRCLE ( 'NONE', #15244, 47.49900000000000233 ) ;
#8913=VERTEX_POINT ( 'NONE', #24261 ) ;
#8934=EDGE_LOOP ( 'NONE', ( #30293, #11117, #41429, #14201 ) ) ;
#8935=AXIS2_PLACEMENT_3D ( 'NONE', #16331, #22686, #39848 ) ;
#8936=AXIS2_PLACEMENT_3D ( 'NONE', #38728, #14785, #28085 ) ;
#8955=EDGE_CURVE ( 'NONE', #25103, #28038, #9195, .T. ) ;
#8956=CARTESIAN_POINT ( 'NONE',  ( -10.00000000000000000, 0.000000000000000000, 0.000000000000000000 ) ) ;
#8962=AXIS2_PLACEMENT_3D ( 'NONE', #13084, #35945, #23333 ) ;
#8971=VERTEX_POINT ( 'NONE', #30130 ) ;
#8977=CARTESIAN_POINT ( 'NONE',  ( 18.00000000000000355, -11.46872990052349550, -45.56340405422456286 ) ) ;
#8982=CARTESIAN_POINT ( 'NONE',  ( 18.00000000000000355, 2.123073309835184386, 47.45152853935334747 ) ) ;
#8992=CARTESIAN_POINT ( 'NONE',  ( 18.00000000000000355, 0.000000000000000000, 0.000000000000000000 ) ) ;
#9000=DIRECTION ( 'NONE',  ( 0.000000000000000000, -0.9510565162951500895, -0.3090169943749582204 ) ) ;
#9007=ORIENTED_EDGE ( 'NONE', *, *, #21166, .F. ) ;
#9011=ORIENTED_EDGE ( 'NONE', *, *, #31609, .F. ) ;
#9012=CARTESIAN_POINT ( 'NONE',  ( 18.00000000000000355, -41.20225022064620646, -23.63323037071445043 ) ) ;
#9013=DIRECTION ( 'NONE',  ( -1.000000000000000000, -0.000000000000000000, 0.000000000000000000 ) ) ;
#9015=VECTOR ( 'NONE', #15144, 1000.000000000000000 ) ;
#9019=ORIENTED_EDGE ( 'NONE', *, *, #20810, .T. ) ;
#9021=VERTEX_POINT ( 'NONE', #40345 ) ;
#9025=CYLINDRICAL_SURFACE ( 'NONE', #37987, 20.00000000000001066 ) ;
#9032=DIRECTION ( 'NONE',  ( -1.000000000000000000, 0.000000000000000000, -0.000000000000000000 ) ) ;
#9040=EDGE_CURVE ( 'NONE', #18339, #26486, #20383, .T. ) ;
#9044=AXIS2_PLACEMENT_3D ( 'NONE', #23960, #575, #40700 ) ;
#9052=SURFACE_STYLE_USAGE ( .BOTH. , #2690 ) ;
#9054=CARTESIAN_POINT ( 'NONE',  ( 18.00000000000000355, 17.08890430202814059, -43.76671000081927332 ) ) ;
#9062=CARTESIAN_POINT ( 'NONE',  ( 18.00000000000000355, 32.00046193115148441, 34.40241257139697950 ) ) ;
#9074=ORIENTED_EDGE ( 'NONE', *, *, #7402, .T. ) ;
#9081=ORIENTED_EDGE ( 'NONE', *, *, #35297, .T. ) ;
#9082=DIRECTION ( 'NONE',  ( 0.000000000000000000, 0.000000000000000000, 1.000000000000000000 ) ) ;
#9086=VERTEX_POINT ( 'NONE', #31856 ) ;
#9096=AXIS2_PLACEMENT_3D ( 'NONE', #8897, #22250, #18977 ) ;
#9110=CIRCLE ( 'NONE', #14025, 47.49900000000000233 ) ;
#9111=EDGE_CURVE ( 'NONE', #25035, #27234, #33581, .T. ) ;
#9134=AXIS2_PLACEMENT_3D ( 'NONE', #34519, #24095, #28011 ) ;
#9135=ORIENTED_EDGE ( 'NONE', *, *, #36701, .F. ) ;
#9152=AXIS2_PLACEMENT_3D ( 'NONE', #14458, #27765, #21026 ) ;
#9156=EDGE_CURVE ( 'NONE', #2894, #35102, #32219, .T. ) ;
#9157=CYLINDRICAL_SURFACE ( 'NONE', #37642, 47.49900000000000233 ) ;
#9164=AXIS2_PLACEMENT_3D ( 'NONE', #30683, #10825, #93 ) ;
#9173=EDGE_CURVE ( 'NONE', #23341, #3516, #24917, .T. ) ;
#9180=LINE ( 'NONE', #25996, #15247 ) ;
#9187=ADVANCED_FACE ( 'NONE', ( #24686 ), #31627, .T. ) ;
#9188=VECTOR ( 'NONE', #14217, 1000.000000000000000 ) ;
#9194=CARTESIAN_POINT ( 'NONE',  ( 18.00000000000000355, 0.000000000000000000, 0.000000000000000000 ) ) ;
#9195=CIRCLE ( 'NONE', #35659, 20.00000000000000711 ) ;
#9204=EDGE_CURVE ( 'NONE', #27281, #12154, #41232, .T. ) ;
#9225=ADVANCED_FACE ( 'NONE', ( #16137 ), #22698, .T. ) ;
#9238=DIRECTION ( 'NONE',  ( 0.000000000000000000, 0.000000000000000000, 1.000000000000000000 ) ) ;
#9239=ORIENTED_EDGE ( 'NONE', *, *, #31235, .F. ) ;
#9248=CARTESIAN_POINT ( 'NONE',  ( 18.00000000000000355, 0.000000000000000000, 0.000000000000000000 ) ) ;
#9250=ADVANCED_FACE ( 'NONE', ( #19211 ), #16586, .T. ) ;
#9253=EDGE_CURVE ( 'NONE', #19733, #255, #29427, .T. ) ;
#9254=CYLINDRICAL_SURFACE ( 'NONE', #37725, 20.00000000000000711 ) ;
#9261=AXIS2_PLACEMENT_3D ( 'NONE', #39031, #29457, #22508 ) ;
#9262=CYLINDRICAL_SURFACE ( 'NONE', #2309, 20.00000000000000711 ) ;
#9268=FACE_OUTER_BOUND ( 'NONE', #29947, .T. ) ;
#9275=EDGE_CURVE ( 'NONE', #11938, #39753, #16899, .T. ) ;
#9278=EDGE_CURVE ( 'NONE', #10268, #631, #7857, .T. ) ;
#9291=AXIS2_PLACEMENT_3D ( 'NONE', #2120, #12412, #41837 ) ;
#9294=CYLINDRICAL_SURFACE ( 'NONE', #35561, 47.49900000000000233 ) ;
#9296=CARTESIAN_POINT ( 'NONE',  ( 18.00000000000000355, -20.99948489194393275, -42.60488980472802467 ) ) ;
#9300=FACE_OUTER_BOUND ( 'NONE', #28185, .T. ) ;
#9311=CARTESIAN_POINT ( 'NONE',  ( 0.000000000000000000, 39.78933988720149273, -24.98727647984960498 ) ) ;
#9324=CARTESIAN_POINT ( 'NONE',  ( 18.00000000000000355, 0.000000000000000000, 0.000000000000000000 ) ) ;
#9333=VERTEX_POINT ( 'NONE', #9344 ) ;
#9344=CARTESIAN_POINT ( 'NONE',  ( 0.000000000000000000, 18.53613841426789222, 48.58406706613909876 ) ) ;
#9353=DIRECTION ( 'NONE',  ( -1.000000000000000000, -0.000000000000000000, -0.000000000000000000 ) ) ;
#9360=CIRCLE ( 'NONE', #33057, 52.00000000000000000 ) ;
#9361=CARTESIAN_POINT ( 'NONE',  ( 0.000000000000000000, 0.000000000000000000, 0.000000000000000000 ) ) ;
#9365=CYLINDRICAL_SURFACE ( 'NONE', #14703, 51.99999999999999289 ) ;
#9370=EDGE_LOOP ( 'NONE', ( #2755, #30348, #4749, #32743 ) ) ;
#9372=EDGE_CURVE ( 'NONE', #11416, #640, #12060, .T. ) ;
#9375=AXIS2_PLACEMENT_3D ( 'NONE', #37161, #13423, #3551 ) ;
#9377=DIRECTION ( 'NONE',  ( 1.000000000000000000, -0.000000000000000000, 0.000000000000000000 ) ) ;
#9382=VECTOR ( 'NONE', #24432, 1000.000000000000000 ) ;
#9386=DIRECTION ( 'NONE',  ( 1.000000000000000000, -0.000000000000000000, -0.000000000000000000 ) ) ;
#9387=AXIS2_PLACEMENT_3D ( 'NONE', #15291, #29003, #5432 ) ;
#9388=ORIENTED_EDGE ( 'NONE', *, *, #2206, .F. ) ;
#9392=AXIS2_PLACEMENT_3D ( 'NONE', #2700, #8851, #42839 ) ;
#9393=EDGE_LOOP ( 'NONE', ( #30445, #19614, #2336, #7981 ) ) ;
#9394=CARTESIAN_POINT ( 'NONE',  ( 9.000000000000001776, 49.65209126885784485, -15.44894276735497662 ) ) ;
#9396=AXIS2_PLACEMENT_3D ( 'NONE', #7948, #24576, #27388 ) ;
#9398=FACE_OUTER_BOUND ( 'NONE', #42070, .T. ) ;
#9401=DIRECTION ( 'NONE',  ( -1.000000000000000000, -0.000000000000000000, 0.000000000000000000 ) ) ;
#9413=AXIS2_PLACEMENT_3D ( 'NONE', #29937, #42987, #13144 ) ;
#9420=VERTEX_POINT ( 'NONE', #20942 ) ;
#9422=CARTESIAN_POINT ( 'NONE',  ( 0.000000000000000000, -39.64889472655755043, 33.64468972902493960 ) ) ;
#9423=VECTOR ( 'NONE', #25514, 1000.000000000000000 ) ;
#9444=CARTESIAN_POINT ( 'NONE',  ( 0.000000000000000000, -46.19362259308839214, 8.585149169758333088 ) ) ;
#9454=AXIS2_PLACEMENT_3D ( 'NONE', #24698, #20793, #34471 ) ;
#9455=DIRECTION ( 'NONE',  ( -1.000000000000000000, 0.000000000000000000, -0.000000000000000000 ) ) ;
#9463=ORIENTED_EDGE ( 'NONE', *, *, #24225, .T. ) ;
#9466=AXIS2_PLACEMENT_3D ( 'NONE', #37047, #10443, #20510 ) ;
#9467=ORIENTED_EDGE ( 'NONE', *, *, #18776, .F. ) ;
#9486=EDGE_LOOP ( 'NONE', ( #33046, #20573 ) ) ;
#9487=CIRCLE ( 'NONE', #20677, 20.00000000000000355 ) ;
#9501=EDGE_CURVE ( 'NONE', #9086, #28134, #36821, .T. ) ;
#9504=DIRECTION ( 'NONE',  ( 0.000000000000000000, 0.000000000000000000, 1.000000000000000000 ) ) ;
#9505=ORIENTED_EDGE ( 'NONE', *, *, #4407, .F. ) ;
#9510=DIRECTION ( 'NONE',  ( -1.000000000000000000, 0.000000000000000000, 0.000000000000000000 ) ) ;
#9518=CARTESIAN_POINT ( 'NONE',  ( 0.000000000000000000, -51.19683565102450729, 9.104066087303294807 ) ) ;
#9520=VECTOR ( 'NONE', #14357, 1000.000000000000000 ) ;
#9523=LINE ( 'NONE', #9296, #22385 ) ;
#9524=ORIENTED_EDGE ( 'NONE', *, *, #34270, .F. ) ;
#9539=DIRECTION ( 'NONE',  ( -1.000000000000000000, 0.000000000000000000, 0.000000000000000000 ) ) ;
#9540=CIRCLE ( 'NONE', #2532, 20.00000000000000355 ) ;
#9541=ORIENTED_EDGE ( 'NONE', *, *, #6605, .T. ) ;
#9547=ORIENTED_EDGE ( 'NONE', *, *, #3409, .T. ) ;
#9557=CIRCLE ( 'NONE', #3231, 47.49900000000000944 ) ;
#9562=CARTESIAN_POINT ( 'NONE',  ( 18.00000000000000355, -39.64889472655706726, -33.64468972902550092 ) ) ;
#9567=AXIS2_PLACEMENT_3D ( 'NONE', #17528, #4829, #37549 ) ;
#9579=ORIENTED_EDGE ( 'NONE', *, *, #956, .T. ) ;
#9583=CARTESIAN_POINT ( 'NONE',  ( 0.000000000000000000, 29.60891106212838508, -37.14118181634735549 ) ) ;
#9587=VERTEX_POINT ( 'NONE', #31803 ) ;
#9589=DIRECTION ( 'NONE',  ( -1.000000000000000000, 0.000000000000000000, -0.000000000000000000 ) ) ;
#9591=EDGE_CURVE ( 'NONE', #17334, #17987, #37811, .T. ) ;
#9598=DIRECTION ( 'NONE',  ( -1.000000000000000000, 0.000000000000000000, 0.000000000000000000 ) ) ;
#9628=VERTEX_POINT ( 'NONE', #5393 ) ;
#9636=ORIENTED_EDGE ( 'NONE', *, *, #42670, .T. ) ;
#9649=AXIS2_PLACEMENT_3D ( 'NONE', #42799, #20171, #33432 ) ;
#9664=EDGE_CURVE ( 'NONE', #5593, #27822, #40569, .T. ) ;
#9667=CARTESIAN_POINT ( 'NONE',  ( 0.000000000000000000, -44.75336757549769118, -14.30704879393654316 ) ) ;
#9677=DIRECTION ( 'NONE',  ( -1.000000000000000000, 0.000000000000000000, 0.000000000000000000 ) ) ;
#9680=DIRECTION ( 'NONE',  ( -1.000000000000000000, -0.000000000000000000, -0.000000000000000000 ) ) ;
#9682=DIRECTION ( 'NONE',  ( 0.000000000000000000, 0.5877852522924742473, -0.8090169943749466741 ) ) ;
#9688=ORIENTED_EDGE ( 'NONE', *, *, #37907, .T. ) ;
#9692=CARTESIAN_POINT ( 'NONE',  ( 18.00000000000000355, 44.61570720899074161, 14.73072383765644133 ) ) ;
#9699=DIRECTION ( 'NONE',  ( -1.000000000000000000, -0.000000000000000000, -0.000000000000000000 ) ) ;
#9712=CYLINDRICAL_SURFACE ( 'NONE', #31119, 47.49900000000000233 ) ;
#9715=FACE_OUTER_BOUND ( 'NONE', #16897, .T. ) ;
#9717=ORIENTED_EDGE ( 'NONE', *, *, #42169, .F. ) ;
#9718=CYLINDRICAL_SURFACE ( 'NONE', #1920, 20.00000000000000355 ) ;
#9724=CARTESIAN_POINT ( 'NONE',  ( 0.000000000000000000, 18.53613841426857434, -48.58406706613883586 ) ) ;
#9734=DIRECTION ( 'NONE',  ( -1.000000000000000000, -0.000000000000000000, 0.000000000000000000 ) ) ;
#9735=VERTEX_POINT ( 'NONE', #19161 ) ;
#9738=CARTESIAN_POINT ( 'NONE',  ( 0.000000000000000000, -25.61928775981074935, 45.25098998563468911 ) ) ;
#9746=EDGE_CURVE ( 'NONE', #17173, #24522, #39604, .T. ) ;
#9747=DIRECTION ( 'NONE',  ( 1.000000000000000000, 0.000000000000000000, 0.000000000000000000 ) ) ;
#9752=VERTEX_POINT ( 'NONE', #9518 ) ;
#9762=ORIENTED_EDGE ( 'NONE', *, *, #27157, .F. ) ;
#9763=DIRECTION ( 'NONE',  ( -1.000000000000000000, 0.000000000000000000, 0.000000000000000000 ) ) ;
#9771=VERTEX_POINT ( 'NONE', #29598 ) ;
#9778=AXIS2_PLACEMENT_3D ( 'NONE', #41884, #5668, #29253 ) ;
#9781=ORIENTED_EDGE ( 'NONE', *, *, #6964, .F. ) ;
#9782=CIRCLE ( 'NONE', #9096, 47.49899999999999523 ) ;
#9785=CIRCLE ( 'NONE', #37652, 52.00000000000000000 ) ;
#9791=LINE ( 'NONE', #26812, #1821 ) ;
#9798=ORIENTED_EDGE ( 'NONE', *, *, #7125, .F. ) ;
#9799=DIRECTION ( 'NONE',  ( -1.000000000000000000, 0.000000000000000000, 0.000000000000000000 ) ) ;
#9811=DIRECTION ( 'NONE',  ( 0.000000000000000000, 0.000000000000000000, 1.000000000000000000 ) ) ;
#9815=DIRECTION ( 'NONE',  ( -1.000000000000000000, 0.000000000000000000, 0.000000000000000000 ) ) ;
#9817=ADVANCED_FACE ( 'NONE', ( #15880 ), #9294, .T. ) ;
#9818=ORIENTED_EDGE ( 'NONE', *, *, #22519, .F. ) ;
#9826=ORIENTED_EDGE ( 'NONE', *, *, #4165, .F. ) ;
#9841=VECTOR ( 'NONE', #9401, 1000.000000000000000 ) ;
#9844=FACE_OUTER_BOUND ( 'NONE', #30417, .T. ) ;
#9851=ORIENTED_EDGE ( 'NONE', *, *, #26411, .F. ) ;
#9858=ORIENTED_EDGE ( 'NONE', *, *, #33956, .T. ) ;
#9868=DIRECTION ( 'NONE',  ( -1.000000000000000000, 0.000000000000000000, 0.000000000000000000 ) ) ;
#9871=CIRCLE ( 'NONE', #41946, 47.49900000000000233 ) ;
#9872=DIRECTION ( 'NONE',  ( 1.000000000000000000, 0.000000000000000000, 0.000000000000000000 ) ) ;
#9878=ORIENTED_EDGE ( 'NONE', *, *, #31522, .T. ) ;
#9879=DIRECTION ( 'NONE',  ( 0.000000000000000000, 0.000000000000000000, 1.000000000000000000 ) ) ;
#9883=ORIENTED_EDGE ( 'NONE', *, *, #9111, .F. ) ;
#9886=EDGE_CURVE ( 'NONE', #14013, #41712, #22353, .T. ) ;
#9888=ORIENTED_EDGE ( 'NONE', *, *, #41082, .T. ) ;
#9891=DIRECTION ( 'NONE',  ( -1.000000000000000000, 0.000000000000000000, 0.000000000000000000 ) ) ;
#9895=CARTESIAN_POINT ( 'NONE',  ( 0.000000000000000000, 17.50309955389612426, 43.60271849949370448 ) ) ;
#9903=DIRECTION ( 'NONE',  ( 0.000000000000000000, 0.000000000000000000, -1.000000000000000000 ) ) ;
#9906=DIRECTION ( 'NONE',  ( 0.000000000000000000, 0.000000000000000000, 1.000000000000000000 ) ) ;
#9912=ORIENTED_EDGE ( 'NONE', *, *, #27910, .T. ) ;
#9913=LINE ( 'NONE', #30012, #11736 ) ;
#9914=CARTESIAN_POINT ( 'NONE',  ( 18.00000000000000355, 46.87740477351718482, -3.172455868805370560 ) ) ;
#9918=ADVANCED_FACE ( 'NONE', ( #36766 ), #750, .T. ) ;
#9921=CYLINDRICAL_SURFACE ( 'NONE', #24968, 47.49900000000000233 ) ;
#9923=CARTESIAN_POINT ( 'NONE',  ( 9.000000000000001776, -0.6505223195679212811, -51.99593080916758936 ) ) ;
#9940=EDGE_LOOP ( 'NONE', ( #23654, #29326, #5965, #7548 ) ) ;
#9947=CYLINDRICAL_SURFACE ( 'NONE', #18611, 20.00000000000000355 ) ;
#9955=EDGE_CURVE ( 'NONE', #4247, #22654, #13987, .T. ) ;
#9958=CARTESIAN_POINT ( 'NONE',  ( 18.00000000000000355, 17.08890430202750110, 43.76671000081951490 ) ) ;
#9960=AXIS2_PLACEMENT_3D ( 'NONE', #24392, #978, #14558 ) ;
#9975=CARTESIAN_POINT ( 'NONE',  ( -132.0000507999999968, 0.000000000000000000, 0.000000000000000000 ) ) ;
#9976=DIRECTION ( 'NONE',  ( 0.000000000000000000, 0.2486898871648482723, 0.9685831611286328524 ) ) ;
#9980=FACE_OUTER_BOUND ( 'NONE', #32179, .T. ) ;
#9983=DIRECTION ( 'NONE',  ( -1.000000000000000000, 0.000000000000000000, -0.000000000000000000 ) ) ;
#9985=CARTESIAN_POINT ( 'NONE',  ( 18.00000000000000355, -25.61928775981074580, 45.25098998563467489 ) ) ;
#9986=EDGE_CURVE ( 'NONE', #4386, #11416, #24375, .T. ) ;
#9990=EDGE_LOOP ( 'NONE', ( #16201, #10985, #41390, #31763 ) ) ;
#9998=DIRECTION ( 'NONE',  ( 0.000000000000000000, 0.000000000000000000, 1.000000000000000000 ) ) ;
#10010=EDGE_CURVE ( 'NONE', #14078, #23500, #38065, .T. ) ;
#10012=CIRCLE ( 'NONE', #34399, 47.49899999999998812 ) ;
#10040=VECTOR ( 'NONE', #35734, 1000.000000000000000 ) ;
#10044=CARTESIAN_POINT ( 'NONE',  ( 0.000000000000000000, 30.93515269692114344, 36.04401931830261674 ) ) ;
#10048=VECTOR ( 'NONE', #40481, 1000.000000000000000 ) ;
#10063=ORIENTED_EDGE ( 'NONE', *, *, #28081, .F. ) ;
#10066=ORIENTED_EDGE ( 'NONE', *, *, #14932, .T. ) ;
#10068=LINE ( 'NONE', #3502, #12476 ) ;
#10074=EDGE_LOOP ( 'NONE', ( #36005, #10953, #3575, #4072 ) ) ;
#10083=ORIENTED_EDGE ( 'NONE', *, *, #40753, .T. ) ;
#10096=ORIENTED_EDGE ( 'NONE', *, *, #20552, .F. ) ;
#10100=VECTOR ( 'NONE', #12705, 1000.000000000000000 ) ;
#10109=ADVANCED_FACE ( 'NONE', ( #41105 ), #15205, .T. ) ;
#10117=CARTESIAN_POINT ( 'NONE',  ( 9.000000000000001776, -35.11945359308136716, 38.34871548466002622 ) ) ;
#10123=CARTESIAN_POINT ( 'NONE',  ( 0.000000000000000000, -46.87740477351720614, 3.172455868805039270 ) ) ;
#10125=EDGE_CURVE ( 'NONE', #6385, #21574, #42505, .T. ) ;
#10126=ORIENTED_EDGE ( 'NONE', *, *, #4522, .F. ) ;
#10127=DIRECTION ( 'NONE',  ( 0.000000000000000000, 0.9510565162951521989, 0.3090169943749514481 ) ) ;
#10130=CARTESIAN_POINT ( 'NONE',  ( 0.000000000000000000, -39.64889472655708147, -33.64468972902550803 ) ) ;
#10140=DIRECTION ( 'NONE',  ( 1.000000000000000000, 0.000000000000000000, 0.000000000000000000 ) ) ;
#10149=ORIENTED_EDGE ( 'NONE', *, *, #31719, .F. ) ;
#10159=AXIS2_PLACEMENT_3D ( 'NONE', #29556, #13204, #42827 ) ;
#10175=ADVANCED_FACE ( 'NONE', ( #35639 ), #38921, .T. ) ;
#10190=DIRECTION ( 'NONE',  ( 0.000000000000000000, -0.9980267284282708928, -0.06279051952932446223 ) ) ;
#10197=CIRCLE ( 'NONE', #29745, 20.00000000000000711 ) ;
#10199=CARTESIAN_POINT ( 'NONE',  ( 150.0000507999999968, 0.000000000000000000, 0.000000000000000000 ) ) ;
#10213=DIRECTION ( 'NONE',  ( 1.000000000000000000, 0.000000000000000000, 0.000000000000000000 ) ) ;
#10215=DIRECTION ( 'NONE',  ( -1.000000000000000000, -0.000000000000000000, 0.000000000000000000 ) ) ;
#10218=CARTESIAN_POINT ( 'NONE',  ( 0.000000000000000000, -31.08872492059985504, 41.68322423723089543 ) ) ;
#10241=AXIS2_PLACEMENT_3D ( 'NONE', #6870, #30871, #40005 ) ;
#10253=VERTEX_POINT ( 'NONE', #35841 ) ;
#10258=ORIENTED_EDGE ( 'NONE', *, *, #38354, .F. ) ;
#10263=ORIENTED_EDGE ( 'NONE', *, *, #11020, .F. ) ;
#10268=VERTEX_POINT ( 'NONE', #15609 ) ;
#10273=ORIENTED_EDGE ( 'NONE', *, *, #20169, .T. ) ;
#10279=VERTEX_POINT ( 'NONE', #42177 ) ;
#10286=CARTESIAN_POINT ( 'NONE',  ( 0.000000000000000000, 0.000000000000000000, 0.000000000000000000 ) ) ;
#10290=EDGE_CURVE ( 'NONE', #13830, #22307, #36967, .T. ) ;
#10298=DIRECTION ( 'NONE',  ( -1.000000000000000000, 0.000000000000000000, -0.000000000000000000 ) ) ;
#10307=DIRECTION ( 'NONE',  ( 0.000000000000000000, 0.000000000000000000, 1.000000000000000000 ) ) ;
#10308=DIRECTION ( 'NONE',  ( 0.000000000000000000, 0.000000000000000000, 1.000000000000000000 ) ) ;
#10325=DIRECTION ( 'NONE',  ( 0.000000000000000000, 0.000000000000000000, -1.000000000000000000 ) ) ;
#10335=EDGE_LOOP ( 'NONE', ( #13319, #41304, #16722, #8147 ) ) ;
#10341=AXIS2_PLACEMENT_3D ( 'NONE', #18754, #37520, #38527 ) ;
#10343=DIRECTION ( 'NONE',  ( -1.000000000000000000, -0.000000000000000000, 0.000000000000000000 ) ) ;
#10344=CARTESIAN_POINT ( 'NONE',  ( 9.000000000000001776, 19.74581912682842599, 48.10512059033399623 ) ) ;
#10350=CYLINDRICAL_SURFACE ( 'NONE', #9375, 20.00000000000000711 ) ;
#10355=EDGE_CURVE ( 'NONE', #13399, #31470, #12613, .T. ) ;
#10356=DIRECTION ( 'NONE',  ( -1.000000000000000000, 0.000000000000000000, 0.000000000000000000 ) ) ;
#10359=DIRECTION ( 'NONE',  ( 0.000000000000000000, 0.000000000000000000, 1.000000000000000000 ) ) ;
#10361=VECTOR ( 'NONE', #32263, 1000.000000000000000 ) ;
#10365=DIRECTION ( 'NONE',  ( 0.000000000000000000, 0.000000000000000000, 1.000000000000000000 ) ) ;
#10378=CARTESIAN_POINT ( 'NONE',  ( 0.000000000000000000, 47.22458491092819344, 5.098390039074386593 ) ) ;
#10385=ORIENTED_EDGE ( 'NONE', *, *, #19445, .T. ) ;
#10390=AXIS2_PLACEMENT_3D ( 'NONE', #30235, #30457, #30033 ) ;
#10396=CIRCLE ( 'NONE', #13907, 51.99999999999999289 ) ;
#10397=CARTESIAN_POINT ( 'NONE',  ( 0.000000000000000000, 19.74581912682909035, -48.10512059033372623 ) ) ;
#10405=ORIENTED_EDGE ( 'NONE', *, *, #16296, .T. ) ;
#10417=CYLINDRICAL_SURFACE ( 'NONE', #22803, 47.49900000000000233 ) ;
#10421=CIRCLE ( 'NONE', #24382, 52.00000000000000000 ) ;
#10423=VERTEX_POINT ( 'NONE', #23673 ) ;
#10425=CARTESIAN_POINT ( 'NONE',  ( 18.00000000000000355, 0.000000000000000000, 0.000000000000000000 ) ) ;
#10426=ORIENTED_EDGE ( 'NONE', *, *, #39262, .F. ) ;
#10437=DIRECTION ( 'NONE',  ( -1.000000000000000000, 0.000000000000000000, -0.000000000000000000 ) ) ;
#10439=FACE_OUTER_BOUND ( 'NONE', #18848, .T. ) ;
#10443=DIRECTION ( 'NONE',  ( -1.000000000000000000, -0.000000000000000000, 0.000000000000000000 ) ) ;
#10448=DIRECTION ( 'NONE',  ( 0.000000000000000000, 0.000000000000000000, -1.000000000000000000 ) ) ;
#10449=DIRECTION ( 'NONE',  ( 0.000000000000000000, 0.2486898871648482723, 0.9685831611286327414 ) ) ;
#10452=FACE_OUTER_BOUND ( 'NONE', #37609, .T. ) ;
#10454=DIRECTION ( 'NONE',  ( -1.000000000000000000, -0.000000000000000000, 0.000000000000000000 ) ) ;
#10455=ORIENTED_EDGE ( 'NONE', *, *, #12238, .T. ) ;
#10456=DIRECTION ( 'NONE',  ( 0.000000000000000000, 0.000000000000000000, 1.000000000000000000 ) ) ;
#10459=FACE_OUTER_BOUND ( 'NONE', #31264, .T. ) ;
#10465=CARTESIAN_POINT ( 'NONE',  ( 0.000000000000000000, 0.000000000000000000, 0.000000000000000000 ) ) ;
#10467=ORIENTED_EDGE ( 'NONE', *, *, #42316, .F. ) ;
#10468=FACE_OUTER_BOUND ( 'NONE', #8934, .T. ) ;
#10479=CARTESIAN_POINT ( 'NONE',  ( 18.00000000000000355, 44.61570720899074161, 14.73072383765644133 ) ) ;
#10483=ORIENTED_EDGE ( 'NONE', *, *, #3005, .F. ) ;
#10487=CARTESIAN_POINT ( 'NONE',  ( 18.00000000000000355, 0.000000000000000000, 0.000000000000000000 ) ) ;
#10490=ORIENTED_EDGE ( 'NONE', *, *, #31955, .T. ) ;
#10495=VERTEX_POINT ( 'NONE', #37582 ) ;
#10497=DIRECTION ( 'NONE',  ( -1.000000000000000000, 0.000000000000000000, 0.000000000000000000 ) ) ;
#10504=CARTESIAN_POINT ( 'NONE',  ( 0.000000000000000000, -51.85248208264514602, -3.914090171286729980 ) ) ;
#10506=CIRCLE ( 'NONE', #34892, 20.00000000000000355 ) ;
#10514=VECTOR ( 'NONE', #32474, 1000.000000000000000 ) ;
#10532=DIRECTION ( 'NONE',  ( -1.000000000000000000, 0.000000000000000000, 0.000000000000000000 ) ) ;
#10533=VERTEX_POINT ( 'NONE', #34100 ) ;
#10535=EDGE_CURVE ( 'NONE', #19546, #4953, #33485, .T. ) ;
#10538=CARTESIAN_POINT ( 'NONE',  ( 0.000000000000000000, 0.000000000000000000, 0.000000000000000000 ) ) ;
#10540=AXIS2_PLACEMENT_3D ( 'NONE', #4403, #7482, #4631 ) ;
#10542=EDGE_CURVE ( 'NONE', #1655, #28779, #22389, .T. ) ;
#10546=ADVANCED_FACE ( 'NONE', ( #31046 ), #31690, .T. ) ;
#10547=ORIENTED_EDGE ( 'NONE', *, *, #5940, .T. ) ;
#10549=ORIENTED_EDGE ( 'NONE', *, *, #16727, .T. ) ;
#10552=DIRECTION ( 'NONE',  ( 0.000000000000000000, -0.5877852522924801315, 0.8090169943749422332 ) ) ;
#10570=CIRCLE ( 'NONE', #24532, 20.00000000000000711 ) ;
#10591=ORIENTED_EDGE ( 'NONE', *, *, #3727, .T. ) ;
#10593=EDGE_CURVE ( 'NONE', #28966, #17321, #39077, .T. ) ;
#10594=CARTESIAN_POINT ( 'NONE',  ( 0.000000000000000000, 32.32520163883631170, -34.09746168776002406 ) ) ;
#10597=ORIENTED_EDGE ( 'NONE', *, *, #26095, .T. ) ;
#10605=VERTEX_POINT ( 'NONE', #21911 ) ;
#10606=CARTESIAN_POINT ( 'NONE',  ( 18.00000000000000355, 13.85708833600031475, -45.43276465116650087 ) ) ;
#10613=ADVANCED_FACE ( 'NONE', ( #29284 ), #19060, .T. ) ;
#10620=DIRECTION ( 'NONE',  ( 0.000000000000000000, 0.000000000000000000, 1.000000000000000000 ) ) ;
#10621=ORIENTED_EDGE ( 'NONE', *, *, #37838, .T. ) ;
#10625=CARTESIAN_POINT ( 'NONE',  ( 18.00000000000000355, 0.000000000000000000, 0.000000000000000000 ) ) ;
#10629=CYLINDRICAL_SURFACE ( 'NONE', #19541, 51.99999999999999289 ) ;
#10636=CYLINDRICAL_SURFACE ( 'NONE', #15045, 47.49900000000000233 ) ;
#10641=VERTEX_POINT ( 'NONE', #41921 ) ;
#10655=CARTESIAN_POINT ( 'NONE',  ( 0.000000000000000000, 0.000000000000000000, 0.000000000000000000 ) ) ;
#10656=DIRECTION ( 'NONE',  ( -1.000000000000000000, 0.000000000000000000, 0.000000000000000000 ) ) ;
#10657=ORIENTED_EDGE ( 'NONE', *, *, #6026, .F. ) ;
#10659=CARTESIAN_POINT ( 'NONE',  ( 18.00000000000000355, -8.053585752061598768, -46.81126742072031988 ) ) ;
#10661=AXIS2_PLACEMENT_3D ( 'NONE', #23521, #6460, #36998 ) ;
#10666=EDGE_CURVE ( 'NONE', #13305, #976, #15987, .T. ) ;
#10671=EDGE_CURVE ( 'NONE', #22892, #20369, #7763, .T. ) ;
#10675=ORIENTED_EDGE ( 'NONE', *, *, #27297, .T. ) ;
#10679=CARTESIAN_POINT ( 'NONE',  ( 18.00000000000000355, -13.56094713063606427, 50.20060470671735686 ) ) ;
#10697=ORIENTED_EDGE ( 'NONE', *, *, #6214, .F. ) ;
#10703=FACE_OUTER_BOUND ( 'NONE', #3354, .T. ) ;
#10718=DIRECTION ( 'NONE',  ( 0.000000000000000000, 0.000000000000000000, 1.000000000000000000 ) ) ;
#10723=DIRECTION ( 'NONE',  ( -1.000000000000000000, 0.000000000000000000, 0.000000000000000000 ) ) ;
#10724=ORIENTED_EDGE ( 'NONE', *, *, #7014, .F. ) ;
#10731=ORIENTED_EDGE ( 'NONE', *, *, #41784, .T. ) ;
#10735=EDGE_CURVE ( 'NONE', #42150, #26382, #21163, .T. ) ;
#10737=AXIS2_PLACEMENT_3D ( 'NONE', #27905, #4081, #7368 ) ;
#10742=LINE ( 'NONE', #37345, #27830 ) ;
#10744=CIRCLE ( 'NONE', #14248, 51.99999999999999289 ) ;
#10747=VECTOR ( 'NONE', #35506, 1000.000000000000000 ) ;
#10748=DIRECTION ( 'NONE',  ( 0.000000000000000000, 0.000000000000000000, 1.000000000000000000 ) ) ;
#10758=VERTEX_POINT ( 'NONE', #20140 ) ;
#10761=EDGE_CURVE ( 'NONE', #12470, #2577, #39496, .T. ) ;
#10763=CARTESIAN_POINT ( 'NONE',  ( 0.000000000000000000, 1.347111479062088405E-15, 11.00000000000000000 ) ) ;
#10780=CIRCLE ( 'NONE', #36533, 52.00000000000000000 ) ;
#10789=ORIENTED_EDGE ( 'NONE', *, *, #20169, .F. ) ;
#10805=ORIENTED_EDGE ( 'NONE', *, *, #9664, .T. ) ;
#10814=DIRECTION ( 'NONE',  ( -1.000000000000000000, 0.000000000000000000, 0.000000000000000000 ) ) ;
#10819=CARTESIAN_POINT ( 'NONE',  ( -10.00000000000000000, 0.000000000000000000, 0.000000000000000000 ) ) ;
#10822=ORIENTED_EDGE ( 'NONE', *, *, #13850, .T. ) ;
#10823=CIRCLE ( 'NONE', #28251, 51.99999999999999289 ) ;
#10825=DIRECTION ( 'NONE',  ( -1.000000000000000000, 0.000000000000000000, 0.000000000000000000 ) ) ;
#10827=EDGE_CURVE ( 'NONE', #25440, #1479, #41192, .T. ) ;
#10831=CARTESIAN_POINT ( 'NONE',  ( 0.000000000000000000, -41.20225022064652620, 23.63323037071389265 ) ) ;
#10838=DIRECTION ( 'NONE',  ( -1.000000000000000000, 0.000000000000000000, 0.000000000000000000 ) ) ;
#10840=EDGE_LOOP ( 'NONE', ( #5014, #37198, #36272, #5738 ) ) ;
#10849=CARTESIAN_POINT ( 'NONE',  ( 18.00000000000000355, 44.61570720899096898, -14.73072383765582671 ) ) ;
#10854=AXIS2_PLACEMENT_3D ( 'NONE', #39117, #5105, #35428 ) ;
#10856=CARTESIAN_POINT ( 'NONE',  ( 18.00000000000000355, 24.47917365150009061, -45.87777302070908547 ) ) ;
#10858=CARTESIAN_POINT ( 'NONE',  ( 18.00000000000000355, 5.667686777401707232, 46.64153600743607342 ) ) ;
#10860=CARTESIAN_POINT ( 'NONE',  ( 18.00000000000000355, -6.109652351741465814, -46.58570277113515345 ) ) ;
#10861=ORIENTED_EDGE ( 'NONE', *, *, #15328, .T. ) ;
#10862=DIRECTION ( 'NONE',  ( 0.000000000000000000, 0.000000000000000000, 1.000000000000000000 ) ) ;
#10863=VERTEX_POINT ( 'NONE', #24643 ) ;
#10868=ORIENTED_EDGE ( 'NONE', *, *, #9372, .T. ) ;
#10888=AXIS2_PLACEMENT_3D ( 'NONE', #21222, #32080, #15320 ) ;
#10899=DIRECTION ( 'NONE',  ( -1.000000000000000000, 0.000000000000000000, -0.000000000000000000 ) ) ;
#10905=ORIENTED_EDGE ( 'NONE', *, *, #33578, .T. ) ;
#10925=VERTEX_POINT ( 'NONE', #22240 ) ;
#10928=AXIS2_PLACEMENT_3D ( 'NONE', #19991, #13427, #17143 ) ;
#10940=CIRCLE ( 'NONE', #36685, 20.00000000000000355 ) ;
#10950=CARTESIAN_POINT ( 'NONE',  ( 18.00000000000000355, 46.11014828289844303, -9.022736828080878624 ) ) ;
#10953=ORIENTED_EDGE ( 'NONE', *, *, #20501, .F. ) ;
#10971=CARTESIAN_POINT ( 'NONE',  ( 18.00000000000000355, 46.19362259308845609, -8.585149169757988474 ) ) ;
#10978=AXIS2_PLACEMENT_3D ( 'NONE', #7569, #1440, #577 ) ;
#10985=ORIENTED_EDGE ( 'NONE', *, *, #42963, .F. ) ;
#10987=AXIS2_PLACEMENT_3D ( 'NONE', #31453, #879, #1538 ) ;
#10999=EDGE_CURVE ( 'NONE', #20369, #8384, #7796, .T. ) ;
#11000=DIRECTION ( 'NONE',  ( 1.000000000000000000, 0.000000000000000000, 0.000000000000000000 ) ) ;
#11001=VERTEX_POINT ( 'NONE', #9738 ) ;
#11007=CARTESIAN_POINT ( 'NONE',  ( 0.000000000000000000, 35.20873326984080620, 31.88259874184042886 ) ) ;
#11010=CIRCLE ( 'NONE', #31217, 20.00000000000000711 ) ;
#11012=DIRECTION ( 'NONE',  ( 0.000000000000000000, 0.000000000000000000, 1.000000000000000000 ) ) ;
#11017=CIRCLE ( 'NONE', #25668, 20.00000000000001066 ) ;
#11020=EDGE_CURVE ( 'NONE', #33656, #12187, #16896, .T. ) ;
#11028=ORIENTED_EDGE ( 'NONE', *, *, #18345, .F. ) ;
#11031=LINE ( 'NONE', #21741, #6834 ) ;
#11034=CARTESIAN_POINT ( 'NONE',  ( 18.00000000000000355, -13.85708833599937861, -45.43276465116677798 ) ) ;
#11052=LINE ( 'NONE', #21110, #8419 ) ;
#11061=VERTEX_POINT ( 'NONE', #36126 ) ;
#11068=ORIENTED_EDGE ( 'NONE', *, *, #7347, .T. ) ;
#11071=ORIENTED_EDGE ( 'NONE', *, *, #14701, .T. ) ;
#11088=DIRECTION ( 'NONE',  ( 0.000000000000000000, 0.3681245526846719240, 0.9297764858882537897 ) ) ;
#11096=AXIS2_PLACEMENT_3D ( 'NONE', #40664, #10814, #20665 ) ;
#11097=CARTESIAN_POINT ( 'NONE',  ( 18.00000000000000355, -39.78933988720132220, 24.98727647984988920 ) ) ;
#11101=DIRECTION ( 'NONE',  ( -1.000000000000000000, 0.000000000000000000, -0.000000000000000000 ) ) ;
#11103=CYLINDRICAL_SURFACE ( 'NONE', #998, 51.99999999999999289 ) ;
#11117=ORIENTED_EDGE ( 'NONE', *, *, #12261, .F. ) ;
#11118=CARTESIAN_POINT ( 'NONE',  ( 18.00000000000000355, -32.32520163883560826, -34.09746168776070618 ) ) ;
#11131=AXIS2_PLACEMENT_3D ( 'NONE', #2389, #11843, #22531 ) ;
#11134=CYLINDRICAL_SURFACE ( 'NONE', #21288, 20.00000000000000355 ) ;
#11157=DIRECTION ( 'NONE',  ( 1.000000000000000000, -0.000000000000000000, -0.000000000000000000 ) ) ;
#11166=CARTESIAN_POINT ( 'NONE',  ( 0.000000000000000000, 0.000000000000000000, 0.000000000000000000 ) ) ;
#11169=CARTESIAN_POINT ( 'NONE',  ( 18.00000000000000355, 47.49120266317495265, -0.8606222198177008176 ) ) ;
#11173=ORIENTED_EDGE ( 'NONE', *, *, #3008, .F. ) ;
#11174=ADVANCED_FACE ( 'NONE', ( #9300 ), #2732, .T. ) ;
#11179=EDGE_CURVE ( 'NONE', #39905, #10925, #39819, .T. ) ;
#11181=VECTOR ( 'NONE', #31103, 1000.000000000000000 ) ;
#11187=CARTESIAN_POINT ( 'NONE',  ( 9.000000000000001776, 39.64889472655780622, -33.64468972902464117 ) ) ;
#11194=EDGE_CURVE ( 'NONE', #27822, #23124, #7097, .T. ) ;
#11197=DIRECTION ( 'NONE',  ( 0.000000000000000000, 0.9510565162951544194, -0.3090169943749447867 ) ) ;
#11198=ORIENTED_EDGE ( 'NONE', *, *, #38098, .F. ) ;
#11200=ORIENTED_EDGE ( 'NONE', *, *, #35960, .T. ) ;
#11207=EDGE_CURVE ( 'NONE', #42728, #19539, #33504, .T. ) ;
#11213=VERTEX_POINT ( 'NONE', #40672 ) ;
#11223=CARTESIAN_POINT ( 'NONE',  ( 0.000000000000000000, 22.43957647427161461, 41.27978878573636479 ) ) ;
#11232=CARTESIAN_POINT ( 'NONE',  ( 0.000000000000000000, -5.667686777402029641, 46.64153600743603789 ) ) ;
#11233=CARTESIAN_POINT ( 'NONE',  ( 9.000000000000001776, -18.53613841426756181, -48.58406706613921244 ) ) ;
#11238=CARTESIAN_POINT ( 'NONE',  ( 18.00000000000000355, 20.99948489194423118, 42.60488980472788967 ) ) ;
#11241=AXIS2_PLACEMENT_3D ( 'NONE', #4690, #21553, #25664 ) ;
#11250=DIRECTION ( 'NONE',  ( -1.000000000000000000, -0.000000000000000000, 0.000000000000000000 ) ) ;
#11252=CIRCLE ( 'NONE', #6333, 20.00000000000000000 ) ;
#11262=DIRECTION ( 'NONE',  ( 0.000000000000000000, 0.000000000000000000, 1.000000000000000000 ) ) ;
#11269=AXIS2_PLACEMENT_3D ( 'NONE', #31279, #11000, #21064 ) ;
#11270=CARTESIAN_POINT ( 'NONE',  ( 18.00000000000000355, -26.17370628620627571, -39.63700417846190049 ) ) ;
#11275=EDGE_LOOP ( 'NONE', ( #20618, #36972, #29612, #29825 ) ) ;
#11276=ADVANCED_FACE ( 'NONE', ( #16752 ), #17402, .T. ) ;
#11280=ORIENTED_EDGE ( 'NONE', *, *, #4813, .F. ) ;
#11285=CARTESIAN_POINT ( 'NONE',  ( 18.00000000000000355, -39.55064067543046491, -25.36340625197400200 ) ) ;
#11289=ORIENTED_EDGE ( 'NONE', *, *, #7650, .T. ) ;
#11300=CARTESIAN_POINT ( 'NONE',  ( 0.000000000000000000, -9.744342220503709129, 46.48873837489794880 ) ) ;
#11306=AXIS2_PLACEMENT_3D ( 'NONE', #25331, #4563, #27951 ) ;
#11307=DIRECTION ( 'NONE',  ( -1.000000000000000000, 0.000000000000000000, 0.000000000000000000 ) ) ;
#11312=EDGE_LOOP ( 'NONE', ( #32532, #26103, #40500, #38457 ) ) ;
#11326=ORIENTED_EDGE ( 'NONE', *, *, #605, .F. ) ;
#11343=CARTESIAN_POINT ( 'NONE',  ( 18.00000000000000355, 0.000000000000000000, 0.000000000000000000 ) ) ;
#11347=DIRECTION ( 'NONE',  ( 0.000000000000000000, 0.000000000000000000, 1.000000000000000000 ) ) ;
#11351=DIRECTION ( 'NONE',  ( 1.000000000000000000, -0.000000000000000000, -0.000000000000000000 ) ) ;
#11358=AXIS2_PLACEMENT_3D ( 'NONE', #42891, #9747, #35498 ) ;
#11369=VERTEX_POINT ( 'NONE', #26466 ) ;
#11372=DIRECTION ( 'NONE',  ( 0.000000000000000000, -0.3681245526846852467, 0.9297764858882484607 ) ) ;
#11376=ORIENTED_EDGE ( 'NONE', *, *, #26800, .F. ) ;
#11386=ORIENTED_EDGE ( 'NONE', *, *, #40336, .F. ) ;
#11393=DIRECTION ( 'NONE',  ( 0.000000000000000000, 0.000000000000000000, 1.000000000000000000 ) ) ;
#11400=VERTEX_POINT ( 'NONE', #5944 ) ;
#11404=ORIENTED_EDGE ( 'NONE', *, *, #19494, .F. ) ;
#11405=ADVANCED_FACE ( 'NONE', ( #16229 ), #6583, .T. ) ;
#11407=DIRECTION ( 'NONE',  ( -1.000000000000000000, 0.000000000000000000, -0.000000000000000000 ) ) ;
#11410=EDGE_LOOP ( 'NONE', ( #33382, #2971, #21700, #29176 ) ) ;
#11412=CARTESIAN_POINT ( 'NONE',  ( 18.00000000000000355, 19.44205635905601781, -43.33776004284589334 ) ) ;
#11416=VERTEX_POINT ( 'NONE', #14 ) ;
#11419=EDGE_CURVE ( 'NONE', #24522, #37184, #18314, .T. ) ;
#11435=CIRCLE ( 'NONE', #12830, 20.00000000000000711 ) ;
#11445=EDGE_LOOP ( 'NONE', ( #16588, #23974, #42539, #14232 ) ) ;
#11448=ADVANCED_FACE ( 'NONE', ( #37769 ), #463, .T. ) ;
#11449=CARTESIAN_POINT ( 'NONE',  ( 18.00000000000000355, 41.20225022064636278, 23.63323037071415911 ) ) ;
#11452=AXIS2_PLACEMENT_3D ( 'NONE', #7837, #41856, #11347 ) ;
#11470=DIRECTION ( 'NONE',  ( -1.000000000000000000, 0.000000000000000000, 0.000000000000000000 ) ) ;
#11477=EDGE_CURVE ( 'NONE', #31641, #18421, #27336, .T. ) ;
#11479=DIRECTION ( 'NONE',  ( -1.000000000000000000, 0.000000000000000000, 0.000000000000000000 ) ) ;
#11481=CIRCLE ( 'NONE', #7968, 20.00000000000000000 ) ;
#11491=ADVANCED_FACE ( 'NONE', ( #37341 ), #4168, .T. ) ;
#11493=CARTESIAN_POINT ( 'NONE',  ( 0.000000000000000000, 46.87740477351718482, -3.172455868805370560 ) ) ;
#11504=ORIENTED_EDGE ( 'NONE', *, *, #12937, .T. ) ;
#11507=CARTESIAN_POINT ( 'NONE',  ( 18.00000000000000355, -47.22458491092815791, -5.098390039074710778 ) ) ;
#11511=CYLINDRICAL_SURFACE ( 'NONE', #32526, 51.99999999999999289 ) ;
#11515=CARTESIAN_POINT ( 'NONE',  ( 0.000000000000000000, 11.46872990052381880, 45.56340405422447049 ) ) ;
#11519=ORIENTED_EDGE ( 'NONE', *, *, #4813, .T. ) ;
#11520=DIRECTION ( 'NONE',  ( 0.000000000000000000, 0.000000000000000000, 1.000000000000000000 ) ) ;
#11537=ORIENTED_EDGE ( 'NONE', *, *, #28780, .T. ) ;
#11548=CIRCLE ( 'NONE', #24810, 47.49900000000000233 ) ;
#11552=ORIENTED_EDGE ( 'NONE', *, *, #25694, .T. ) ;
#11555=ORIENTED_EDGE ( 'NONE', *, *, #34321, .T. ) ;
#11579=CARTESIAN_POINT ( 'NONE',  ( 18.00000000000000355, -44.47301969247456555, 16.68249143361894582 ) ) ;
#11580=VERTEX_POINT ( 'NONE', #14467 ) ;
#11584=DIRECTION ( 'NONE',  ( 1.000000000000000000, 0.000000000000000000, 0.000000000000000000 ) ) ;
#11590=EDGE_CURVE ( 'NONE', #41981, #7783, #3717, .T. ) ;
#11593=EDGE_LOOP ( 'NONE', ( #1773, #18094, #18896, #5340 ) ) ;
#11595=EDGE_CURVE ( 'NONE', #39961, #39644, #16888, .T. ) ;
#11601=DIRECTION ( 'NONE',  ( -1.000000000000000000, 0.000000000000000000, 0.000000000000000000 ) ) ;
#11607=EDGE_LOOP ( 'NONE', ( #42248, #784 ) ) ;
#11617=EDGE_CURVE ( 'NONE', #10758, #976, #23865, .T. ) ;
#11627=CYLINDRICAL_SURFACE ( 'NONE', #38196, 47.49900000000000233 ) ;
#11636=ORIENTED_EDGE ( 'NONE', *, *, #16623, .F. ) ;
#11637=CARTESIAN_POINT ( 'NONE',  ( 18.00000000000000355, -3.840921266750155993, 47.34345070675168188 ) ) ;
#11642=CARTESIAN_POINT ( 'NONE',  ( 18.00000000000000355, 0.000000000000000000, 0.000000000000000000 ) ) ;
#11643=ORIENTED_EDGE ( 'NONE', *, *, #38408, .F. ) ;
#11657=EDGE_LOOP ( 'NONE', ( #21549, #10490, #26552, #13838 ) ) ;
#11666=VECTOR ( 'NONE', #12253, 1000.000000000000000 ) ;
#11668=CIRCLE ( 'NONE', #15842, 20.00000000000001066 ) ;
#11670=VERTEX_POINT ( 'NONE', #41698 ) ;
#11673=EDGE_CURVE ( 'NONE', #30654, #17334, #38415, .T. ) ;
#11674=CYLINDRICAL_SURFACE ( 'NONE', #1800, 47.49900000000000233 ) ;
#11675=CIRCLE ( 'NONE', #22162, 47.49900000000000233 ) ;
#11683=CARTESIAN_POINT ( 'NONE',  ( 18.00000000000000355, 42.60732521687572927, 19.80331771201673519 ) ) ;
#11686=LINE ( 'NONE', #30872, #20092 ) ;
#11693=CARTESIAN_POINT ( 'NONE',  ( 18.00000000000000355, -47.22458491092815791, -5.098390039074710778 ) ) ;
#11698=AXIS2_PLACEMENT_3D ( 'NONE', #12792, #26106, #13660 ) ;
#11699=AXIS2_PLACEMENT_3D ( 'NONE', #37766, #3944, #11393 ) ;
#11711=CIRCLE ( 'NONE', #13796, 20.00000000000000711 ) ;
#11736=VECTOR ( 'NONE', #42631, 1000.000000000000000 ) ;
#11739=CARTESIAN_POINT ( 'NONE',  ( 18.00000000000000355, 0.000000000000000000, 0.000000000000000000 ) ) ;
#11742=VECTOR ( 'NONE', #14523, 1000.000000000000000 ) ;
#11743=DIRECTION ( 'NONE',  ( 0.000000000000000000, 0.000000000000000000, 1.000000000000000000 ) ) ;
#11746=CARTESIAN_POINT ( 'NONE',  ( 18.00000000000000355, -17.50309955389580452, -43.60271849949383949 ) ) ;
#11756=AXIS2_PLACEMENT_3D ( 'NONE', #2890, #6406, #43054 ) ;
#11767=DIRECTION ( 'NONE',  ( -1.000000000000000000, 0.000000000000000000, 0.000000000000000000 ) ) ;
#11771=VECTOR ( 'NONE', #13075, 1000.000000000000000 ) ;
#11779=ORIENTED_EDGE ( 'NONE', *, *, #16441, .F. ) ;
#11785=ADVANCED_FACE ( 'NONE', ( #13279 ), #35514, .T. ) ;
#11788=FACE_OUTER_BOUND ( 'NONE', #25133, .T. ) ;
#11792=AXIS2_PLACEMENT_3D ( 'NONE', #38323, #35050, #42648 ) ;
#11797=AXIS2_PLACEMENT_3D ( 'NONE', #11683, #24572, #11894 ) ;
#11798=EDGE_CURVE ( 'NONE', #31610, #10863, #25970, .T. ) ;
#11801=CARTESIAN_POINT ( 'NONE',  ( 18.00000000000000355, -19.44205635905570873, 43.33776004284602124 ) ) ;
#11804=DIRECTION ( 'NONE',  ( -1.000000000000000000, -0.000000000000000000, 0.000000000000000000 ) ) ;
#11833=EDGE_CURVE ( 'NONE', #24221, #3449, #23036, .T. ) ;
#11842=ORIENTED_EDGE ( 'NONE', *, *, #36697, .T. ) ;
#11843=DIRECTION ( 'NONE',  ( -1.000000000000000000, 0.000000000000000000, -0.000000000000000000 ) ) ;
#11847=ADVANCED_FACE ( 'NONE', ( #40492 ), #10629, .T. ) ;
#11848=CIRCLE ( 'NONE', #26435, 47.49900000000000233 ) ;
#11851=EDGE_CURVE ( 'NONE', #30436, #12372, #27189, .T. ) ;
#11870=DIRECTION ( 'NONE',  ( -1.000000000000000000, -0.000000000000000000, -0.000000000000000000 ) ) ;
#11871=CARTESIAN_POINT ( 'NONE',  ( 18.00000000000000355, -39.78933988720098114, -24.98727647985043276 ) ) ;
#11875=AXIS2_PLACEMENT_3D ( 'NONE', #41817, #8014, #21811 ) ;
#11878=CIRCLE ( 'NONE', #23717, 47.49900000000000233 ) ;
#11883=ORIENTED_EDGE ( 'NONE', *, *, #20974, .F. ) ;
#11894=DIRECTION ( 'NONE',  ( 0.000000000000000000, 0.7705132427757903635, -0.6374239897486881912 ) ) ;
#11897=EDGE_CURVE ( 'NONE', #15350, #23668, #11878, .T. ) ;
#11899=DIRECTION ( 'NONE',  ( -1.000000000000000000, 0.000000000000000000, 0.000000000000000000 ) ) ;
#11905=CIRCLE ( 'NONE', #11875, 52.00000000000000000 ) ;
#11913=DIRECTION ( 'NONE',  ( -1.000000000000000000, -0.000000000000000000, -0.000000000000000000 ) ) ;
#11919=EDGE_CURVE ( 'NONE', #39753, #34203, #28603, .T. ) ;
#11921=DIRECTION ( 'NONE',  ( -1.000000000000000000, 0.000000000000000000, -0.000000000000000000 ) ) ;
#11933=CARTESIAN_POINT ( 'NONE',  ( 18.00000000000000355, 29.60891106212838508, -37.14118181634735549 ) ) ;
#11938=VERTEX_POINT ( 'NONE', #37227 ) ;
#11945=ADVANCED_FACE ( 'NONE', ( #33532 ), #4056, .T. ) ;
#11947=FACE_OUTER_BOUND ( 'NONE', #11445, .T. ) ;
#11956=ORIENTED_EDGE ( 'NONE', *, *, #34742, .T. ) ;
#11960=ORIENTED_EDGE ( 'NONE', *, *, #8473, .T. ) ;
#11979=CIRCLE ( 'NONE', #19638, 20.00000000000000711 ) ;
#11980=DIRECTION ( 'NONE',  ( -1.000000000000000000, 0.000000000000000000, -0.000000000000000000 ) ) ;
#11985=CIRCLE ( 'NONE', #41898, 47.49900000000001654 ) ;
#11989=ORIENTED_EDGE ( 'NONE', *, *, #34297, .T. ) ;
#11998=AXIS2_PLACEMENT_3D ( 'NONE', #15563, #5709, #19489 ) ;
#12003=CIRCLE ( 'NONE', #8483, 47.49899999999999523 ) ;
#12014=DIRECTION ( 'NONE',  ( -1.000000000000000000, 0.000000000000000000, 0.000000000000000000 ) ) ;
#12020=ORIENTED_EDGE ( 'NONE', *, *, #6752, .F. ) ;
#12025=ADVANCED_FACE ( 'NONE', ( #1653 ), #31996, .T. ) ;
#12028=LINE ( 'NONE', #35964, #34907 ) ;
#12032=VECTOR ( 'NONE', #14439, 1000.000000000000000 ) ;
#12035=ORIENTED_EDGE ( 'NONE', *, *, #10290, .F. ) ;
#12036=DIRECTION ( 'NONE',  ( -1.000000000000000000, -0.000000000000000000, 0.000000000000000000 ) ) ;
#12037=AXIS2_PLACEMENT_3D ( 'NONE', #41655, #11804, #38377 ) ;
#12047=ORIENTED_EDGE ( 'NONE', *, *, #38337, .F. ) ;
#12056=CARTESIAN_POINT ( 'NONE',  ( 0.000000000000000000, -19.44205635905511897, -43.33776004284629124 ) ) ;
#12059=DIRECTION ( 'NONE',  ( -1.000000000000000000, -0.000000000000000000, 0.000000000000000000 ) ) ;
#12060=CIRCLE ( 'NONE', #26678, 52.00000000000000000 ) ;
#12062=DIRECTION ( 'NONE',  ( 1.000000000000000000, 0.000000000000000000, 0.000000000000000000 ) ) ;
#12069=DIRECTION ( 'NONE',  ( -1.000000000000000000, -0.000000000000000000, -0.000000000000000000 ) ) ;
#12071=FACE_OUTER_BOUND ( 'NONE', #41911, .T. ) ;
#12073=VERTEX_POINT ( 'NONE', #8429 ) ;
#12087=EDGE_CURVE ( 'NONE', #20302, #30905, #41072, .T. ) ;
#12091=ADVANCED_FACE ( 'NONE', ( #9715 ), #28736, .T. ) ;
#12096=CARTESIAN_POINT ( 'NONE',  ( 18.00000000000000355, 39.64889472655779201, -33.64468972902464117 ) ) ;
#12099=DIRECTION ( 'NONE',  ( -1.000000000000000000, -0.000000000000000000, -0.000000000000000000 ) ) ;
#12109=DIRECTION ( 'NONE',  ( -1.000000000000000000, 0.000000000000000000, 0.000000000000000000 ) ) ;
#12111=CYLINDRICAL_SURFACE ( 'NONE', #33137, 20.00000000000000355 ) ;
#12113=ORIENTED_EDGE ( 'NONE', *, *, #11919, .F. ) ;
#12117=CARTESIAN_POINT ( 'NONE',  ( 18.00000000000000355, -51.93417535146739539, -2.615612846549722370 ) ) ;
#12129=EDGE_LOOP ( 'NONE', ( #12438, #41077, #7244, #18555 ) ) ;
#12132=ORIENTED_EDGE ( 'NONE', *, *, #891, .T. ) ;
#12134=FILL_AREA_STYLE ('',( #35858 ) ) ;
#12146=FACE_OUTER_BOUND ( 'NONE', #36646, .T. ) ;
#12154=VERTEX_POINT ( 'NONE', #42432 ) ;
#12157=CARTESIAN_POINT ( 'NONE',  ( 18.00000000000000355, -47.32430374665916162, -21.55018039121577189 ) ) ;
#12159=CYLINDRICAL_SURFACE ( 'NONE', #8189, 47.49900000000000233 ) ;
#12183=FACE_OUTER_BOUND ( 'NONE', #28295, .T. ) ;
#12187=VERTEX_POINT ( 'NONE', #12576 ) ;
#12190=CARTESIAN_POINT ( 'NONE',  ( 9.000000000000001776, -25.61928775981013118, -45.25098998563503727 ) ) ;
#12203=AXIS2_PLACEMENT_3D ( 'NONE', #33732, #13916, #3608 ) ;
#12206=CYLINDRICAL_SURFACE ( 'NONE', #16504, 51.99999999999999289 ) ;
#12209=DIRECTION ( 'NONE',  ( -1.000000000000000000, -0.000000000000000000, -0.000000000000000000 ) ) ;
#12216=CARTESIAN_POINT ( 'NONE',  ( 18.00000000000000355, 0.000000000000000000, 0.000000000000000000 ) ) ;
#12222=DIRECTION ( 'NONE',  ( 0.000000000000000000, 0.1253332335642974860, 0.9921147013144787641 ) ) ;
#12223=VERTEX_POINT ( 'NONE', #26951 ) ;
#12226=CARTESIAN_POINT ( 'NONE',  ( 18.00000000000000355, -46.90537658765328644, -2.727856614654796452 ) ) ;
#12231=DIRECTION ( 'NONE',  ( -1.000000000000000000, -0.000000000000000000, 0.000000000000000000 ) ) ;
#12233=ORIENTED_EDGE ( 'NONE', *, *, #24530, .T. ) ;
#12237=CYLINDRICAL_SURFACE ( 'NONE', #30814, 47.49900000000000233 ) ;
#12238=EDGE_CURVE ( 'NONE', #30905, #22661, #5871, .T. ) ;
#12251=VECTOR ( 'NONE', #3691, 1000.000000000000000 ) ;
#12253=DIRECTION ( 'NONE',  ( 1.000000000000000000, -0.000000000000000000, -0.000000000000000000 ) ) ;
#12257=EDGE_CURVE ( 'NONE', #1606, #36282, #5163, .T. ) ;
#12261=EDGE_CURVE ( 'NONE', #255, #1619, #11481, .T. ) ;
#12265=ORIENTED_EDGE ( 'NONE', *, *, #18558, .T. ) ;
#12278=VERTEX_POINT ( 'NONE', #16937 ) ;
#12285=FACE_OUTER_BOUND ( 'NONE', #5554, .T. ) ;
#12295=CARTESIAN_POINT ( 'NONE',  ( -10.00000000000000000, 0.000000000000000000, 0.000000000000000000 ) ) ;
#12296=ORIENTED_EDGE ( 'NONE', *, *, #10535, .F. ) ;
#12306=VERTEX_POINT ( 'NONE', #10130 ) ;
#12307=CYLINDRICAL_SURFACE ( 'NONE', #28372, 51.99999999999999289 ) ;
#12312=DIRECTION ( 'NONE',  ( -1.000000000000000000, 0.000000000000000000, 0.000000000000000000 ) ) ;
#12313=AXIS2_PLACEMENT_3D ( 'NONE', #18433, #41724, #28862 ) ;
#12317=EDGE_LOOP ( 'NONE', ( #2195, #33837, #12431, #5338 ) ) ;
#12321=CARTESIAN_POINT ( 'NONE',  ( 18.00000000000000355, -8.053585752062225822, 46.81126742072019908 ) ) ;
#12325=DIRECTION ( 'NONE',  ( 0.000000000000000000, 0.3681245526846720906, 0.9297764858882537897 ) ) ;
#12326=DIRECTION ( 'NONE',  ( -1.000000000000000000, 0.000000000000000000, -0.000000000000000000 ) ) ;
#12344=VECTOR ( 'NONE', #14584, 1000.000000000000000 ) ;
#12345=DIRECTION ( 'NONE',  ( -1.000000000000000000, 0.000000000000000000, 0.000000000000000000 ) ) ;
#12352=( LENGTH_UNIT ( ) NAMED_UNIT ( * ) SI_UNIT ( .MILLI., .METRE. ) );
#12354=CIRCLE ( 'NONE', #37389, 20.00000000000000711 ) ;
#12359=CARTESIAN_POINT ( 'NONE',  ( 18.00000000000000355, 39.64889472655730884, 33.64468972902522381 ) ) ;
#12362=ORIENTED_EDGE ( 'NONE', *, *, #10999, .F. ) ;
#12365=EDGE_LOOP ( 'NONE', ( #20839, #36710, #27320, #35731 ) ) ;
#12366=CARTESIAN_POINT ( 'NONE',  ( 18.00000000000000355, -40.47821179127690527, -32.64221760512803172 ) ) ;
#12372=VERTEX_POINT ( 'NONE', #30657 ) ;
#12375=DIRECTION ( 'NONE',  ( -1.000000000000000000, -0.000000000000000000, -0.000000000000000000 ) ) ;
#12376=AXIS2_PLACEMENT_3D ( 'NONE', #14961, #27612, #28051 ) ;
#12377=DIRECTION ( 'NONE',  ( 0.000000000000000000, -0.7705132427757815927, -0.6374239897486989603 ) ) ;
#12387=CIRCLE ( 'NONE', #16568, 51.99999999999999289 ) ;
#12402=ORIENTED_EDGE ( 'NONE', *, *, #8793, .T. ) ;
#12407=DIRECTION ( 'NONE',  ( -1.000000000000000000, 0.000000000000000000, 0.000000000000000000 ) ) ;
#12412=DIRECTION ( 'NONE',  ( -1.000000000000000000, 0.000000000000000000, 0.000000000000000000 ) ) ;
#12416=DIRECTION ( 'NONE',  ( 0.000000000000000000, 0.9822872507286891652, -0.1873813145857216034 ) ) ;
#12418=CIRCLE ( 'NONE', #23576, 51.99999999999999289 ) ;
#12431=ORIENTED_EDGE ( 'NONE', *, *, #20256, .T. ) ;
#12437=CARTESIAN_POINT ( 'NONE',  ( 0.000000000000000000, 43.83938735307268075, 18.28286404005813637 ) ) ;
#12438=ORIENTED_EDGE ( 'NONE', *, *, #712, .T. ) ;
#12447=DIRECTION ( 'NONE',  ( -1.000000000000000000, 0.000000000000000000, 0.000000000000000000 ) ) ;
#12451=CARTESIAN_POINT ( 'NONE',  ( 18.00000000000000355, 17.08890430202750110, 43.76671000081951490 ) ) ;
#12458=DIRECTION ( 'NONE',  ( -1.000000000000000000, -0.000000000000000000, -0.000000000000000000 ) ) ;
#12459=EDGE_CURVE ( 'NONE', #4386, #8463, #10744, .T. ) ;
#12466=CARTESIAN_POINT ( 'NONE',  ( 0.000000000000000000, 0.000000000000000000, 0.000000000000000000 ) ) ;
#12468=ORIENTED_EDGE ( 'NONE', *, *, #36826, .F. ) ;
#12470=VERTEX_POINT ( 'NONE', #8581 ) ;
#12471=CIRCLE ( 'NONE', #18768, 20.00000000000000711 ) ;
#12476=VECTOR ( 'NONE', #7220, 1000.000000000000000 ) ;
#12483=CARTESIAN_POINT ( 'NONE',  ( 18.00000000000000355, 44.61570720899096898, -14.73072383765582671 ) ) ;
#12489=ORIENTED_EDGE ( 'NONE', *, *, #27734, .T. ) ;
#12493=ORIENTED_EDGE ( 'NONE', *, *, #12608, .T. ) ;
#12500=CYLINDRICAL_SURFACE ( 'NONE', #37710, 47.49900000000000233 ) ;
#12504=DIRECTION ( 'NONE',  ( 0.000000000000000000, 0.000000000000000000, 1.000000000000000000 ) ) ;
#12506=EDGE_CURVE ( 'NONE', #37859, #15611, #37950, .T. ) ;
#12508=DIRECTION ( 'NONE',  ( -1.000000000000000000, 0.000000000000000000, 0.000000000000000000 ) ) ;
#12531=CARTESIAN_POINT ( 'NONE',  ( 18.00000000000000355, -9.744342220503087404, -46.48873837489808380 ) ) ;
#12536=DIRECTION ( 'NONE',  ( -1.000000000000000000, -0.000000000000000000, -0.000000000000000000 ) ) ;
#12543=ORIENTED_EDGE ( 'NONE', *, *, #29791, .T. ) ;
#12564=DIRECTION ( 'NONE',  ( -1.000000000000000000, 0.000000000000000000, -0.000000000000000000 ) ) ;
#12576=CARTESIAN_POINT ( 'NONE',  ( 0.000000000000000000, 13.56094713063641599, -50.20060470671725739 ) ) ;
#12580=CIRCLE ( 'NONE', #22350, 52.00000000000000000 ) ;
#12582=AXIS2_PLACEMENT_3D ( 'NONE', #1190, #11913, #8398 ) ;
#12584=DIRECTION ( 'NONE',  ( -1.000000000000000000, -0.000000000000000000, 0.000000000000000000 ) ) ;
#12608=EDGE_CURVE ( 'NONE', #42167, #24321, #9360, .T. ) ;
#12613=CIRCLE ( 'NONE', #18225, 11.00000000000000000 ) ;
#12622=EDGE_CURVE ( 'NONE', #34783, #1751, #8802, .T. ) ;
#12636=DIRECTION ( 'NONE',  ( -1.000000000000000000, -0.000000000000000000, -0.000000000000000000 ) ) ;
#12640=CARTESIAN_POINT ( 'NONE',  ( 0.000000000000000000, -41.20225022064620646, -23.63323037071445043 ) ) ;
#12646=CARTESIAN_POINT ( 'NONE',  ( -10.00000000000000000, 0.000000000000000000, 0.000000000000000000 ) ) ;
#12654=FACE_OUTER_BOUND ( 'NONE', #12719, .T. ) ;
#12667=EDGE_CURVE ( 'NONE', #22227, #36282, #10780, .T. ) ;
#12679=CARTESIAN_POINT ( 'NONE',  ( -10.00000000000000000, 0.000000000000000000, 0.000000000000000000 ) ) ;
#12691=CARTESIAN_POINT ( 'NONE',  ( 0.000000000000000000, 46.90537658765331486, 2.727856614654470491 ) ) ;
#12701=ORIENTED_EDGE ( 'NONE', *, *, #12937, .F. ) ;
#12702=CARTESIAN_POINT ( 'NONE',  ( 9.000000000000001776, -51.93417535146742381, 2.615612846549007831 ) ) ;
#12705=DIRECTION ( 'NONE',  ( 1.000000000000000000, -0.000000000000000000, -0.000000000000000000 ) ) ;
#12707=CYLINDRICAL_SURFACE ( 'NONE', #11998, 20.00000000000000711 ) ;
#12719=EDGE_LOOP ( 'NONE', ( #18036, #36578, #4476, #21310 ) ) ;
#12721=EDGE_CURVE ( 'NONE', #21131, #4060, #6374, .T. ) ;
#12729=ORIENTED_EDGE ( 'NONE', *, *, #15991, .F. ) ;
#12731=CARTESIAN_POINT ( 'NONE',  ( 0.000000000000000000, 0.000000000000000000, 0.000000000000000000 ) ) ;
#12738=ORIENTED_EDGE ( 'NONE', *, *, #12799, .F. ) ;
#12742=EDGE_CURVE ( 'NONE', #40198, #14608, #16364, .T. ) ;
#12759=FACE_OUTER_BOUND ( 'NONE', #12365, .T. ) ;
#12772=CIRCLE ( 'NONE', #9261, 51.99999999999999289 ) ;
#12774=CARTESIAN_POINT ( 'NONE',  ( 18.00000000000000355, -0.6505223195686603566, 51.99593080916757515 ) ) ;
#12779=DIRECTION ( 'NONE',  ( -1.000000000000000000, -0.000000000000000000, 0.000000000000000000 ) ) ;
#12780=EDGE_LOOP ( 'NONE', ( #23191, #30773, #4738, #39717 ) ) ;
#12792=CARTESIAN_POINT ( 'NONE',  ( 0.000000000000000000, 32.00046193115148441, 34.40241257139697950 ) ) ;
#12795=CARTESIAN_POINT ( 'NONE',  ( 0.000000000000000000, -39.78933988720132220, 24.98727647984988920 ) ) ;
#12799=EDGE_CURVE ( 'NONE', #6443, #22892, #3758, .T. ) ;
#12813=EDGE_CURVE ( 'NONE', #31610, #26339, #25447, .T. ) ;
#12821=VECTOR ( 'NONE', #37288, 1000.000000000000000 ) ;
#12822=PLANE ( 'NONE',  #11358 ) ;
#12828=LINE ( 'NONE', #42473, #41406 ) ;
#12830=AXIS2_PLACEMENT_3D ( 'NONE', #6416, #7659, #23470 ) ;
#12832=ORIENTED_EDGE ( 'NONE', *, *, #20695, .F. ) ;
#12845=ADVANCED_FACE ( 'NONE', ( #4330 ), #11134, .T. ) ;
#12847=CARTESIAN_POINT ( 'NONE',  ( 9.000000000000001776, -50.95304419620816816, -10.38206564895716255 ) ) ;
#12858=EDGE_CURVE ( 'NONE', #6740, #7094, #35882, .T. ) ;
#12864=CARTESIAN_POINT ( 'NONE',  ( -10.00000000000000000, 0.000000000000000000, 0.000000000000000000 ) ) ;
#12865=DIRECTION ( 'NONE',  ( -1.000000000000000000, 0.000000000000000000, 0.000000000000000000 ) ) ;
#12876=ORIENTED_EDGE ( 'NONE', *, *, #35849, .T. ) ;
#12882=ADVANCED_FACE ( 'NONE', ( #5206 ), #15065, .T. ) ;
#12888=CIRCLE ( 'NONE', #6598, 20.00000000000000355 ) ;
#12889=DIRECTION ( 'NONE',  ( -1.000000000000000000, -0.000000000000000000, 0.000000000000000000 ) ) ;
#12890=CARTESIAN_POINT ( 'NONE',  ( 0.000000000000000000, -9.744342220503083851, -46.48873837489806959 ) ) ;
#12901=AXIS2_PLACEMENT_3D ( 'NONE', #26577, #19416, #36581 ) ;
#12902=ORIENTED_EDGE ( 'NONE', *, *, #42000, .T. ) ;
#12904=CARTESIAN_POINT ( 'NONE',  ( 0.000000000000000000, 11.46872990052444408, -45.56340405422433548 ) ) ;
#12908=FACE_OUTER_BOUND ( 'NONE', #40572, .T. ) ;
#12910=EDGE_CURVE ( 'NONE', #17463, #24263, #30339, .T. ) ;
#12915=ORIENTED_EDGE ( 'NONE', *, *, #1711, .F. ) ;
#12920=DIRECTION ( 'NONE',  ( -1.000000000000000000, 0.000000000000000000, -0.000000000000000000 ) ) ;
#12937=EDGE_CURVE ( 'NONE', #19812, #5593, #24070, .T. ) ;
#12944=CIRCLE ( 'NONE', #29670, 51.99999999999999289 ) ;
#12947=CARTESIAN_POINT ( 'NONE',  ( 0.000000000000000000, 13.85708833599968770, 45.43276465116669982 ) ) ;
#12951=ADVANCED_FACE ( 'NONE', ( #41643 ), #8482, .T. ) ;
#12961=VERTEX_POINT ( 'NONE', #15496 ) ;
#12964=ORIENTED_EDGE ( 'NONE', *, *, #30286, .T. ) ;
#12967=AXIS2_PLACEMENT_3D ( 'NONE', #10625, #30705, #20266 ) ;
#12977=CARTESIAN_POINT ( 'NONE',  ( 18.00000000000000355, 44.75336757549799671, -14.30704879393557150 ) ) ;
#12978=AXIS2_PLACEMENT_3D ( 'NONE', #34778, #39895, #39100 ) ;
#12979=AXIS2_PLACEMENT_3D ( 'NONE', #13739, #11479, #25043 ) ;
#12985=DIRECTION ( 'NONE',  ( 0.000000000000000000, 0.000000000000000000, 1.000000000000000000 ) ) ;
#12988=ORIENTED_EDGE ( 'NONE', *, *, #10355, .T. ) ;
#12996=CARTESIAN_POINT ( 'NONE',  ( 18.00000000000000355, 39.78933988720115877, 24.98727647985016276 ) ) ;
#13004=AXIS2_PLACEMENT_3D ( 'NONE', #9914, #29805, #30218 ) ;
#13014=DIRECTION ( 'NONE',  ( 0.000000000000000000, 0.3681245526846786964, -0.9297764858882511252 ) ) ;
#13017=ORIENTED_EDGE ( 'NONE', *, *, #15042, .F. ) ;
#13026=CARTESIAN_POINT ( 'NONE',  ( 18.00000000000000355, 0.000000000000000000, 0.000000000000000000 ) ) ;
#13032=AXIS2_PLACEMENT_3D ( 'NONE', #19573, #42862, #35885 ) ;
#13035=CARTESIAN_POINT ( 'NONE',  ( 18.00000000000000355, 0.000000000000000000, 0.000000000000000000 ) ) ;
#13046=EDGE_LOOP ( 'NONE', ( #217, #14477, #25209, #38857 ) ) ;
#13049=EDGE_LOOP ( 'NONE', ( #9883, #34702, #13747, #10822 ) ) ;
#13057=EDGE_CURVE ( 'NONE', #16464, #13205, #40045, .T. ) ;
#13058=EDGE_CURVE ( 'NONE', #8904, #8390, #26139, .T. ) ;
#13064=VERTEX_POINT ( 'NONE', #3189 ) ;
#13071=CIRCLE ( 'NONE', #26330, 51.99999999999999289 ) ;
#13074=EDGE_CURVE ( 'NONE', #5452, #2577, #15013, .T. ) ;
#13075=DIRECTION ( 'NONE',  ( -1.000000000000000000, 0.000000000000000000, -0.000000000000000000 ) ) ;
#13084=CARTESIAN_POINT ( 'NONE',  ( 18.00000000000000355, -46.11014828289851408, 9.022736828080542892 ) ) ;
#13085=ORIENTED_EDGE ( 'NONE', *, *, #31372, .F. ) ;
#13086=CARTESIAN_POINT ( 'NONE',  ( 0.000000000000000000, 0.000000000000000000, 0.000000000000000000 ) ) ;
#13087=DIRECTION ( 'NONE',  ( 0.000000000000000000, -0.9048270524660235736, 0.4257792915650641108 ) ) ;
#13088=EDGE_LOOP ( 'NONE', ( #14142, #29102, #18898, #42818 ) ) ;
#13094=AXIS2_PLACEMENT_3D ( 'NONE', #3081, #36473, #40180 ) ;
#13096=DIRECTION ( 'NONE',  ( 0.000000000000000000, 0.000000000000000000, 1.000000000000000000 ) ) ;
#13114=AXIS2_PLACEMENT_3D ( 'NONE', #21609, #11767, #18972 ) ;
#13137=FACE_OUTER_BOUND ( 'NONE', #7570, .T. ) ;
#13144=DIRECTION ( 'NONE',  ( 0.000000000000000000, 0.000000000000000000, 1.000000000000000000 ) ) ;
#13149=VECTOR ( 'NONE', #36215, 1000.000000000000000 ) ;
#13150=VECTOR ( 'NONE', #9983, 1000.000000000000000 ) ;
#13151=CARTESIAN_POINT ( 'NONE',  ( 18.00000000000000355, 46.87740477351712798, 3.172455868806036694 ) ) ;
#13152=CARTESIAN_POINT ( 'NONE',  ( 18.00000000000000355, 2.123073309835184386, 47.45152853935334747 ) ) ;
#13156=ORIENTED_EDGE ( 'NONE', *, *, #13850, .F. ) ;
#13158=AXIS2_PLACEMENT_3D ( 'NONE', #23013, #17, #26261 ) ;
#13169=SURFACE_SIDE_STYLE ('',( #23214 ) ) ;
#13172=CARTESIAN_POINT ( 'NONE',  ( 18.00000000000000355, 0.000000000000000000, 0.000000000000000000 ) ) ;
#13182=CIRCLE ( 'NONE', #15989, 51.99999999999999289 ) ;
#13193=ORIENTED_EDGE ( 'NONE', *, *, #27912, .F. ) ;
#13200=EDGE_LOOP ( 'NONE', ( #38517, #39982, #22967, #22113 ) ) ;
#13204=DIRECTION ( 'NONE',  ( -1.000000000000000000, 0.000000000000000000, 0.000000000000000000 ) ) ;
#13205=VERTEX_POINT ( 'NONE', #4497 ) ;
#13209=CARTESIAN_POINT ( 'NONE',  ( 9.000000000000001776, -36.06787431788649911, -37.45808914225527531 ) ) ;
#13212=CARTESIAN_POINT ( 'NONE',  ( 0.000000000000000000, -13.56094713063606427, 50.20060470671735686 ) ) ;
#13221=ORIENTED_EDGE ( 'NONE', *, *, #29461, .T. ) ;
#13222=DIRECTION ( 'NONE',  ( -1.000000000000000000, -0.000000000000000000, -0.000000000000000000 ) ) ;
#13229=CARTESIAN_POINT ( 'NONE',  ( 18.00000000000000355, -42.41764978026621691, 20.20639853260276197 ) ) ;
#13231=CARTESIAN_POINT ( 'NONE',  ( 18.00000000000000355, 5.871425383721547320, 51.66745943012283249 ) ) ;
#13235=DIRECTION ( 'NONE',  ( 0.000000000000000000, -0.1253332335643113082, 0.9921147013144769877 ) ) ;
#13238=CIRCLE ( 'NONE', #26459, 20.00000000000000355 ) ;
#13255=CARTESIAN_POINT ( 'NONE',  ( 9.000000000000001776, 47.32430374665962347, -21.55018039121477003 ) ) ;
#13256=LINE ( 'NONE', #29401, #29041 ) ;
#13257=ORIENTED_EDGE ( 'NONE', *, *, #21563, .T. ) ;
#13259=ORIENTED_EDGE ( 'NONE', *, *, #18776, .T. ) ;
#13267=ADVANCED_FACE ( 'NONE', ( #3835 ), #13495, .T. ) ;
#13279=FACE_OUTER_BOUND ( 'NONE', #40606, .T. ) ;
#13293=ADVANCED_FACE ( 'NONE', ( #40498 ), #10636, .T. ) ;
#13300=AXIS2_PLACEMENT_3D ( 'NONE', #16541, #33514, #29842 ) ;
#13305=VERTEX_POINT ( 'NONE', #34614 ) ;
#13319=ORIENTED_EDGE ( 'NONE', *, *, #9746, .T. ) ;
#13326=ORIENTED_EDGE ( 'NONE', *, *, #35282, .T. ) ;
#13330=VECTOR ( 'NONE', #23675, 1000.000000000000000 ) ;
#13337=ORIENTED_EDGE ( 'NONE', *, *, #38978, .T. ) ;
#13347=ORIENTED_EDGE ( 'NONE', *, *, #15250, .T. ) ;
#13348=CARTESIAN_POINT ( 'NONE',  ( 0.000000000000000000, 19.74581912682842244, 48.10512059033399623 ) ) ;
#13351=CIRCLE ( 'NONE', #9152, 20.00000000000000711 ) ;
#13362=CIRCLE ( 'NONE', #4258, 47.49900000000000944 ) ;
#13371=AXIS2_PLACEMENT_3D ( 'NONE', #40738, #14385, #27696 ) ;
#13375=ORIENTED_EDGE ( 'NONE', *, *, #25989, .F. ) ;
#13382=PRESENTATION_STYLE_ASSIGNMENT (( #6579 ) ) ;
#13388=ORIENTED_EDGE ( 'NONE', *, *, #20546, .F. ) ;
#13390=DIRECTION ( 'NONE',  ( -1.000000000000000000, 0.000000000000000000, 0.000000000000000000 ) ) ;
#13399=VERTEX_POINT ( 'NONE', #21588 ) ;
#13402=DIRECTION ( 'NONE',  ( 0.000000000000000000, -0.1253332335643113360, 0.9921147013144769877 ) ) ;
#13420=ORIENTED_EDGE ( 'NONE', *, *, #41790, .T. ) ;
#13423=DIRECTION ( 'NONE',  ( -1.000000000000000000, 0.000000000000000000, -0.000000000000000000 ) ) ;
#13426=CYLINDRICAL_SURFACE ( 'NONE', #39942, 51.99999999999999289 ) ;
#13427=DIRECTION ( 'NONE',  ( -1.000000000000000000, -0.000000000000000000, -0.000000000000000000 ) ) ;
#13431=DIRECTION ( 'NONE',  ( 0.000000000000000000, -0.2486898871648415554, -0.9685831611286345177 ) ) ;
#13432=EDGE_CURVE ( 'NONE', #36472, #4217, #21349, .T. ) ;
#13434=ORIENTED_EDGE ( 'NONE', *, *, #33016, .T. ) ;
#13437=CARTESIAN_POINT ( 'NONE',  ( 18.00000000000000355, 0.000000000000000000, 0.000000000000000000 ) ) ;
#13441=DIRECTION ( 'NONE',  ( 0.000000000000000000, -0.9980267284282723361, 0.06279051952930261860 ) ) ;
#13447=ORIENTED_EDGE ( 'NONE', *, *, #24054, .T. ) ;
#13448=ORIENTED_EDGE ( 'NONE', *, *, #16296, .F. ) ;
#13451=DIRECTION ( 'NONE',  ( -1.000000000000000000, 0.000000000000000000, 0.000000000000000000 ) ) ;
#13455=ORIENTED_EDGE ( 'NONE', *, *, #9886, .T. ) ;
#13465=DIRECTION ( 'NONE',  ( -1.000000000000000000, -0.000000000000000000, -0.000000000000000000 ) ) ;
#13472=DIRECTION ( 'NONE',  ( -1.000000000000000000, 0.000000000000000000, -0.000000000000000000 ) ) ;
#13474=DIRECTION ( 'NONE',  ( 0.000000000000000000, 0.000000000000000000, 1.000000000000000000 ) ) ;
#13477=CARTESIAN_POINT ( 'NONE',  ( 9.000000000000001776, -49.65209126885752511, -15.44894276735603889 ) ) ;
#13479=DIRECTION ( 'NONE',  ( -1.000000000000000000, -0.000000000000000000, -0.000000000000000000 ) ) ;
#13483=ADVANCED_FACE ( 'NONE', ( #20861 ), #40213, .T. ) ;
#13486=CARTESIAN_POINT ( 'NONE',  ( 18.00000000000000355, -9.744342220503087404, -46.48873837489808380 ) ) ;
#13495=CYLINDRICAL_SURFACE ( 'NONE', #3136, 51.99999999999999289 ) ;
#13501=ADVANCED_FACE ( 'NONE', ( #4418 ), #4208, .T. ) ;
#13503=DIRECTION ( 'NONE',  ( -1.000000000000000000, -0.000000000000000000, 0.000000000000000000 ) ) ;
#13509=SHAPE_REPRESENTATION ( 'spur gear_iso_ISO - Spur gear 2M 50T 20PA 18FW ---S50B22H150L15.0N', ( #13552 ), #23928 ) ;
#13512=AXIS2_PLACEMENT_3D ( 'NONE', #34498, #28425, #37985 ) ;
#13517=CARTESIAN_POINT ( 'NONE',  ( 18.00000000000000355, 0.000000000000000000, 0.000000000000000000 ) ) ;
#13530=FACE_OUTER_BOUND ( 'NONE', #34312, .T. ) ;
#13533=CARTESIAN_POINT ( 'NONE',  ( 18.00000000000000355, 0.000000000000000000, 0.000000000000000000 ) ) ;
#13539=EDGE_CURVE ( 'NONE', #39306, #34314, #19932, .T. ) ;
#13551=DIRECTION ( 'NONE',  ( 0.000000000000000000, 0.9510565162951544194, -0.3090169943749447312 ) ) ;
#13552=AXIS2_PLACEMENT_3D ( 'NONE', #3852, #14597, #10213 ) ;
#13557=ORIENTED_EDGE ( 'NONE', *, *, #5551, .T. ) ;
#13559=ORIENTED_EDGE ( 'NONE', *, *, #39941, .F. ) ;
#13562=EDGE_CURVE ( 'NONE', #11213, #3516, #31776, .T. ) ;
#13571=FACE_OUTER_BOUND ( 'NONE', #14724, .T. ) ;
#13575=CIRCLE ( 'NONE', #37274, 20.00000000000000000 ) ;
#13580=EDGE_CURVE ( 'NONE', #27343, #19555, #23985, .T. ) ;
#13586=FACE_OUTER_BOUND ( 'NONE', #37729, .T. ) ;
#13597=ORIENTED_EDGE ( 'NONE', *, *, #35083, .T. ) ;
#13601=DIRECTION ( 'NONE',  ( 0.000000000000000000, 0.000000000000000000, 1.000000000000000000 ) ) ;
#13619=EDGE_LOOP ( 'NONE', ( #2048, #21039, #30786, #7632 ) ) ;
#13627=CARTESIAN_POINT ( 'NONE',  ( 18.00000000000000355, 20.99948489194423118, 42.60488980472788967 ) ) ;
#13640=DIRECTION ( 'NONE',  ( -1.000000000000000000, -0.000000000000000000, 0.000000000000000000 ) ) ;
#13647=ORIENTED_EDGE ( 'NONE', *, *, #29903, .T. ) ;
#13650=CARTESIAN_POINT ( 'NONE',  ( 0.000000000000000000, 44.47301969247467923, -16.68249143361863318 ) ) ;
#13652=CIRCLE ( 'NONE', #29655, 52.00000000000000000 ) ;
#13660=DIRECTION ( 'NONE',  ( 0.000000000000000000, 0.000000000000000000, -1.000000000000000000 ) ) ;
#13661=CIRCLE ( 'NONE', #42281, 52.00000000000000000 ) ;
#13674=ORIENTED_EDGE ( 'NONE', *, *, #3879, .F. ) ;
#13677=EDGE_CURVE ( 'NONE', #23373, #37256, #22764, .T. ) ;
#13678=CARTESIAN_POINT ( 'NONE',  ( 18.00000000000000355, 46.87740477351718482, -3.172455868805370560 ) ) ;
#13681=VECTOR ( 'NONE', #19490, 1000.000000000000000 ) ;
#13682=CYLINDRICAL_SURFACE ( 'NONE', #39356, 47.49900000000000233 ) ;
#13714=CIRCLE ( 'NONE', #25564, 51.99999999999999289 ) ;
#13716=EDGE_LOOP ( 'NONE', ( #23230, #17825, #4623, #39231 ) ) ;
#13721=VERTEX_POINT ( 'NONE', #14085 ) ;
#13722=DIRECTION ( 'NONE',  ( -1.000000000000000000, 0.000000000000000000, 0.000000000000000000 ) ) ;
#13725=LINE ( 'NONE', #3426, #30557 ) ;
#13731=VECTOR ( 'NONE', #599, 1000.000000000000000 ) ;
#13734=FACE_OUTER_BOUND ( 'NONE', #9370, .T. ) ;
#13739=CARTESIAN_POINT ( 'NONE',  ( 18.00000000000000355, -11.46872990052412788, 45.56340405422441364 ) ) ;
#13747=ORIENTED_EDGE ( 'NONE', *, *, #4876, .T. ) ;
#13754=VECTOR ( 'NONE', #9013, 1000.000000000000000 ) ;
#13755=DIRECTION ( 'NONE',  ( 0.000000000000000000, 0.9822872507286879440, 0.1873813145857286533 ) ) ;
#13761=CIRCLE ( 'NONE', #9567, 47.49900000000000233 ) ;
#13776=ORIENTED_EDGE ( 'NONE', *, *, #28768, .F. ) ;
#13783=AXIS2_PLACEMENT_3D ( 'NONE', #23007, #225, #33634 ) ;
#13796=AXIS2_PLACEMENT_3D ( 'NONE', #9444, #9872, #35826 ) ;
#13797=EDGE_CURVE ( 'NONE', #32816, #31641, #8578, .T. ) ;
#13798=ADVANCED_FACE ( 'NONE', ( #31299 ), #28680, .T. ) ;
#13799=DIRECTION ( 'NONE',  ( -1.000000000000000000, -0.000000000000000000, -0.000000000000000000 ) ) ;
#13809=DIRECTION ( 'NONE',  ( 0.000000000000000000, 0.000000000000000000, 1.000000000000000000 ) ) ;
#13826=AXIS2_PLACEMENT_3D ( 'NONE', #39316, #42968, #36640 ) ;
#13827=CARTESIAN_POINT ( 'NONE',  ( 18.00000000000000355, 11.46872990052381880, 45.56340405422447049 ) ) ;
#13830=VERTEX_POINT ( 'NONE', #12096 ) ;
#13838=ORIENTED_EDGE ( 'NONE', *, *, #16361, .T. ) ;
#13847=EDGE_CURVE ( 'NONE', #41179, #8111, #6680, .T. ) ;
#13850=EDGE_CURVE ( 'NONE', #31429, #27234, #5529, .T. ) ;
#13852=EDGE_LOOP ( 'NONE', ( #42079, #43122, #28634, #26240 ) ) ;
#13853=DIRECTION ( 'NONE',  ( -1.000000000000000000, -0.000000000000000000, 0.000000000000000000 ) ) ;
#13856=AXIS2_PLACEMENT_3D ( 'NONE', #5716, #15570, #8564 ) ;
#13866=LINE ( 'NONE', #10117, #19885 ) ;
#13869=ORIENTED_EDGE ( 'NONE', *, *, #1735, .T. ) ;
#13870=CARTESIAN_POINT ( 'NONE',  ( 18.00000000000000355, 35.20873326984080620, 31.88259874184042886 ) ) ;
#13878=ORIENTED_EDGE ( 'NONE', *, *, #6968, .F. ) ;
#13879=DIRECTION ( 'NONE',  ( -1.000000000000000000, 0.000000000000000000, -0.000000000000000000 ) ) ;
#13895=ORIENTED_EDGE ( 'NONE', *, *, #20759, .F. ) ;
#13901=AXIS2_PLACEMENT_3D ( 'NONE', #38275, #21958, #4684 ) ;
#13906=ORIENTED_EDGE ( 'NONE', *, *, #15404, .F. ) ;
#13907=AXIS2_PLACEMENT_3D ( 'NONE', #23655, #7024, #32993 ) ;
#13910=ORIENTED_EDGE ( 'NONE', *, *, #1847, .T. ) ;
#13916=DIRECTION ( 'NONE',  ( -1.000000000000000000, 0.000000000000000000, 0.000000000000000000 ) ) ;
#13920=DIRECTION ( 'NONE',  ( 0.000000000000000000, 0.000000000000000000, -1.000000000000000000 ) ) ;
#13928=AXIS2_PLACEMENT_3D ( 'NONE', #26809, #16145, #40080 ) ;
#13929=DIRECTION ( 'NONE',  ( 0.000000000000000000, 0.8443279255020162966, -0.5358267949789948803 ) ) ;
#13943=ADVANCED_FACE ( 'NONE', ( #15586 ), #12307, .T. ) ;
#13948=FACE_OUTER_BOUND ( 'NONE', #26219, .T. ) ;
#13950=CARTESIAN_POINT ( 'NONE',  ( -10.00000000000000000, 0.000000000000000000, 0.000000000000000000 ) ) ;
#13952=CARTESIAN_POINT ( 'NONE',  ( 18.00000000000000355, -41.20225022064653331, 23.63323037071389621 ) ) ;
#13953=CARTESIAN_POINT ( 'NONE',  ( 18.00000000000000355, 0.000000000000000000, 0.000000000000000000 ) ) ;
#13960=AXIS2_PLACEMENT_3D ( 'NONE', #15268, #19170, #28561 ) ;
#13961=DIRECTION ( 'NONE',  ( -1.000000000000000000, -0.000000000000000000, -0.000000000000000000 ) ) ;
#13963=VECTOR ( 'NONE', #31914, 1000.000000000000000 ) ;
#13970=VERTEX_POINT ( 'NONE', #12947 ) ;
#13978=DIRECTION ( 'NONE',  ( -1.000000000000000000, 0.000000000000000000, 0.000000000000000000 ) ) ;
#13979=ORIENTED_EDGE ( 'NONE', *, *, #33578, .F. ) ;
#13987=CIRCLE ( 'NONE', #1404, 20.00000000000000355 ) ;
#13988=EDGE_LOOP ( 'NONE', ( #7877, #692, #32063, #17365 ) ) ;
#13989=CIRCLE ( 'NONE', #37655, 47.49900000000000233 ) ;
#13991=FACE_OUTER_BOUND ( 'NONE', #35822, .T. ) ;
#14003=DIRECTION ( 'NONE',  ( 1.000000000000000000, 0.000000000000000000, 0.000000000000000000 ) ) ;
#14013=VERTEX_POINT ( 'NONE', #12 ) ;
#14024=MANIFOLD_SOLID_BREP ( 'Bore', #3778 ) ;
#14025=AXIS2_PLACEMENT_3D ( 'NONE', #40292, #26793, #355 ) ;
#14033=EDGE_CURVE ( 'NONE', #20369, #20160, #35812, .T. ) ;
#14041=DIRECTION ( 'NONE',  ( -1.000000000000000000, -0.000000000000000000, 0.000000000000000000 ) ) ;
#14042=ORIENTED_EDGE ( 'NONE', *, *, #15961, .F. ) ;
#14043=DIRECTION ( 'NONE',  ( -1.000000000000000000, -0.000000000000000000, 0.000000000000000000 ) ) ;
#14045=ORIENTED_EDGE ( 'NONE', *, *, #26438, .F. ) ;
#14058=DIRECTION ( 'NONE',  ( 0.000000000000000000, -0.6845471059286792892, -0.7289686274214203232 ) ) ;
#14065=CIRCLE ( 'NONE', #19644, 20.00000000000000711 ) ;
#14070=CARTESIAN_POINT ( 'NONE',  ( 18.00000000000000355, 0.000000000000000000, 0.000000000000000000 ) ) ;
#14075=CARTESIAN_POINT ( 'NONE',  ( 0.000000000000000000, 22.43957647427220081, -41.27978878573604504 ) ) ;
#14078=VERTEX_POINT ( 'NONE', #17750 ) ;
#14085=CARTESIAN_POINT ( 'NONE',  ( 18.00000000000000355, -24.72041153920759982, 40.55929306992680949 ) ) ;
#14088=DIRECTION ( 'NONE',  ( 1.000000000000000000, 0.000000000000000000, 0.000000000000000000 ) ) ;
#14093=ORIENTED_EDGE ( 'NONE', *, *, #28043, .F. ) ;
#14094=CARTESIAN_POINT ( 'NONE',  ( 0.000000000000000000, 25.61928775981106554, -45.25098998563451147 ) ) ;
#14095=ORIENTED_EDGE ( 'NONE', *, *, #20110, .T. ) ;
#14117=DIRECTION ( 'NONE',  ( 0.000000000000000000, -0.8443279255020087470, -0.5358267949790065376 ) ) ;
#14142=ORIENTED_EDGE ( 'NONE', *, *, #7869, .T. ) ;
#14145=FACE_OUTER_BOUND ( 'NONE', #34128, .T. ) ;
#14151=ORIENTED_EDGE ( 'NONE', *, *, #37767, .T. ) ;
#14158=CARTESIAN_POINT ( 'NONE',  ( 18.00000000000000355, 6.109652351741791776, 46.58570277113511793 ) ) ;
#14162=DIRECTION ( 'NONE',  ( 0.000000000000000000, 0.000000000000000000, 1.000000000000000000 ) ) ;
#14165=DIRECTION ( 'NONE',  ( -1.000000000000000000, 0.000000000000000000, 0.000000000000000000 ) ) ;
#14168=DIRECTION ( 'NONE',  ( 0.000000000000000000, 0.1253332335642974305, 0.9921147013144787641 ) ) ;
#14173=DIRECTION ( 'NONE',  ( -1.000000000000000000, -0.000000000000000000, 0.000000000000000000 ) ) ;
#14177=CARTESIAN_POINT ( 'NONE',  ( 18.00000000000000355, 11.46872990052444408, -45.56340405422433548 ) ) ;
#14179=CARTESIAN_POINT ( 'NONE',  ( 0.000000000000000000, 11.90021268425555512, 45.45261810511218670 ) ) ;
#14189=EDGE_CURVE ( 'NONE', #14608, #755, #31814, .T. ) ;
#14197=EDGE_LOOP ( 'NONE', ( #10697, #29546, #359, #38703 ) ) ;
#14199=LINE ( 'NONE', #27496, #5535 ) ;
#14201=ORIENTED_EDGE ( 'NONE', *, *, #38015, .T. ) ;
#14204=DIRECTION ( 'NONE',  ( 0.000000000000000000, 0.000000000000000000, 1.000000000000000000 ) ) ;
#14208=CARTESIAN_POINT ( 'NONE',  ( 18.00000000000000355, -42.03146605346801579, 22.12489237027304512 ) ) ;
#14211=DIRECTION ( 'NONE',  ( 0.000000000000000000, 0.9048270524660176894, 0.4257792915650767118 ) ) ;
#14213=LINE ( 'NONE', #27516, #42817 ) ;
#14217=DIRECTION ( 'NONE',  ( -1.000000000000000000, -0.000000000000000000, 0.000000000000000000 ) ) ;
#14219=DIRECTION ( 'NONE',  ( 0.000000000000000000, 0.9980267284282716700, -0.06279051952930995995 ) ) ;
#14220=VECTOR ( 'NONE', #34328, 1000.000000000000000 ) ;
#14221=DIRECTION ( 'NONE',  ( 0.000000000000000000, 0.000000000000000000, 1.000000000000000000 ) ) ;
#14222=CARTESIAN_POINT ( 'NONE',  ( 18.00000000000000355, 0.000000000000000000, 0.000000000000000000 ) ) ;
#14232=ORIENTED_EDGE ( 'NONE', *, *, #26448, .T. ) ;
#14240=AXIS2_PLACEMENT_3D ( 'NONE', #20729, #595, #30730 ) ;
#14248=AXIS2_PLACEMENT_3D ( 'NONE', #30866, #1602, #17806 ) ;
#14249=ORIENTED_EDGE ( 'NONE', *, *, #27370, .F. ) ;
#14251=CIRCLE ( 'NONE', #42793, 52.00000000000000000 ) ;
#14255=VERTEX_POINT ( 'NONE', #41247 ) ;
#14260=VERTEX_POINT ( 'NONE', #4834 ) ;
#14264=ORIENTED_EDGE ( 'NONE', *, *, #34915, .T. ) ;
#14265=DIRECTION ( 'NONE',  ( -1.000000000000000000, 0.000000000000000000, 0.000000000000000000 ) ) ;
#14269=ADVANCED_FACE ( 'NONE', ( #21885 ), #24516, .T. ) ;
#14271=CARTESIAN_POINT ( 'NONE',  ( 18.00000000000000355, -22.43957647427129842, -41.27978878573651400 ) ) ;
#14272=DIRECTION ( 'NONE',  ( 0.000000000000000000, -0.1253332335643113360, 0.9921147013144769877 ) ) ;
#14273=CYLINDRICAL_SURFACE ( 'NONE', #22051, 47.49900000000000233 ) ;
#14276=VERTEX_POINT ( 'NONE', #31460 ) ;
#14279=CARTESIAN_POINT ( 'NONE',  ( 18.00000000000000355, -39.64889472655755043, 33.64468972902493960 ) ) ;
#14287=ORIENTED_EDGE ( 'NONE', *, *, #30448, .T. ) ;
#14291=CIRCLE ( 'NONE', #3090, 51.99999999999999289 ) ;
#14294=LINE ( 'NONE', #31085, #18027 ) ;
#14296=CARTESIAN_POINT ( 'NONE',  ( 9.000000000000001776, 35.11945359308110426, 38.34871548466026070 ) ) ;
#14299=LINE ( 'NONE', #11034, #21472 ) ;
#14301=CYLINDRICAL_SURFACE ( 'NONE', #5936, 51.99999999999999289 ) ;
#14304=ORIENTED_EDGE ( 'NONE', *, *, #38202, .F. ) ;
#14313=CIRCLE ( 'NONE', #38666, 47.49900000000000944 ) ;
#14315=CIRCLE ( 'NONE', #19903, 20.00000000000000355 ) ;
#14317=ORIENTED_EDGE ( 'NONE', *, *, #22720, .F. ) ;
#14334=CYLINDRICAL_SURFACE ( 'NONE', #958, 47.49900000000000233 ) ;
#14338=CIRCLE ( 'NONE', #5960, 20.00000000000000711 ) ;
#14346=DIRECTION ( 'NONE',  ( 0.000000000000000000, 0.9980267284282712259, 0.06279051952931685721 ) ) ;
#14348=CIRCLE ( 'NONE', #6649, 52.00000000000000000 ) ;
#14357=DIRECTION ( 'NONE',  ( -1.000000000000000000, -0.000000000000000000, 0.000000000000000000 ) ) ;
#14358=ORIENTED_EDGE ( 'NONE', *, *, #21761, .T. ) ;
#14369=AXIS2_PLACEMENT_3D ( 'NONE', #3649, #2786, #13096 ) ;
#14372=CYLINDRICAL_SURFACE ( 'NONE', #10737, 51.99999999999999289 ) ;
#14375=AXIS2_PLACEMENT_3D ( 'NONE', #21936, #4884, #1599 ) ;
#14380=ADVANCED_FACE ( 'NONE', ( #6110 ), #15747, .T. ) ;
#14385=DIRECTION ( 'NONE',  ( -1.000000000000000000, -0.000000000000000000, -0.000000000000000000 ) ) ;
#14399=CIRCLE ( 'NONE', #24894, 20.00000000000000355 ) ;
#14409=CIRCLE ( 'NONE', #27682, 20.00000000000001066 ) ;
#14411=ORIENTED_EDGE ( 'NONE', *, *, #3193, .F. ) ;
#14415=CIRCLE ( 'NONE', #1144, 20.00000000000000000 ) ;
#14416=ORIENTED_EDGE ( 'NONE', *, *, #35271, .T. ) ;
#14418=CYLINDRICAL_SURFACE ( 'NONE', #36885, 47.49900000000000233 ) ;
#14422=DIRECTION ( 'NONE',  ( 0.000000000000000000, 0.000000000000000000, 1.000000000000000000 ) ) ;
#14424=ORIENTED_EDGE ( 'NONE', *, *, #25334, .F. ) ;
#14431=EDGE_CURVE ( 'NONE', #5278, #33305, #23753, .T. ) ;
#14433=CIRCLE ( 'NONE', #31147, 20.00000000000000711 ) ;
#14439=DIRECTION ( 'NONE',  ( 1.000000000000000000, 0.000000000000000000, -0.000000000000000000 ) ) ;
#14451=DIRECTION ( 'NONE',  ( -1.000000000000000000, 0.000000000000000000, 0.000000000000000000 ) ) ;
#14458=CARTESIAN_POINT ( 'NONE',  ( 0.000000000000000000, -42.41764978026593269, -20.20639853260334107 ) ) ;
#14467=CARTESIAN_POINT ( 'NONE',  ( 18.00000000000000355, -20.99948489194393275, -42.60488980472802467 ) ) ;
#14470=VERTEX_POINT ( 'NONE', #3013 ) ;
#14473=DIRECTION ( 'NONE',  ( -1.000000000000000000, -0.000000000000000000, -0.000000000000000000 ) ) ;
#14477=ORIENTED_EDGE ( 'NONE', *, *, #16249, .F. ) ;
#14483=AXIS2_PLACEMENT_3D ( 'NONE', #14672, #27533, #40808 ) ;
#14485=VERTEX_POINT ( 'NONE', #16172 ) ;
#14492=EDGE_CURVE ( 'NONE', #21903, #2287, #12354, .T. ) ;
#14511=VECTOR ( 'NONE', #15344, 1000.000000000000000 ) ;
#14514=APPLICATION_CONTEXT ( 'automotive_design' ) ;
#14515=EDGE_LOOP ( 'NONE', ( #1279, #4804, #39913, #24370 ) ) ;
#14523=DIRECTION ( 'NONE',  ( -1.000000000000000000, 0.000000000000000000, -0.000000000000000000 ) ) ;
#14524=ORIENTED_EDGE ( 'NONE', *, *, #12459, .T. ) ;
#14531=CARTESIAN_POINT ( 'NONE',  ( -10.00000000000000000, 0.000000000000000000, 0.000000000000000000 ) ) ;
#14533=ORIENTED_EDGE ( 'NONE', *, *, #20323, .F. ) ;
#14537=CIRCLE ( 'NONE', #4765, 51.99999999999999289 ) ;
#14540=ORIENTED_EDGE ( 'NONE', *, *, #16623, .T. ) ;
#14558=DIRECTION ( 'NONE',  ( 0.000000000000000000, 0.9048270524660205760, -0.4257792915650704391 ) ) ;
#14565=ORIENTED_EDGE ( 'NONE', *, *, #33118, .F. ) ;
#14566=EDGE_CURVE ( 'NONE', #10279, #10758, #33970, .T. ) ;
#14579=EDGE_LOOP ( 'NONE', ( #30452, #28341, #40053, #36922 ) ) ;
#14583=EDGE_CURVE ( 'NONE', #40375, #18884, #22868, .T. ) ;
#14584=DIRECTION ( 'NONE',  ( -1.000000000000000000, 0.000000000000000000, -0.000000000000000000 ) ) ;
#14587=VERTEX_POINT ( 'NONE', #7782 ) ;
#14596=CIRCLE ( 'NONE', #41017, 20.00000000000000711 ) ;
#14597=DIRECTION ( 'NONE',  ( 0.000000000000000000, 0.000000000000000000, 1.000000000000000000 ) ) ;
#14605=DIRECTION ( 'NONE',  ( 0.000000000000000000, 0.000000000000000000, -1.000000000000000000 ) ) ;
#14608=VERTEX_POINT ( 'NONE', #10856 ) ;
#14611=EDGE_LOOP ( 'NONE', ( #6123, #15741, #32488, #38603 ) ) ;
#14614=DIRECTION ( 'NONE',  ( -1.000000000000000000, 0.000000000000000000, 0.000000000000000000 ) ) ;
#14623=ORIENTED_EDGE ( 'NONE', *, *, #11590, .T. ) ;
#14636=ORIENTED_EDGE ( 'NONE', *, *, #32697, .T. ) ;
#14643=ORIENTED_EDGE ( 'NONE', *, *, #36594, .F. ) ;
#14645=CARTESIAN_POINT ( 'NONE',  ( 0.000000000000000000, 7.162210897275730126, 51.50439529848829778 ) ) ;
#14653=AXIS2_PLACEMENT_3D ( 'NONE', #23061, #8860, #19142 ) ;
#14655=ORIENTED_EDGE ( 'NONE', *, *, #4756, .T. ) ;
#14661=CARTESIAN_POINT ( 'NONE',  ( 18.00000000000000355, -32.00046193115124282, -34.40241257139720688 ) ) ;
#14664=DIRECTION ( 'NONE',  ( -1.000000000000000000, 0.000000000000000000, 0.000000000000000000 ) ) ;
#14672=CARTESIAN_POINT ( 'NONE',  ( 18.00000000000000355, -36.34385289850609979, 29.77717097092063270 ) ) ;
#14673=VERTEX_POINT ( 'NONE', #17214 ) ;
#14681=ADVANCED_FACE ( 'NONE', ( #30501 ), #18093, .T. ) ;
#14693=FACE_OUTER_BOUND ( 'NONE', #13988, .T. ) ;
#14694=CARTESIAN_POINT ( 'NONE',  ( 18.00000000000000355, 32.32520163883584274, 34.09746168776050013 ) ) ;
#14697=ORIENTED_EDGE ( 'NONE', *, *, #32192, .F. ) ;
#14699=VERTEX_POINT ( 'NONE', #21994 ) ;
#14701=EDGE_CURVE ( 'NONE', #41125, #8821, #41633, .T. ) ;
#14703=AXIS2_PLACEMENT_3D ( 'NONE', #32714, #16157, #27057 ) ;
#14710=ORIENTED_EDGE ( 'NONE', *, *, #30088, .T. ) ;
#14724=EDGE_LOOP ( 'NONE', ( #22380, #3808, #37230, #36550 ) ) ;
#14734=CYLINDRICAL_SURFACE ( 'NONE', #12978, 47.49900000000000233 ) ;
#14739=LINE ( 'NONE', #11238, #24270 ) ;
#14756=CARTESIAN_POINT ( 'NONE',  ( 0.000000000000000000, -46.90537658765333617, 2.727856614654147638 ) ) ;
#14764=LINE ( 'NONE', #13952, #13731 ) ;
#14770=EDGE_CURVE ( 'NONE', #23787, #3192, #12387, .T. ) ;
#14776=CARTESIAN_POINT ( 'NONE',  ( 18.00000000000000355, -47.22458491092822896, 5.098390039074067737 ) ) ;
#14785=DIRECTION ( 'NONE',  ( -1.000000000000000000, -0.000000000000000000, 0.000000000000000000 ) ) ;
#14796=DIRECTION ( 'NONE',  ( 1.000000000000000000, 0.000000000000000000, 0.000000000000000000 ) ) ;
#14797=ORIENTED_EDGE ( 'NONE', *, *, #22975, .F. ) ;
#14806=ORIENTED_EDGE ( 'NONE', *, *, #11851, .T. ) ;
#14809=VECTOR ( 'NONE', #41207, 1000.000000000000000 ) ;
#14812=ORIENTED_EDGE ( 'NONE', *, *, #34223, .F. ) ;
#14829=ADVANCED_FACE ( 'NONE', ( #11947 ), #9718, .T. ) ;
#14834=AXIS2_PLACEMENT_3D ( 'NONE', #7161, #17025, #20517 ) ;
#14846=DIRECTION ( 'NONE',  ( -1.000000000000000000, -0.000000000000000000, -0.000000000000000000 ) ) ;
#14854=DIRECTION ( 'NONE',  ( 0.000000000000000000, 0.000000000000000000, 1.000000000000000000 ) ) ;
#14858=CARTESIAN_POINT ( 'NONE',  ( 18.00000000000000355, -37.91532898920899441, -28.61088654061679648 ) ) ;
#14860=DIRECTION ( 'NONE',  ( 0.000000000000000000, 0.000000000000000000, -1.000000000000000000 ) ) ;
#14864=ORIENTED_EDGE ( 'NONE', *, *, #4140, .T. ) ;
#14869=DIRECTION ( 'NONE',  ( 1.000000000000000000, 0.000000000000000000, 0.000000000000000000 ) ) ;
#14874=CARTESIAN_POINT ( 'NONE',  ( 0.000000000000000000, 51.93417535146742381, -2.615612846549375536 ) ) ;
#14875=EDGE_CURVE ( 'NONE', #37240, #10495, #13071, .T. ) ;
#14880=ADVANCED_FACE ( 'NONE', ( #6645 ), #9921, .T. ) ;
#14884=DIRECTION ( 'NONE',  ( -1.000000000000000000, -0.000000000000000000, 0.000000000000000000 ) ) ;
#14889=LINE ( 'NONE', #4370, #29800 ) ;
#14900=ADVANCED_FACE ( 'NONE', ( #36106 ), #26519, .T. ) ;
#14912=CARTESIAN_POINT ( 'NONE',  ( 0.000000000000000000, 27.79676263918241119, -37.88001506494740056 ) ) ;
#14914=CIRCLE ( 'NONE', #7201, 20.00000000000000711 ) ;
#14919=ORIENTED_EDGE ( 'NONE', *, *, #22326, .F. ) ;
#14923=VERTEX_POINT ( 'NONE', #16071 ) ;
#14924=CARTESIAN_POINT ( 'NONE',  ( 18.00000000000000355, -44.47301969247432396, -16.68249143361957465 ) ) ;
#14932=EDGE_CURVE ( 'NONE', #18546, #20442, #29823, .T. ) ;
#14937=ADVANCED_FACE ( 'NONE', ( #23270 ), #26319, .T. ) ;
#14945=CIRCLE ( 'NONE', #14240, 47.49900000000000944 ) ;
#14950=ORIENTED_EDGE ( 'NONE', *, *, #36251, .F. ) ;
#14954=VECTOR ( 'NONE', #41236, 1000.000000000000000 ) ;
#14961=CARTESIAN_POINT ( 'NONE',  ( 18.00000000000000355, -0.2227391519119825691, 46.98410307550729215 ) ) ;
#14965=ORIENTED_EDGE ( 'NONE', *, *, #12257, .F. ) ;
#14972=VERTEX_POINT ( 'NONE', #14094 ) ;
#14975=DIRECTION ( 'NONE',  ( -1.000000000000000000, 0.000000000000000000, -0.000000000000000000 ) ) ;
#14976=AXIS2_PLACEMENT_3D ( 'NONE', #38123, #25293, #5172 ) ;
#14986=DIRECTION ( 'NONE',  ( 0.000000000000000000, -0.9048270524660145808, -0.4257792915650830956 ) ) ;
#14998=VECTOR ( 'NONE', #2479, 1000.000000000000000 ) ;
#15000=EDGE_CURVE ( 'NONE', #30041, #37276, #14294, .T. ) ;
#15013=CIRCLE ( 'NONE', #1033, 51.99999999999999289 ) ;
#15023=EDGE_CURVE ( 'NONE', #22307, #30436, #37397, .T. ) ;
#15026=DIRECTION ( 'NONE',  ( 0.000000000000000000, 0.8443279255020125218, 0.5358267949790006535 ) ) ;
#15029=ORIENTED_EDGE ( 'NONE', *, *, #11833, .T. ) ;
#15042=EDGE_CURVE ( 'NONE', #39753, #16742, #14739, .T. ) ;
#15045=AXIS2_PLACEMENT_3D ( 'NONE', #30714, #26787, #34184 ) ;
#15051=CARTESIAN_POINT ( 'NONE',  ( 0.000000000000000000, 27.43636312076321104, 38.14186064215159888 ) ) ;
#15056=AXIS2_PLACEMENT_3D ( 'NONE', #40605, #41045, #10748 ) ;
#15065=CYLINDRICAL_SURFACE ( 'NONE', #9387, 47.49900000000000233 ) ;
#15083=AXIS2_PLACEMENT_3D ( 'NONE', #22572, #36630, #33375 ) ;
#15087=VECTOR ( 'NONE', #31681, 1000.000000000000000 ) ;
#15091=CARTESIAN_POINT ( 'NONE',  ( 0.000000000000000000, 0.000000000000000000, 0.000000000000000000 ) ) ;
#15092=DIRECTION ( 'NONE',  ( 0.000000000000000000, 0.000000000000000000, 1.000000000000000000 ) ) ;
#15093=DIRECTION ( 'NONE',  ( 0.000000000000000000, 0.000000000000000000, 1.000000000000000000 ) ) ;
#15094=DIRECTION ( 'NONE',  ( -1.000000000000000000, 0.000000000000000000, -0.000000000000000000 ) ) ;
#15112=CARTESIAN_POINT ( 'NONE',  ( 18.00000000000000355, 36.05989434073613609, 30.12041790338630776 ) ) ;
#15114=ADVANCED_FACE ( 'NONE', ( #24129 ), #3774, .T. ) ;
#15116=CIRCLE ( 'NONE', #19278, 52.00000000000000000 ) ;
#15121=CIRCLE ( 'NONE', #17941, 20.00000000000000711 ) ;
#15135=EDGE_CURVE ( 'NONE', #40496, #30041, #36078, .T. ) ;
#15137=EDGE_LOOP ( 'NONE', ( #22829, #12988 ) ) ;
#15138=CARTESIAN_POINT ( 'NONE',  ( 18.00000000000000355, -51.85248208264519576, 3.914090171286020325 ) ) ;
#15139=ORIENTED_EDGE ( 'NONE', *, *, #400, .T. ) ;
#15144=DIRECTION ( 'NONE',  ( -1.000000000000000000, 0.000000000000000000, 0.000000000000000000 ) ) ;
#15146=ORIENTED_EDGE ( 'NONE', *, *, #29852, .F. ) ;
#15160=EDGE_CURVE ( 'NONE', #24128, #16426, #730, .T. ) ;
#15172=ORIENTED_EDGE ( 'NONE', *, *, #16142, .F. ) ;
#15180=AXIS2_PLACEMENT_3D ( 'NONE', #23063, #33859, #6429 ) ;
#15181=CARTESIAN_POINT ( 'NONE',  ( 18.00000000000000355, 36.06787431788676912, 37.45808914225501240 ) ) ;
#15192=EDGE_CURVE ( 'NONE', #23382, #19555, #8911, .T. ) ;
#15198=DIRECTION ( 'NONE',  ( -1.000000000000000000, 0.000000000000000000, -0.000000000000000000 ) ) ;
#15205=CYLINDRICAL_SURFACE ( 'NONE', #12582, 51.99999999999999289 ) ;
#15219=ORIENTED_EDGE ( 'NONE', *, *, #34270, .T. ) ;
#15224=DIRECTION ( 'NONE',  ( 1.000000000000000000, 0.000000000000000000, -0.000000000000000000 ) ) ;
#15231=ORIENTED_EDGE ( 'NONE', *, *, #26453, .F. ) ;
#15238=CIRCLE ( 'NONE', #18712, 20.00000000000001066 ) ;
#15244=AXIS2_PLACEMENT_3D ( 'NONE', #28895, #24786, #8584 ) ;
#15247=VECTOR ( 'NONE', #42538, 1000.000000000000000 ) ;
#15248=DIRECTION ( 'NONE',  ( -1.000000000000000000, -0.000000000000000000, 0.000000000000000000 ) ) ;
#15250=EDGE_CURVE ( 'NONE', #33958, #33515, #21516, .T. ) ;
#15254=LINE ( 'NONE', #21150, #37659 ) ;
#15268=CARTESIAN_POINT ( 'NONE',  ( 18.00000000000000355, 0.000000000000000000, 0.000000000000000000 ) ) ;
#15270=AXIS2_PLACEMENT_3D ( 'NONE', #34248, #20778, #14204 ) ;
#15271=VECTOR ( 'NONE', #17003, 1000.000000000000000 ) ;
#15272=CARTESIAN_POINT ( 'NONE',  ( 0.000000000000000000, -51.93417535146743802, 2.615612846549014492 ) ) ;
#15285=ORIENTED_EDGE ( 'NONE', *, *, #12667, .T. ) ;
#15291=CARTESIAN_POINT ( 'NONE',  ( 18.00000000000000355, 0.000000000000000000, 0.000000000000000000 ) ) ;
#15296=EDGE_CURVE ( 'NONE', #1993, #3154, #12418, .T. ) ;
#15297=FACE_OUTER_BOUND ( 'NONE', #27201, .T. ) ;
#15301=ORIENTED_EDGE ( 'NONE', *, *, #1105, .T. ) ;
#15305=DIRECTION ( 'NONE',  ( -1.000000000000000000, -0.000000000000000000, -0.000000000000000000 ) ) ;
#15307=DIRECTION ( 'NONE',  ( -1.000000000000000000, 0.000000000000000000, 0.000000000000000000 ) ) ;
#15319=FACE_OUTER_BOUND ( 'NONE', #28205, .T. ) ;
#15320=DIRECTION ( 'NONE',  ( 0.000000000000000000, 0.6845471059286899473, -0.7289686274214103312 ) ) ;
#15328=EDGE_CURVE ( 'NONE', #3009, #32816, #35403, .T. ) ;
#15339=EDGE_CURVE ( 'NONE', #25565, #12306, #20855, .T. ) ;
#15342=EDGE_LOOP ( 'NONE', ( #35374, #39061, #30187, #35800 ) ) ;
#15344=DIRECTION ( 'NONE',  ( 1.000000000000000000, -0.000000000000000000, 0.000000000000000000 ) ) ;
#15349=DIRECTION ( 'NONE',  ( 0.000000000000000000, 0.000000000000000000, -1.000000000000000000 ) ) ;
#15350=VERTEX_POINT ( 'NONE', #26044 ) ;
#15351=EDGE_CURVE ( 'NONE', #20442, #28617, #42366, .T. ) ;
#15352=VERTEX_POINT ( 'NONE', #22580 ) ;
#15356=EDGE_CURVE ( 'NONE', #37256, #39961, #37521, .T. ) ;
#15380=PRODUCT_DEFINITION ( 'UNKNOWN', '', #31662, #22078 ) ;
#15384=ORIENTED_EDGE ( 'NONE', *, *, #36187, .T. ) ;
#15385=EDGE_LOOP ( 'NONE', ( #16983, #4363, #15146, #22943 ) ) ;
#15386=CARTESIAN_POINT ( 'NONE',  ( -10.00000000000000000, 0.000000000000000000, 51.99999999999999289 ) ) ;
#15397=AXIS2_PLACEMENT_3D ( 'NONE', #14222, #24052, #24499 ) ;
#15399=CYLINDRICAL_SURFACE ( 'NONE', #8752, 20.00000000000000711 ) ;
#15400=ORIENTED_EDGE ( 'NONE', *, *, #42719, .T. ) ;
#15401=ORIENTED_EDGE ( 'NONE', *, *, #20323, .T. ) ;
#15404=EDGE_CURVE ( 'NONE', #32412, #3192, #29750, .T. ) ;
#15416=ORIENTED_EDGE ( 'NONE', *, *, #25200, .T. ) ;
#15422=VERTEX_POINT ( 'NONE', #12531 ) ;
#15424=LINE ( 'NONE', #1423, #2491 ) ;
#15425=EDGE_CURVE ( 'NONE', #9420, #20431, #29968, .T. ) ;
#15431=ADVANCED_FACE ( 'NONE', ( #6587 ), #26683, .T. ) ;
#15432=EDGE_CURVE ( 'NONE', #29484, #42037, #4049, .T. ) ;
#15442=VECTOR ( 'NONE', #23761, 1000.000000000000000 ) ;
#15444=ORIENTED_EDGE ( 'NONE', *, *, #27157, .T. ) ;
#15475=AXIS2_PLACEMENT_3D ( 'NONE', #2470, #29554, #16257 ) ;
#15480=FACE_OUTER_BOUND ( 'NONE', #7789, .T. ) ;
#15481=ORIENTED_EDGE ( 'NONE', *, *, #19048, .F. ) ;
#15493=DIRECTION ( 'NONE',  ( 0.000000000000000000, 0.000000000000000000, 1.000000000000000000 ) ) ;
#15496=CARTESIAN_POINT ( 'NONE',  ( 0.000000000000000000, -46.77034588191289544, -22.72740077717278595 ) ) ;
#15497=CIRCLE ( 'NONE', #27308, 52.00000000000000000 ) ;
#15498=LINE ( 'NONE', #25121, #27214 ) ;
#15499=EDGE_LOOP ( 'NONE', ( #19665, #24039, #15709, #32495 ) ) ;
#15511=LINE ( 'NONE', #42071, #10040 ) ;
#15513=DIRECTION ( 'NONE',  ( 1.000000000000000000, 0.000000000000000000, 0.000000000000000000 ) ) ;
#15516=CARTESIAN_POINT ( 'NONE',  ( 18.00000000000000355, -46.11014828289851408, 9.022736828080542892 ) ) ;
#15519=ORIENTED_EDGE ( 'NONE', *, *, #33016, .F. ) ;
#15534=ORIENTED_EDGE ( 'NONE', *, *, #28712, .F. ) ;
#15537=ADVANCED_FACE ( 'NONE', ( #26907 ), #240, .T. ) ;
#15541=LINE ( 'NONE', #5892, #29505 ) ;
#15551=VECTOR ( 'NONE', #40298, 1000.000000000000000 ) ;
#15559=ORIENTED_EDGE ( 'NONE', *, *, #39262, .T. ) ;
#15561=DIRECTION ( 'NONE',  ( -1.000000000000000000, -0.000000000000000000, 0.000000000000000000 ) ) ;
#15563=CARTESIAN_POINT ( 'NONE',  ( 18.00000000000000355, 27.79676263918241119, -37.88001506494740056 ) ) ;
#15570=DIRECTION ( 'NONE',  ( -1.000000000000000000, 0.000000000000000000, -0.000000000000000000 ) ) ;
#15576=VERTEX_POINT ( 'NONE', #6595 ) ;
#15586=FACE_OUTER_BOUND ( 'NONE', #20467, .T. ) ;
#15597=DIRECTION ( 'NONE',  ( 0.000000000000000000, 0.000000000000000000, 1.000000000000000000 ) ) ;
#15599=ORIENTED_EDGE ( 'NONE', *, *, #41457, .T. ) ;
#15609=CARTESIAN_POINT ( 'NONE',  ( 0.000000000000000000, 30.93515269692163017, -36.04401931830219752 ) ) ;
#15611=VERTEX_POINT ( 'NONE', #19316 ) ;
#15618=DIRECTION ( 'NONE',  ( 0.000000000000000000, 0.000000000000000000, 1.000000000000000000 ) ) ;
#15619=CIRCLE ( 'NONE', #933, 52.00000000000000000 ) ;
#15626=CARTESIAN_POINT ( 'NONE',  ( 18.00000000000000355, -43.55304910509384797, -28.41006711800031681 ) ) ;
#15627=ORIENTED_EDGE ( 'NONE', *, *, #34010, .T. ) ;
#15630=ADVANCED_FACE ( 'NONE', ( #16032 ), #32793, .T. ) ;
#15631=AXIS2_PLACEMENT_3D ( 'NONE', #5435, #18799, #2136 ) ;
#15650=AXIS2_PLACEMENT_3D ( 'NONE', #32699, #10215, #36175 ) ;
#15652=CIRCLE ( 'NONE', #40702, 20.00000000000000711 ) ;
#15655=ORIENTED_EDGE ( 'NONE', *, *, #40623, .F. ) ;
#15661=EDGE_CURVE ( 'NONE', #42889, #8370, #6841, .T. ) ;
#15664=CARTESIAN_POINT ( 'NONE',  ( 18.00000000000000355, -32.00046193115174731, 34.40241257139675923 ) ) ;
#15668=CARTESIAN_POINT ( 'NONE',  ( 18.00000000000000355, 46.90537658765331486, 2.727856614654470491 ) ) ;
#15698=CYLINDRICAL_SURFACE ( 'NONE', #42210, 47.49900000000000233 ) ;
#15704=CARTESIAN_POINT ( 'NONE',  ( 18.00000000000000355, 0.000000000000000000, 0.000000000000000000 ) ) ;
#15709=ORIENTED_EDGE ( 'NONE', *, *, #12622, .T. ) ;
#15715=ORIENTED_EDGE ( 'NONE', *, *, #31113, .F. ) ;
#15718=ORIENTED_EDGE ( 'NONE', *, *, #37791, .T. ) ;
#15723=CARTESIAN_POINT ( 'NONE',  ( 0.000000000000000000, -40.47821179127737423, 32.64221760512745618 ) ) ;
#15731=ORIENTED_EDGE ( 'NONE', *, *, #14492, .F. ) ;
#15741=ORIENTED_EDGE ( 'NONE', *, *, #41190, .T. ) ;
#15746=AXIS2_PLACEMENT_3D ( 'NONE', #35043, #28322, #41587 ) ;
#15747=CYLINDRICAL_SURFACE ( 'NONE', #1859, 51.99999999999999289 ) ;
#15750=CIRCLE ( 'NONE', #15083, 20.00000000000000355 ) ;
#15756=CARTESIAN_POINT ( 'NONE',  ( 18.00000000000000355, -51.85248208264514602, -3.914090171286729980 ) ) ;
#15760=ADVANCED_FACE ( 'NONE', ( #24529 ), #36921, .T. ) ;
#15768=DIRECTION ( 'NONE',  ( 0.000000000000000000, 0.000000000000000000, 1.000000000000000000 ) ) ;
#15771=CARTESIAN_POINT ( 'NONE',  ( 9.000000000000001776, 0.6505223195683029758, 51.99593080916758936 ) ) ;
#15779=CYLINDRICAL_SURFACE ( 'NONE', #27315, 20.00000000000000355 ) ;
#15781=CIRCLE ( 'NONE', #405, 47.49900000000000233 ) ;
#15786=AXIS2_PLACEMENT_3D ( 'NONE', #26333, #42447, #29182 ) ;
#15791=VERTEX_POINT ( 'NONE', #15138 ) ;
#15794=EDGE_LOOP ( 'NONE', ( #14042, #21149, #16852, #229 ) ) ;
#15796=FILL_AREA_STYLE_COLOUR ( '', #40836 ) ;
#15819=VERTEX_POINT ( 'NONE', #1990 ) ;
#15821=ORIENTED_EDGE ( 'NONE', *, *, #16669, .T. ) ;
#15826=EDGE_CURVE ( 'NONE', #23382, #26511, #36728, .T. ) ;
#15841=CYLINDRICAL_SURFACE ( 'NONE', #6684, 20.00000000000000355 ) ;
#15842=AXIS2_PLACEMENT_3D ( 'NONE', #24367, #20229, #27392 ) ;
#15845=CARTESIAN_POINT ( 'NONE',  ( 0.000000000000000000, 0.000000000000000000, -11.00000000000000000 ) ) ;
#15847=VERTEX_POINT ( 'NONE', #25599 ) ;
#15848=AXIS2_PLACEMENT_3D ( 'NONE', #33846, #663, #7009 ) ;
#15850=CYLINDRICAL_SURFACE ( 'NONE', #25450, 20.00000000000000711 ) ;
#15854=ORIENTED_EDGE ( 'NONE', *, *, #29349, .F. ) ;
#15868=ORIENTED_EDGE ( 'NONE', *, *, #33951, .F. ) ;
#15878=ORIENTED_EDGE ( 'NONE', *, *, #22140, .F. ) ;
#15880=FACE_OUTER_BOUND ( 'NONE', #498, .T. ) ;
#15881=AXIS2_PLACEMENT_3D ( 'NONE', #29971, #13390, #40394 ) ;
#15885=ORIENTED_EDGE ( 'NONE', *, *, #34113, .F. ) ;
#15886=CARTESIAN_POINT ( 'NONE',  ( 0.000000000000000000, -49.25004636492376875, -16.68630974939812006 ) ) ;
#15895=ORIENTED_EDGE ( 'NONE', *, *, #32402, .T. ) ;
#15898=DIRECTION ( 'NONE',  ( 1.000000000000000000, 0.000000000000000000, 0.000000000000000000 ) ) ;
#15904=AXIS2_PLACEMENT_3D ( 'NONE', #20115, #33585, #9811 ) ;
#15926=ORIENTED_EDGE ( 'NONE', *, *, #18370, .T. ) ;
#15930=CYLINDRICAL_SURFACE ( 'NONE', #2467, 51.99999999999999289 ) ;
#15934=VERTEX_POINT ( 'NONE', #1565 ) ;
#15940=DIRECTION ( 'NONE',  ( -1.000000000000000000, 0.000000000000000000, 0.000000000000000000 ) ) ;
#15947=ORIENTED_EDGE ( 'NONE', *, *, #9040, .T. ) ;
#15952=EDGE_LOOP ( 'NONE', ( #34993, #37847, #2885, #13447 ) ) ;
#15959=ADVANCED_FACE ( 'NONE', ( #12908 ), #26641, .T. ) ;
#15961=EDGE_CURVE ( 'NONE', #41712, #41179, #6129, .T. ) ;
#15963=CIRCLE ( 'NONE', #40299, 47.49899999999999523 ) ;
#15965=EDGE_CURVE ( 'NONE', #235, #15791, #16186, .T. ) ;
#15970=CARTESIAN_POINT ( 'NONE',  ( 18.00000000000000355, 31.08872492060013926, -41.68322423723066805 ) ) ;
#15978=DIRECTION ( 'NONE',  ( 0.000000000000000000, 0.6845471059286847293, 0.7289686274214153272 ) ) ;
#15981=DIRECTION ( 'NONE',  ( -1.000000000000000000, -0.000000000000000000, -0.000000000000000000 ) ) ;
#15987=LINE ( 'NONE', #12702, #9841 ) ;
#15989=AXIS2_PLACEMENT_3D ( 'NONE', #31576, #1668, #8441 ) ;
#15991=EDGE_CURVE ( 'NONE', #41139, #23382, #20133, .T. ) ;
#15995=FACE_OUTER_BOUND ( 'NONE', #24505, .T. ) ;
#16001=ORIENTED_EDGE ( 'NONE', *, *, #17827, .T. ) ;
#16003=VERTEX_POINT ( 'NONE', #13348 ) ;
#16021=DIRECTION ( 'NONE',  ( -1.000000000000000000, 0.000000000000000000, 0.000000000000000000 ) ) ;
#16027=DIRECTION ( 'NONE',  ( 0.000000000000000000, 0.9510565162951544194, -0.3090169943749447312 ) ) ;
#16028=ADVANCED_FACE ( 'NONE', ( #13137 ), #26428, .T. ) ;
#16032=FACE_OUTER_BOUND ( 'NONE', #38835, .T. ) ;
#16037=ORIENTED_EDGE ( 'NONE', *, *, #11851, .F. ) ;
#16041=ORIENTED_EDGE ( 'NONE', *, *, #37947, .F. ) ;
#16054=DIRECTION ( 'NONE',  ( 0.000000000000000000, 0.000000000000000000, 1.000000000000000000 ) ) ;
#16057=DIRECTION ( 'NONE',  ( 0.000000000000000000, 0.000000000000000000, 1.000000000000000000 ) ) ;
#16061=DIRECTION ( 'NONE',  ( -1.000000000000000000, -0.000000000000000000, -0.000000000000000000 ) ) ;
#16063=CARTESIAN_POINT ( 'NONE',  ( 18.00000000000000355, -22.43957647427189528, 41.27978878573620847 ) ) ;
#16071=CARTESIAN_POINT ( 'NONE',  ( 18.00000000000000355, -47.22458491092822896, 5.098390039074067737 ) ) ;
#16076=ADVANCED_FACE ( 'NONE', ( #6338 ), #6538, .T. ) ;
#16077=AXIS2_PLACEMENT_3D ( 'NONE', #32491, #5229, #38591 ) ;
#16079=VECTOR ( 'NONE', #30973, 1000.000000000000000 ) ;
#16084=CARTESIAN_POINT ( 'NONE',  ( 0.000000000000000000, 0.000000000000000000, 0.000000000000000000 ) ) ;
#16090=DIRECTION ( 'NONE',  ( 0.000000000000000000, -0.8443279255020199603, 0.5358267949789887741 ) ) ;
#16123=CARTESIAN_POINT ( 'NONE',  ( 0.000000000000000000, 42.03146605346785947, 22.12489237027331512 ) ) ;
#16134=VECTOR ( 'NONE', #4517, 1000.000000000000000 ) ;
#16137=FACE_OUTER_BOUND ( 'NONE', #1253, .T. ) ;
#16142=EDGE_CURVE ( 'NONE', #36864, #27480, #7849, .T. ) ;
#16145=DIRECTION ( 'NONE',  ( -1.000000000000000000, 0.000000000000000000, 0.000000000000000000 ) ) ;
#16153=CIRCLE ( 'NONE', #5664, 47.49900000000000233 ) ;
#16157=DIRECTION ( 'NONE',  ( -1.000000000000000000, -0.000000000000000000, -0.000000000000000000 ) ) ;
#16163=DIRECTION ( 'NONE',  ( 0.000000000000000000, 0.000000000000000000, 1.000000000000000000 ) ) ;
#16172=CARTESIAN_POINT ( 'NONE',  ( 0.000000000000000000, 45.78515115856043138, 12.64416602183680993 ) ) ;
#16186=LINE ( 'NONE', #16400, #41595 ) ;
#16201=ORIENTED_EDGE ( 'NONE', *, *, #21611, .T. ) ;
#16202=DIRECTION ( 'NONE',  ( 0.000000000000000000, 0.000000000000000000, 1.000000000000000000 ) ) ;
#16204=LINE ( 'NONE', #36229, #38054 ) ;
#16215=CARTESIAN_POINT ( 'NONE',  ( 0.000000000000000000, 22.82995208772688756, 41.06517797613672371 ) ) ;
#16224=DIRECTION ( 'NONE',  ( 0.000000000000000000, 0.4817536741017102164, 0.8763066800438664705 ) ) ;
#16229=FACE_OUTER_BOUND ( 'NONE', #5708, .T. ) ;
#16233=ORIENTED_EDGE ( 'NONE', *, *, #22519, .T. ) ;
#16239=VERTEX_POINT ( 'NONE', #41210 ) ;
#16247=ORIENTED_EDGE ( 'NONE', *, *, #38354, .T. ) ;
#16249=EDGE_CURVE ( 'NONE', #41828, #33958, #18590, .T. ) ;
#16253=EDGE_CURVE ( 'NONE', #20877, #14699, #1916, .T. ) ;
#16257=DIRECTION ( 'NONE',  ( 0.000000000000000000, 0.000000000000000000, 1.000000000000000000 ) ) ;
#16269=FACE_OUTER_BOUND ( 'NONE', #35696, .T. ) ;
#16271=ORIENTED_EDGE ( 'NONE', *, *, #3005, .T. ) ;
#16277=AXIS2_PLACEMENT_3D ( 'NONE', #11166, #37109, #40581 ) ;
#16278=DIRECTION ( 'NONE',  ( -1.000000000000000000, 0.000000000000000000, -0.000000000000000000 ) ) ;
#16280=FACE_OUTER_BOUND ( 'NONE', #15137, .T. ) ;
#16290=DIRECTION ( 'NONE',  ( -1.000000000000000000, -0.000000000000000000, 0.000000000000000000 ) ) ;
#16293=VERTEX_POINT ( 'NONE', #18807 ) ;
#16296=EDGE_CURVE ( 'NONE', #29484, #1556, #32062, .T. ) ;
#16301=CARTESIAN_POINT ( 'NONE',  ( 18.00000000000000355, 24.72041153920732981, 40.55929306992697292 ) ) ;
#16306=DIRECTION ( 'NONE',  ( -1.000000000000000000, 0.000000000000000000, -0.000000000000000000 ) ) ;
#16321=AXIS2_PLACEMENT_3D ( 'NONE', #28302, #1641, #20688 ) ;
#16328=VERTEX_POINT ( 'NONE', #31214 ) ;
#16329=EDGE_CURVE ( 'NONE', #27480, #39452, #6803, .T. ) ;
#16331=CARTESIAN_POINT ( 'NONE',  ( -10.00000000000000000, 0.000000000000000000, 0.000000000000000000 ) ) ;
#16344=DIRECTION ( 'NONE',  ( -1.000000000000000000, 0.000000000000000000, 0.000000000000000000 ) ) ;
#16346=CARTESIAN_POINT ( 'NONE',  ( 0.000000000000000000, -3.840921266750155993, 47.34345070675168188 ) ) ;
#16349=ORIENTED_EDGE ( 'NONE', *, *, #29266, .F. ) ;
#16350=CARTESIAN_POINT ( 'NONE',  ( -132.0000507999999968, 0.000000000000000000, -11.00000000000000000 ) ) ;
#16354=CARTESIAN_POINT ( 'NONE',  ( 0.000000000000000000, 36.06787431788676912, 37.45808914225499819 ) ) ;
#16357=DIRECTION ( 'NONE',  ( -1.000000000000000000, 0.000000000000000000, 0.000000000000000000 ) ) ;
#16361=EDGE_CURVE ( 'NONE', #27530, #3449, #11010, .T. ) ;
#16364=CIRCLE ( 'NONE', #34465, 51.99999999999999289 ) ;
#16379=AXIS2_PLACEMENT_3D ( 'NONE', #30426, #24113, #269 ) ;
#16380=ADVANCED_FACE ( 'NONE', ( #24180 ), #37866, .T. ) ;
#16387=CARTESIAN_POINT ( 'NONE',  ( 18.00000000000000355, 47.22458491092820765, 5.098390039074388369 ) ) ;
#16400=CARTESIAN_POINT ( 'NONE',  ( 9.000000000000001776, -51.85248208264520287, 3.914090171286016773 ) ) ;
#16401=ORIENTED_EDGE ( 'NONE', *, *, #31966, .F. ) ;
#16407=VERTEX_POINT ( 'NONE', #27427 ) ;
#16412=CYLINDRICAL_SURFACE ( 'NONE', #37064, 47.49900000000000233 ) ;
#16426=VERTEX_POINT ( 'NONE', #4482 ) ;
#16439=FACE_OUTER_BOUND ( 'NONE', #15499, .T. ) ;
#16441=EDGE_CURVE ( 'NONE', #20431, #38699, #24299, .T. ) ;
#16443=DIRECTION ( 'NONE',  ( 0.000000000000000000, 0.000000000000000000, 1.000000000000000000 ) ) ;
#16451=ORIENTED_EDGE ( 'NONE', *, *, #41033, .T. ) ;
#16452=VECTOR ( 'NONE', #34533, 1000.000000000000000 ) ;
#16454=CARTESIAN_POINT ( 'NONE',  ( 18.00000000000000355, -24.72041153920704204, -40.55929306992713634 ) ) ;
#16463=DIRECTION ( 'NONE',  ( -1.000000000000000000, 0.000000000000000000, 0.000000000000000000 ) ) ;
#16464=VERTEX_POINT ( 'NONE', #24614 ) ;
#16495=CARTESIAN_POINT ( 'NONE',  ( 18.00000000000000355, -44.75336757549789013, 14.30704879393590012 ) ) ;
#16497=ADVANCED_FACE ( 'NONE', ( #27005 ), #40277, .T. ) ;
#16498=ORIENTED_EDGE ( 'NONE', *, *, #14701, .F. ) ;
#16501=FACE_OUTER_BOUND ( 'NONE', #8544, .T. ) ;
#16504=AXIS2_PLACEMENT_3D ( 'NONE', #18354, #28141, #21632 ) ;
#16513=ORIENTED_EDGE ( 'NONE', *, *, #33215, .F. ) ;
#16516=DIRECTION ( 'NONE',  ( 0.000000000000000000, 0.6845471059286847293, 0.7289686274214153272 ) ) ;
#16526=CIRCLE ( 'NONE', #37283, 52.00000000000000000 ) ;
#16535=DIRECTION ( 'NONE',  ( -1.000000000000000000, 0.000000000000000000, -0.000000000000000000 ) ) ;
#16537=VECTOR ( 'NONE', #6913, 1000.000000000000000 ) ;
#16540=VERTEX_POINT ( 'NONE', #12366 ) ;
#16541=CARTESIAN_POINT ( 'NONE',  ( 18.00000000000000355, 0.000000000000000000, 0.000000000000000000 ) ) ;
#16544=DIRECTION ( 'NONE',  ( 0.000000000000000000, 0.000000000000000000, 1.000000000000000000 ) ) ;
#16549=ORIENTED_EDGE ( 'NONE', *, *, #26610, .F. ) ;
#16551=DIRECTION ( 'NONE',  ( -1.000000000000000000, 0.000000000000000000, -0.000000000000000000 ) ) ;
#16552=ORIENTED_EDGE ( 'NONE', *, *, #15023, .T. ) ;
#16564=AXIS2_PLACEMENT_3D ( 'NONE', #34510, #10532, #7031 ) ;
#16568=AXIS2_PLACEMENT_3D ( 'NONE', #11739, #31998, #28320 ) ;
#16586=CYLINDRICAL_SURFACE ( 'NONE', #30116, 20.00000000000001066 ) ;
#16588=ORIENTED_EDGE ( 'NONE', *, *, #10666, .T. ) ;
#16595=VECTOR ( 'NONE', #5744, 1000.000000000000000 ) ;
#16597=ADVANCED_FACE ( 'NONE', ( #8218 ), #21578, .T. ) ;
#16598=CARTESIAN_POINT ( 'NONE',  ( 18.00000000000000355, 32.32520163883584274, 34.09746168776050013 ) ) ;
#16601=DIRECTION ( 'NONE',  ( 0.000000000000000000, 0.9510565162951544194, -0.3090169943749447867 ) ) ;
#16602=VECTOR ( 'NONE', #15307, 1000.000000000000000 ) ;
#16607=CARTESIAN_POINT ( 'NONE',  ( 18.00000000000000355, 0.000000000000000000, 0.000000000000000000 ) ) ;
#16622=CIRCLE ( 'NONE', #22926, 20.00000000000000711 ) ;
#16623=EDGE_CURVE ( 'NONE', #41127, #28999, #28463, .T. ) ;
#16631=AXIS2_PLACEMENT_3D ( 'NONE', #11871, #32553, #29296 ) ;
#16634=AXIS2_PLACEMENT_3D ( 'NONE', #33222, #32991, #39738 ) ;
#16635=ORIENTED_EDGE ( 'NONE', *, *, #43076, .T. ) ;
#16636=ADVANCED_FACE ( 'NONE', ( #12146 ), #19138, .T. ) ;
#16637=LINE ( 'NONE', #39058, #28730 ) ;
#16639=DIRECTION ( 'NONE',  ( -1.000000000000000000, -0.000000000000000000, 0.000000000000000000 ) ) ;
#16641=CARTESIAN_POINT ( 'NONE',  ( 18.00000000000000355, 9.744342220504043084, -46.48873837489787064 ) ) ;
#16648=CARTESIAN_POINT ( 'NONE',  ( 9.000000000000001776, -46.77034588191319386, 22.72740077717214291 ) ) ;
#16657=CARTESIAN_POINT ( 'NONE',  ( 18.00000000000000355, 49.65209126885784485, -15.44894276735498195 ) ) ;
#16669=EDGE_CURVE ( 'NONE', #16830, #10533, #14537, .T. ) ;
#16686=CIRCLE ( 'NONE', #22272, 47.49900000000000233 ) ;
#16698=ORIENTED_EDGE ( 'NONE', *, *, #28737, .T. ) ;
#16704=EDGE_CURVE ( 'NONE', #24321, #39186, #9913, .T. ) ;
#16709=ORIENTED_EDGE ( 'NONE', *, *, #11179, .T. ) ;
#16711=VERTEX_POINT ( 'NONE', #19559 ) ;
#16712=DIRECTION ( 'NONE',  ( 0.000000000000000000, 0.000000000000000000, 1.000000000000000000 ) ) ;
#16717=CIRCLE ( 'NONE', #29248, 20.00000000000000355 ) ;
#16722=ORIENTED_EDGE ( 'NONE', *, *, #28640, .T. ) ;
#16723=DIRECTION ( 'NONE',  ( 0.000000000000000000, 0.000000000000000000, 1.000000000000000000 ) ) ;
#16726=CARTESIAN_POINT ( 'NONE',  ( 0.000000000000000000, -46.11014828289851408, 9.022736828080542892 ) ) ;
#16727=EDGE_CURVE ( 'NONE', #8913, #36864, #6678, .T. ) ;
#16729=CARTESIAN_POINT ( 'NONE',  ( 18.00000000000000355, 0.000000000000000000, 0.000000000000000000 ) ) ;
#16734=DIRECTION ( 'NONE',  ( -1.000000000000000000, -0.000000000000000000, -0.000000000000000000 ) ) ;
#16736=VERTEX_POINT ( 'NONE', #22627 ) ;
#16742=VERTEX_POINT ( 'NONE', #6423 ) ;
#16752=FACE_OUTER_BOUND ( 'NONE', #40928, .T. ) ;
#16784=CARTESIAN_POINT ( 'NONE',  ( 18.00000000000000355, -3.840921266750155993, 47.34345070675168188 ) ) ;
#16792=CARTESIAN_POINT ( 'NONE',  ( 18.00000000000000355, 47.49120266317495265, 0.8606222198176843863 ) ) ;
#16796=CIRCLE ( 'NONE', #26510, 11.00000000000000000 ) ;
#16802=CARTESIAN_POINT ( 'NONE',  ( 18.00000000000000355, -24.72041153920759982, 40.55929306992680949 ) ) ;
#16809=AXIS2_PLACEMENT_3D ( 'NONE', #8021, #21165, #14605 ) ;
#16810=CARTESIAN_POINT ( 'NONE',  ( 18.00000000000000355, 0.000000000000000000, 0.000000000000000000 ) ) ;
#16812=EDGE_CURVE ( 'NONE', #39427, #1993, #5995, .T. ) ;
#16820=DIRECTION ( 'NONE',  ( 1.000000000000000000, 0.000000000000000000, -0.000000000000000000 ) ) ;
#16822=EDGE_LOOP ( 'NONE', ( #12543, #35524, #15401, #14864 ) ) ;
#16830=VERTEX_POINT ( 'NONE', #7337 ) ;
#16836=AXIS2_PLACEMENT_3D ( 'NONE', #18426, #4188, #7910 ) ;
#16842=ADVANCED_FACE ( 'NONE', ( #27006 ), #36357, .T. ) ;
#16851=AXIS2_PLACEMENT_3D ( 'NONE', #26242, #36031, #6156 ) ;
#16852=ORIENTED_EDGE ( 'NONE', *, *, #23452, .F. ) ;
#16888=LINE ( 'NONE', #20589, #37776 ) ;
#16893=AXIS2_PLACEMENT_3D ( 'NONE', #7861, #5022, #21219 ) ;
#16896=CIRCLE ( 'NONE', #7067, 20.00000000000000355 ) ;
#16897=EDGE_LOOP ( 'NONE', ( #9781, #676, #36067, #21454 ) ) ;
#16899=CIRCLE ( 'NONE', #24567, 47.49900000000000233 ) ;
#16900=FACE_OUTER_BOUND ( 'NONE', #31050, .T. ) ;
#16903=ORIENTED_EDGE ( 'NONE', *, *, #32355, .F. ) ;
#16906=ORIENTED_EDGE ( 'NONE', *, *, #35064, .F. ) ;
#16908=ORIENTED_EDGE ( 'NONE', *, *, #30506, .F. ) ;
#16915=ORIENTED_EDGE ( 'NONE', *, *, #29664, .T. ) ;
#16922=ORIENTED_EDGE ( 'NONE', *, *, #8683, .T. ) ;
#16923=ADVANCED_FACE ( 'NONE', ( #30492 ), #3180, .T. ) ;
#16924=CIRCLE ( 'NONE', #29421, 52.00000000000000000 ) ;
#16935=CARTESIAN_POINT ( 'NONE',  ( 18.00000000000000355, 7.162210897275733679, 51.50439529848829068 ) ) ;
#16937=CARTESIAN_POINT ( 'NONE',  ( 0.000000000000000000, -44.25018368420762016, 27.31155879685165999 ) ) ;
#16952=DIRECTION ( 'NONE',  ( -1.000000000000000000, 0.000000000000000000, -0.000000000000000000 ) ) ;
#16953=ORIENTED_EDGE ( 'NONE', *, *, #28347, .F. ) ;
#16967=DIRECTION ( 'NONE',  ( 1.000000000000000000, 0.000000000000000000, 0.000000000000000000 ) ) ;
#16970=ORIENTED_EDGE ( 'NONE', *, *, #26448, .F. ) ;
#16971=EDGE_CURVE ( 'NONE', #15422, #18374, #118, .T. ) ;
#16973=FACE_OUTER_BOUND ( 'NONE', #7844, .T. ) ;
#16977=ORIENTED_EDGE ( 'NONE', *, *, #42044, .T. ) ;
#16983=ORIENTED_EDGE ( 'NONE', *, *, #1847, .F. ) ;
#16987=DIRECTION ( 'NONE',  ( 0.000000000000000000, 0.000000000000000000, 1.000000000000000000 ) ) ;
#16988=VERTEX_POINT ( 'NONE', #17860 ) ;
#16990=AXIS2_PLACEMENT_3D ( 'NONE', #35294, #22897, #22257 ) ;
#16991=DIRECTION ( 'NONE',  ( -1.000000000000000000, -0.000000000000000000, 0.000000000000000000 ) ) ;
#17003=DIRECTION ( 'NONE',  ( 1.000000000000000000, -0.000000000000000000, 0.000000000000000000 ) ) ;
#17013=VERTEX_POINT ( 'NONE', #18088 ) ;
#17020=DIRECTION ( 'NONE',  ( -1.000000000000000000, 0.000000000000000000, -0.000000000000000000 ) ) ;
#17025=DIRECTION ( 'NONE',  ( -1.000000000000000000, -0.000000000000000000, -0.000000000000000000 ) ) ;
#17026=ADVANCED_FACE ( 'NONE', ( #8425 ), #41133, .T. ) ;
#17029=CARTESIAN_POINT ( 'NONE',  ( 18.00000000000000355, 44.75336757549779776, 14.30704879393622164 ) ) ;
#17039=DIRECTION ( 'NONE',  ( 0.000000000000000000, 0.000000000000000000, 1.000000000000000000 ) ) ;
#17046=CARTESIAN_POINT ( 'NONE',  ( 9.000000000000001776, -43.55304910509384797, -28.41006711800032036 ) ) ;
#17051=CARTESIAN_POINT ( 'NONE',  ( 0.000000000000000000, 0.000000000000000000, 0.000000000000000000 ) ) ;
#17053=CARTESIAN_POINT ( 'NONE',  ( 18.00000000000000355, 47.00885577955421013, -6.806061952191806874 ) ) ;
#17059=ORIENTED_EDGE ( 'NONE', *, *, #15404, .T. ) ;
#17061=AXIS2_PLACEMENT_3D ( 'NONE', #42076, #41438, #15093 ) ;
#17062=VERTEX_POINT ( 'NONE', #34825 ) ;
#17066=ORIENTED_EDGE ( 'NONE', *, *, #35082, .F. ) ;
#17067=CARTESIAN_POINT ( 'NONE',  ( 0.000000000000000000, 0.000000000000000000, 0.000000000000000000 ) ) ;
#17092=AXIS2_PLACEMENT_3D ( 'NONE', #17246, #20299, #4520 ) ;
#17093=AXIS2_PLACEMENT_3D ( 'NONE', #7937, #41303, #21306 ) ;
#17097=CYLINDRICAL_SURFACE ( 'NONE', #38142, 51.99999999999999289 ) ;
#17099=EDGE_CURVE ( 'NONE', #12223, #3009, #19303, .T. ) ;
#17100=DIRECTION ( 'NONE',  ( -1.000000000000000000, 0.000000000000000000, 0.000000000000000000 ) ) ;
#17108=VERTEX_POINT ( 'NONE', #37656 ) ;
#17113=ORIENTED_EDGE ( 'NONE', *, *, #28684, .F. ) ;
#17122=DIRECTION ( 'NONE',  ( 0.000000000000000000, 0.000000000000000000, 1.000000000000000000 ) ) ;
#17127=CARTESIAN_POINT ( 'NONE',  ( 18.00000000000000355, -42.41764978026593269, -20.20639853260334107 ) ) ;
#17131=AXIS2_PLACEMENT_3D ( 'NONE', #441, #6560, #39714 ) ;
#17132=DIRECTION ( 'NONE',  ( 0.000000000000000000, -0.9822872507286903865, 0.1873813145857149975 ) ) ;
#17133=DIRECTION ( 'NONE',  ( 0.000000000000000000, 0.8443279255020126328, 0.5358267949790005424 ) ) ;
#17143=DIRECTION ( 'NONE',  ( 0.000000000000000000, 0.000000000000000000, 1.000000000000000000 ) ) ;
#17145=CARTESIAN_POINT ( 'NONE',  ( 18.00000000000000355, -26.17370628620681927, 39.63700417846155233 ) ) ;
#17148=FACE_OUTER_BOUND ( 'NONE', #35769, .T. ) ;
#17151=EDGE_CURVE ( 'NONE', #3818, #31641, #28369, .T. ) ;
#17164=CARTESIAN_POINT ( 'NONE',  ( 18.00000000000000355, 45.78515115856043138, 12.64416602183680993 ) ) ;
#17165=VERTEX_POINT ( 'NONE', #2492 ) ;
#17173=VERTEX_POINT ( 'NONE', #32406 ) ;
#17186=CARTESIAN_POINT ( 'NONE',  ( 0.000000000000000000, 0.000000000000000000, 0.000000000000000000 ) ) ;
#17188=ORIENTED_EDGE ( 'NONE', *, *, #8542, .F. ) ;
#17190=ADVANCED_FACE ( 'NONE', ( #42208 ), #29575, .T. ) ;
#17200=AXIS2_PLACEMENT_3D ( 'NONE', #37280, #7616, #17039 ) ;
#17202=CARTESIAN_POINT ( 'NONE',  ( 9.000000000000001776, -31.08872492059927595, -41.68322423723131465 ) ) ;
#17203=AXIS2_PLACEMENT_3D ( 'NONE', #21597, #24860, #31802 ) ;
#17214=CARTESIAN_POINT ( 'NONE',  ( 0.000000000000000000, 26.17370628620655282, 39.63700417846171575 ) ) ;
#17216=DIRECTION ( 'NONE',  ( 0.000000000000000000, 0.000000000000000000, 1.000000000000000000 ) ) ;
#17230=( GEOMETRIC_REPRESENTATION_CONTEXT ( 3 ) GLOBAL_UNCERTAINTY_ASSIGNED_CONTEXT ( ( #29602 ) ) GLOBAL_UNIT_ASSIGNED_CONTEXT ( ( #26675, #35612, #32570 ) ) REPRESENTATION_CONTEXT ( 'NONE', 'WORKASPACE' ) );
#17235=VECTOR ( 'NONE', #18095, 1000.000000000000000 ) ;
#17240=CARTESIAN_POINT ( 'NONE',  ( 0.000000000000000000, -24.72041153920704204, -40.55929306992713634 ) ) ;
#17246=CARTESIAN_POINT ( 'NONE',  ( 18.00000000000000355, 0.000000000000000000, 0.000000000000000000 ) ) ;
#17255=CIRCLE ( 'NONE', #30493, 20.00000000000000711 ) ;
#17259=DIRECTION ( 'NONE',  ( 0.000000000000000000, 0.000000000000000000, 1.000000000000000000 ) ) ;
#17276=DIRECTION ( 'NONE',  ( -1.000000000000000000, 0.000000000000000000, -0.000000000000000000 ) ) ;
#17279=ORIENTED_EDGE ( 'NONE', *, *, #4756, .F. ) ;
#17308=EDGE_CURVE ( 'NONE', #30585, #16736, #22628, .T. ) ;
#17310=EDGE_CURVE ( 'NONE', #4060, #11416, #29042, .T. ) ;
#17318=CARTESIAN_POINT ( 'NONE',  ( 18.00000000000000355, -38.92705108641749945, 27.21837053747784552 ) ) ;
#17319=CYLINDRICAL_SURFACE ( 'NONE', #42542, 20.00000000000000355 ) ;
#17320=CIRCLE ( 'NONE', #41654, 20.00000000000000355 ) ;
#17321=VERTEX_POINT ( 'NONE', #16935 ) ;
#17330=DIRECTION ( 'NONE',  ( -1.000000000000000000, 0.000000000000000000, -0.000000000000000000 ) ) ;
#17334=VERTEX_POINT ( 'NONE', #6635 ) ;
#17339=ORIENTED_EDGE ( 'NONE', *, *, #2446, .T. ) ;
#17345=ORIENTED_EDGE ( 'NONE', *, *, #1979, .T. ) ;
#17347=ORIENTED_EDGE ( 'NONE', *, *, #20808, .F. ) ;
#17365=ORIENTED_EDGE ( 'NONE', *, *, #34847, .T. ) ;
#17367=FACE_OUTER_BOUND ( 'NONE', #39444, .T. ) ;
#17372=EDGE_LOOP ( 'NONE', ( #28945, #27372, #19181, #11504 ) ) ;
#17392=CARTESIAN_POINT ( 'NONE',  ( 18.00000000000000355, 12.30077720129095198, 50.52416135122085450 ) ) ;
#17402=CYLINDRICAL_SURFACE ( 'NONE', #25281, 51.99999999999999289 ) ;
#17405=CIRCLE ( 'NONE', #23690, 47.49900000000000944 ) ;
#17410=ORIENTED_EDGE ( 'NONE', *, *, #20357, .F. ) ;
#17411=CARTESIAN_POINT ( 'NONE',  ( 18.00000000000000355, -46.87740477351715640, 16.82754413119429771 ) ) ;
#17416=DIRECTION ( 'NONE',  ( 0.000000000000000000, 0.3681245526846786964, -0.9297764858882511252 ) ) ;
#17418=ADVANCED_FACE ( 'NONE', ( #16501 ), #30438, .T. ) ;
#17419=EDGE_CURVE ( 'NONE', #18858, #909, #65, .T. ) ;
#17430=CARTESIAN_POINT ( 'NONE',  ( 0.000000000000000000, 0.000000000000000000, 0.000000000000000000 ) ) ;
#17434=AXIS2_PLACEMENT_3D ( 'NONE', #19803, #22658, #29837 ) ;
#17435=LINE ( 'NONE', #30277, #29756 ) ;
#17437=AXIS2_PLACEMENT_3D ( 'NONE', #33445, #36926, #29766 ) ;
#17439=ORIENTED_EDGE ( 'NONE', *, *, #30231, .T. ) ;
#17452=ORIENTED_EDGE ( 'NONE', *, *, #8804, .T. ) ;
#17454=ORIENTED_EDGE ( 'NONE', *, *, #11179, .F. ) ;
#17460=FACE_OUTER_BOUND ( 'NONE', #8295, .T. ) ;
#17462=ADVANCED_FACE ( 'NONE', ( #3768 ), #23262, .T. ) ;
#17463=VERTEX_POINT ( 'NONE', #4001 ) ;
#17473=ADVANCED_FACE ( 'NONE', ( #17148 ), #9712, .T. ) ;
#17482=DIRECTION ( 'NONE',  ( -1.000000000000000000, 0.000000000000000000, 0.000000000000000000 ) ) ;
#17485=AXIS2_PLACEMENT_3D ( 'NONE', #37429, #23943, #20248 ) ;
#17498=CARTESIAN_POINT ( 'NONE',  ( 0.000000000000000000, 0.000000000000000000, 0.000000000000000000 ) ) ;
#17528=CARTESIAN_POINT ( 'NONE',  ( 18.00000000000000355, 0.000000000000000000, 0.000000000000000000 ) ) ;
#17530=CIRCLE ( 'NONE', #25197, 51.99999999999999289 ) ;
#17531=DIRECTION ( 'NONE',  ( -1.000000000000000000, 0.000000000000000000, 0.000000000000000000 ) ) ;
#17539=DIRECTION ( 'NONE',  ( 0.000000000000000000, -6.938893903907226800E-15, 1.000000000000000000 ) ) ;
#17540=ORIENTED_EDGE ( 'NONE', *, *, #20951, .T. ) ;
#17543=FACE_OUTER_BOUND ( 'NONE', #21613, .T. ) ;
#17556=AXIS2_PLACEMENT_3D ( 'NONE', #37839, #7962, #18065 ) ;
#17566=DIRECTION ( 'NONE',  ( -1.000000000000000000, 0.000000000000000000, -0.000000000000000000 ) ) ;
#17576=EDGE_CURVE ( 'NONE', #38193, #22892, #18040, .T. ) ;
#17577=DIRECTION ( 'NONE',  ( -1.000000000000000000, 0.000000000000000000, 0.000000000000000000 ) ) ;
#17578=CYLINDRICAL_SURFACE ( 'NONE', #16379, 20.00000000000000711 ) ;
#17588=ORIENTED_EDGE ( 'NONE', *, *, #19654, .F. ) ;
#17619=AXIS2_PLACEMENT_3D ( 'NONE', #42305, #33139, #32499 ) ;
#17626=DIRECTION ( 'NONE',  ( -1.000000000000000000, -0.000000000000000000, -0.000000000000000000 ) ) ;
#17647=AXIS2_PLACEMENT_3D ( 'NONE', #41832, #31390, #31824 ) ;
#17656=EDGE_CURVE ( 'NONE', #1418, #11001, #2552, .T. ) ;
#17657=CYLINDRICAL_SURFACE ( 'NONE', #28217, 20.00000000000000355 ) ;
#17663=ORIENTED_EDGE ( 'NONE', *, *, #20270, .F. ) ;
#17675=DIRECTION ( 'NONE',  ( -1.000000000000000000, -0.000000000000000000, -0.000000000000000000 ) ) ;
#17676=CARTESIAN_POINT ( 'NONE',  ( 18.00000000000000355, 0.000000000000000000, 0.000000000000000000 ) ) ;
#17679=CARTESIAN_POINT ( 'NONE',  ( 0.000000000000000000, -36.05989434073635636, 30.12041790338605551 ) ) ;
#17682=CARTESIAN_POINT ( 'NONE',  ( 9.000000000000001776, -43.55304910509425298, 28.41006711799970574 ) ) ;
#17696=DIRECTION ( 'NONE',  ( -1.000000000000000000, -0.000000000000000000, -0.000000000000000000 ) ) ;
#17697=CIRCLE ( 'NONE', #32294, 20.00000000000000355 ) ;
#17709=ORIENTED_EDGE ( 'NONE', *, *, #7271, .F. ) ;
#17717=FACE_OUTER_BOUND ( 'NONE', #19799, .T. ) ;
#17728=DIRECTION ( 'NONE',  ( 0.000000000000000000, 0.6845471059286899473, -0.7289686274214103312 ) ) ;
#17732=CARTESIAN_POINT ( 'NONE',  ( 0.000000000000000000, 0.000000000000000000, 0.000000000000000000 ) ) ;
#17735=DIRECTION ( 'NONE',  ( 0.000000000000000000, 0.000000000000000000, -1.000000000000000000 ) ) ;
#17739=VERTEX_POINT ( 'NONE', #38897 ) ;
#17741=CARTESIAN_POINT ( 'NONE',  ( 18.00000000000000355, 0.000000000000000000, 0.000000000000000000 ) ) ;
#17749=AXIS2_PLACEMENT_3D ( 'NONE', #12996, #26302, #23049 ) ;
#17750=CARTESIAN_POINT ( 'NONE',  ( 18.00000000000000355, -47.49120266317494554, -0.8606222198180160099 ) ) ;
#17755=CIRCLE ( 'NONE', #4459, 51.99999999999999289 ) ;
#17777=EDGE_CURVE ( 'NONE', #19747, #26478, #25838, .T. ) ;
#17783=CARTESIAN_POINT ( 'NONE',  ( 18.00000000000000355, 44.47301969247445186, 16.68249143361925491 ) ) ;
#17785=CARTESIAN_POINT ( 'NONE',  ( 18.00000000000000355, -42.03146605346771025, -22.12489237027361000 ) ) ;
#17788=EDGE_LOOP ( 'NONE', ( #1503, #43180, #38563, #37309 ) ) ;
#17792=CARTESIAN_POINT ( 'NONE',  ( 18.00000000000000355, 13.85708833600031475, -45.43276465116650087 ) ) ;
#17806=DIRECTION ( 'NONE',  ( 0.000000000000000000, 0.000000000000000000, 1.000000000000000000 ) ) ;
#17810=VERTEX_POINT ( 'NONE', #2227 ) ;
#17816=ORIENTED_EDGE ( 'NONE', *, *, #23452, .T. ) ;
#17825=ORIENTED_EDGE ( 'NONE', *, *, #37441, .T. ) ;
#17827=EDGE_CURVE ( 'NONE', #1103, #4859, #9557, .T. ) ;
#17842=DIRECTION ( 'NONE',  ( -1.000000000000000000, -0.000000000000000000, 0.000000000000000000 ) ) ;
#17854=DIRECTION ( 'NONE',  ( -1.000000000000000000, 0.000000000000000000, 0.000000000000000000 ) ) ;
#17857=ORIENTED_EDGE ( 'NONE', *, *, #34845, .T. ) ;
#17860=CARTESIAN_POINT ( 'NONE',  ( 0.000000000000000000, 47.00885577955412487, 6.806061952192453468 ) ) ;
#17866=CIRCLE ( 'NONE', #42181, 20.00000000000000711 ) ;
#17882=CIRCLE ( 'NONE', #23434, 20.00000000000000355 ) ;
#17883=CIRCLE ( 'NONE', #31080, 20.00000000000000711 ) ;
#17889=ORIENTED_EDGE ( 'NONE', *, *, #7704, .F. ) ;
#17897=AXIS2_PLACEMENT_3D ( 'NONE', #31001, #10497, #437 ) ;
#17919=AXIS2_PLACEMENT_3D ( 'NONE', #32328, #18663, #5510 ) ;
#17924=DIRECTION ( 'NONE',  ( 0.000000000000000000, 0.000000000000000000, 1.000000000000000000 ) ) ;
#17925=ADVANCED_FACE ( 'NONE', ( #16439 ), #20167, .T. ) ;
#17928=AXIS2_PLACEMENT_3D ( 'NONE', #38102, #18951, #11743 ) ;
#17932=DIRECTION ( 'NONE',  ( 0.000000000000000000, 0.7705132427757861446, 0.6374239897486934092 ) ) ;
#17937=LINE ( 'NONE', #25277, #20753 ) ;
#17941=AXIS2_PLACEMENT_3D ( 'NONE', #5573, #29568, #35657 ) ;
#17955=CARTESIAN_POINT ( 'NONE',  ( 18.00000000000000355, -35.20873326984057883, -31.88259874184068465 ) ) ;
#17960=VECTOR ( 'NONE', #3364, 1000.000000000000000 ) ;
#17966=CARTESIAN_POINT ( 'NONE',  ( 0.000000000000000000, -26.17370628620627571, -39.63700417846190049 ) ) ;
#17980=ADVANCED_FACE ( 'NONE', ( #6580 ), #17097, .T. ) ;
#17982=AXIS2_PLACEMENT_3D ( 'NONE', #28265, #34345, #41309 ) ;
#17987=VERTEX_POINT ( 'NONE', #23215 ) ;
#17991=DIRECTION ( 'NONE',  ( -1.000000000000000000, -0.000000000000000000, 0.000000000000000000 ) ) ;
#17995=CIRCLE ( 'NONE', #23545, 47.49900000000000944 ) ;
#18011=ORIENTED_EDGE ( 'NONE', *, *, #20236, .T. ) ;
#18022=AXIS2_PLACEMENT_3D ( 'NONE', #19886, #32727, #2808 ) ;
#18024=ORIENTED_EDGE ( 'NONE', *, *, #33627, .F. ) ;
#18027=VECTOR ( 'NONE', #13879, 1000.000000000000000 ) ;
#18029=DIRECTION ( 'NONE',  ( 0.000000000000000000, 0.000000000000000000, -1.000000000000000000 ) ) ;
#18036=ORIENTED_EDGE ( 'NONE', *, *, #18277, .T. ) ;
#18037=AXIS2_PLACEMENT_3D ( 'NONE', #40468, #36780, #14117 ) ;
#18040=LINE ( 'NONE', #1600, #31153 ) ;
#18041=DIRECTION ( 'NONE',  ( -1.000000000000000000, -0.000000000000000000, -0.000000000000000000 ) ) ;
#18046=DIRECTION ( 'NONE',  ( -1.000000000000000000, 0.000000000000000000, 0.000000000000000000 ) ) ;
#18047=CYLINDRICAL_SURFACE ( 'NONE', #6748, 51.99999999999999289 ) ;
#18049=DIRECTION ( 'NONE',  ( -1.000000000000000000, -0.000000000000000000, -0.000000000000000000 ) ) ;
#18053=FACE_BOUND ( 'NONE', #11607, .T. ) ;
#18056=EDGE_CURVE ( 'NONE', #7995, #11400, #37414, .T. ) ;
#18057=AXIS2_PLACEMENT_3D ( 'NONE', #4395, #4621, #40607 ) ;
#18064=AXIS2_PLACEMENT_3D ( 'NONE', #39804, #40013, #6232 ) ;
#18065=DIRECTION ( 'NONE',  ( 0.000000000000000000, 0.000000000000000000, 1.000000000000000000 ) ) ;
#18080=AXIS2_PLACEMENT_3D ( 'NONE', #31421, #18153, #14854 ) ;
#18085=ORIENTED_EDGE ( 'NONE', *, *, #15250, .F. ) ;
#18088=CARTESIAN_POINT ( 'NONE',  ( 0.000000000000000000, 38.92705108641770551, -27.21837053747755419 ) ) ;
#18093=CYLINDRICAL_SURFACE ( 'NONE', #10978, 20.00000000000000711 ) ;
#18094=ORIENTED_EDGE ( 'NONE', *, *, #32544, .T. ) ;
#18095=DIRECTION ( 'NONE',  ( -1.000000000000000000, -0.000000000000000000, 0.000000000000000000 ) ) ;
#18097=CARTESIAN_POINT ( 'NONE',  ( 0.000000000000000000, 42.41764978026606769, 20.20639853260304619 ) ) ;
#18103=DIRECTION ( 'NONE',  ( -1.000000000000000000, 0.000000000000000000, 0.000000000000000000 ) ) ;
#18108=EDGE_CURVE ( 'NONE', #1020, #8971, #24959, .T. ) ;
#18119=CARTESIAN_POINT ( 'NONE',  ( 18.00000000000000355, 0.000000000000000000, 0.000000000000000000 ) ) ;
#18121=DIRECTION ( 'NONE',  ( -1.000000000000000000, 0.000000000000000000, 0.000000000000000000 ) ) ;
#18123=DIRECTION ( 'NONE',  ( 0.000000000000000000, -0.9048270524660235736, 0.4257792915650641108 ) ) ;
#18126=CARTESIAN_POINT ( 'NONE',  ( 0.000000000000000000, 0.2227391519123156360, -46.98410307550729215 ) ) ;
#18142=CIRCLE ( 'NONE', #11131, 20.00000000000000711 ) ;
#18143=ORIENTED_EDGE ( 'NONE', *, *, #9275, .F. ) ;
#18146=DIRECTION ( 'NONE',  ( 0.000000000000000000, 0.000000000000000000, 1.000000000000000000 ) ) ;
#18147=DIRECTION ( 'NONE',  ( 1.000000000000000000, -0.000000000000000000, 0.000000000000000000 ) ) ;
#18153=DIRECTION ( 'NONE',  ( -1.000000000000000000, 0.000000000000000000, -0.000000000000000000 ) ) ;
#18154=ORIENTED_EDGE ( 'NONE', *, *, #2954, .T. ) ;
#18158=EDGE_CURVE ( 'NONE', #27914, #7995, #7228, .T. ) ;
#18163=DIRECTION ( 'NONE',  ( -1.000000000000000000, 0.000000000000000000, 0.000000000000000000 ) ) ;
#18167=AXIS2_PLACEMENT_3D ( 'NONE', #783, #6699, #27432 ) ;
#18169=ORIENTED_EDGE ( 'NONE', *, *, #10827, .T. ) ;
#18170=AXIS2_PLACEMENT_3D ( 'NONE', #42343, #38861, #42119 ) ;
#18171=CARTESIAN_POINT ( 'NONE',  ( 18.00000000000000355, 49.65209126885762458, 15.44894276735567651 ) ) ;
#18173=ORIENTED_EDGE ( 'NONE', *, *, #36562, .T. ) ;
#18175=CARTESIAN_POINT ( 'NONE',  ( 0.000000000000000000, -43.55304910509424587, 28.41006711799970219 ) ) ;
#18191=VECTOR ( 'NONE', #18147, 1000.000000000000000 ) ;
#18197=DIRECTION ( 'NONE',  ( 1.000000000000000000, -0.000000000000000000, 0.000000000000000000 ) ) ;
#18217=CIRCLE ( 'NONE', #17485, 51.99999999999999289 ) ;
#18224=AXIS2_PLACEMENT_3D ( 'NONE', #25714, #38966, #25912 ) ;
#18225=AXIS2_PLACEMENT_3D ( 'NONE', #40409, #36714, #17122 ) ;
#18234=CARTESIAN_POINT ( 'NONE',  ( 18.00000000000000355, 27.43636312076321104, 38.14186064215159888 ) ) ;
#18237=EDGE_LOOP ( 'NONE', ( #2170, #1000, #24434, #25560 ) ) ;
#18241=ORIENTED_EDGE ( 'NONE', *, *, #37350, .T. ) ;
#18252=DIRECTION ( 'NONE',  ( -1.000000000000000000, -0.000000000000000000, -0.000000000000000000 ) ) ;
#18253=EDGE_LOOP ( 'NONE', ( #8156, #19477, #22588, #7804 ) ) ;
#18258=LINE ( 'NONE', #31523, #38168 ) ;
#18268=ORIENTED_EDGE ( 'NONE', *, *, #39788, .T. ) ;
#18277=EDGE_CURVE ( 'NONE', #23787, #11001, #1765, .T. ) ;
#18280=VERTEX_POINT ( 'NONE', #15970 ) ;
#18288=CARTESIAN_POINT ( 'NONE',  ( 18.00000000000000355, 0.000000000000000000, 0.000000000000000000 ) ) ;
#18294=DIRECTION ( 'NONE',  ( -1.000000000000000000, 0.000000000000000000, -0.000000000000000000 ) ) ;
#18302=ORIENTED_EDGE ( 'NONE', *, *, #569, .T. ) ;
#18307=DIRECTION ( 'NONE',  ( -1.000000000000000000, 0.000000000000000000, -0.000000000000000000 ) ) ;
#18314=CIRCLE ( 'NONE', #3622, 20.00000000000000711 ) ;
#18316=CARTESIAN_POINT ( 'NONE',  ( 0.000000000000000000, 13.56094713063571433, 50.20060470671744923 ) ) ;
#18323=CARTESIAN_POINT ( 'NONE',  ( 0.000000000000000000, 36.34385289850631295, -29.77717097092038756 ) ) ;
#18331=ADVANCED_FACE ( 'NONE', ( #35760 ), #41901, .T. ) ;
#18339=VERTEX_POINT ( 'NONE', #18838 ) ;
#18345=EDGE_CURVE ( 'NONE', #5490, #34783, #15238, .T. ) ;
#18354=CARTESIAN_POINT ( 'NONE',  ( -10.00000000000000000, 0.000000000000000000, 0.000000000000000000 ) ) ;
#18355=CARTESIAN_POINT ( 'NONE',  ( 18.00000000000000355, -32.32520163883607722, 34.09746168776025854 ) ) ;
#18359=FACE_OUTER_BOUND ( 'NONE', #38312, .T. ) ;
#18367=CARTESIAN_POINT ( 'NONE',  ( 0.000000000000000000, 46.87740477351718482, 16.82754413119463166 ) ) ;
#18370=EDGE_CURVE ( 'NONE', #30536, #14276, #38845, .T. ) ;
#18374=VERTEX_POINT ( 'NONE', #12890 ) ;
#18376=CARTESIAN_POINT ( 'NONE',  ( 0.000000000000000000, 17.50309955389674954, -43.60271849949345579 ) ) ;
#18378=CYLINDRICAL_SURFACE ( 'NONE', #27476, 20.00000000000000355 ) ;
#18392=LINE ( 'NONE', #11169, #30950 ) ;
#18395=EDGE_CURVE ( 'NONE', #32974, #36878, #37450, .T. ) ;
#18421=VERTEX_POINT ( 'NONE', #26198 ) ;
#18426=CARTESIAN_POINT ( 'NONE',  ( 18.00000000000000355, 0.000000000000000000, 0.000000000000000000 ) ) ;
#18427=AXIS2_PLACEMENT_3D ( 'NONE', #26298, #3114, #13809 ) ;
#18431=DIRECTION ( 'NONE',  ( 0.000000000000000000, 0.000000000000000000, 1.000000000000000000 ) ) ;
#18432=AXIS2_PLACEMENT_3D ( 'NONE', #18840, #23167, #6327 ) ;
#18433=CARTESIAN_POINT ( 'NONE',  ( 18.00000000000000355, 0.000000000000000000, 0.000000000000000000 ) ) ;
#18435=DIRECTION ( 'NONE',  ( 1.000000000000000000, 0.000000000000000000, -0.000000000000000000 ) ) ;
#18437=LINE ( 'NONE', #41283, #16452 ) ;
#18456=DIRECTION ( 'NONE',  ( 0.000000000000000000, 0.000000000000000000, 1.000000000000000000 ) ) ;
#18457=AXIS2_PLACEMENT_3D ( 'NONE', #12466, #7167, #167 ) ;
#18463=ORIENTED_EDGE ( 'NONE', *, *, #4641, .F. ) ;
#18466=EDGE_CURVE ( 'NONE', #26511, #18955, #25988, .T. ) ;
#18469=ORIENTED_EDGE ( 'NONE', *, *, #27559, .F. ) ;
#18481=AXIS2_PLACEMENT_3D ( 'NONE', #31810, #28968, #42239 ) ;
#18489=CARTESIAN_POINT ( 'NONE',  ( 18.00000000000000355, -46.90537658765333617, 2.727856614654147638 ) ) ;
#18522=LINE ( 'NONE', #35258, #12344 ) ;
#18546=VERTEX_POINT ( 'NONE', #40335 ) ;
#18552=DIRECTION ( 'NONE',  ( 0.000000000000000000, 0.000000000000000000, 1.000000000000000000 ) ) ;
#18553=VECTOR ( 'NONE', #38551, 1000.000000000000000 ) ;
#18555=ORIENTED_EDGE ( 'NONE', *, *, #36669, .T. ) ;
#18558=EDGE_CURVE ( 'NONE', #12961, #28114, #21511, .T. ) ;
#18568=DIRECTION ( 'NONE',  ( -1.000000000000000000, 0.000000000000000000, 0.000000000000000000 ) ) ;
#18589=CIRCLE ( 'NONE', #22769, 20.00000000000000711 ) ;
#18590=LINE ( 'NONE', #11579, #29820 ) ;
#18593=ORIENTED_EDGE ( 'NONE', *, *, #29903, .F. ) ;
#18600=CARTESIAN_POINT ( 'NONE',  ( 9.000000000000001776, -49.25004636492375454, -16.68630974939812006 ) ) ;
#18606=VECTOR ( 'NONE', #18869, 1000.000000000000000 ) ;
#18611=AXIS2_PLACEMENT_3D ( 'NONE', #39823, #2945, #32660 ) ;
#18620=CYLINDRICAL_SURFACE ( 'NONE', #3915, 20.00000000000000355 ) ;
#18621=CIRCLE ( 'NONE', #5329, 20.00000000000000000 ) ;
#18622=ORIENTED_EDGE ( 'NONE', *, *, #42234, .T. ) ;
#18627=DIRECTION ( 'NONE',  ( -1.000000000000000000, 0.000000000000000000, 0.000000000000000000 ) ) ;
#18645=ORIENTED_EDGE ( 'NONE', *, *, #11194, .F. ) ;
#18649=CARTESIAN_POINT ( 'NONE',  ( 18.00000000000000355, -34.03046037009278280, 33.13733193845793323 ) ) ;
#18652=ORIENTED_EDGE ( 'NONE', *, *, #605, .T. ) ;
#18660=ORIENTED_EDGE ( 'NONE', *, *, #33118, .T. ) ;
#18663=DIRECTION ( 'NONE',  ( -1.000000000000000000, 0.000000000000000000, 0.000000000000000000 ) ) ;
#18677=CIRCLE ( 'NONE', #11698, 20.00000000000000711 ) ;
#18692=ORIENTED_EDGE ( 'NONE', *, *, #22511, .F. ) ;
#18696=CARTESIAN_POINT ( 'NONE',  ( 0.000000000000000000, 0.000000000000000000, 0.000000000000000000 ) ) ;
#18699=CARTESIAN_POINT ( 'NONE',  ( 18.00000000000000355, 43.55304910509406113, 28.41006711800000062 ) ) ;
#18708=ORIENTED_EDGE ( 'NONE', *, *, #17151, .F. ) ;
#18712=AXIS2_PLACEMENT_3D ( 'NONE', #22524, #42100, #19038 ) ;
#18714=ADVANCED_FACE ( 'NONE', ( #5634 ), #21844, .T. ) ;
#18750=ORIENTED_EDGE ( 'NONE', *, *, #41298, .F. ) ;
#18754=CARTESIAN_POINT ( 'NONE',  ( 18.00000000000000355, 39.55064067543064965, 25.36340625197373555 ) ) ;
#18755=DIRECTION ( 'NONE',  ( -1.000000000000000000, 0.000000000000000000, 0.000000000000000000 ) ) ;
#18763=DIRECTION ( 'NONE',  ( 0.000000000000000000, 0.000000000000000000, 1.000000000000000000 ) ) ;
#18768=AXIS2_PLACEMENT_3D ( 'NONE', #6488, #23128, #6282 ) ;
#18771=DIRECTION ( 'NONE',  ( 0.000000000000000000, 0.000000000000000000, 1.000000000000000000 ) ) ;
#18776=EDGE_CURVE ( 'NONE', #35634, #23198, #22933, .T. ) ;
#18794=CARTESIAN_POINT ( 'NONE',  ( 18.00000000000000355, -17.08890430202782085, 43.76671000081940122 ) ) ;
#18798=ORIENTED_EDGE ( 'NONE', *, *, #29435, .F. ) ;
#18799=DIRECTION ( 'NONE',  ( -1.000000000000000000, -0.000000000000000000, 0.000000000000000000 ) ) ;
#18807=CARTESIAN_POINT ( 'NONE',  ( 18.00000000000000355, 2.123073309835852296, -47.45152853935331905 ) ) ;
#18812=ORIENTED_EDGE ( 'NONE', *, *, #22702, .T. ) ;
#18814=DIRECTION ( 'NONE',  ( 0.000000000000000000, 0.000000000000000000, -1.000000000000000000 ) ) ;
#18828=AXIS2_PLACEMENT_3D ( 'NONE', #21688, #28206, #24523 ) ;
#18832=ORIENTED_EDGE ( 'NONE', *, *, #16971, .T. ) ;
#18838=CARTESIAN_POINT ( 'NONE',  ( 18.00000000000000355, -13.56094713063537682, -50.20060470671753450 ) ) ;
#18839=EDGE_CURVE ( 'NONE', #4630, #4850, #23119, .T. ) ;
#18840=CARTESIAN_POINT ( 'NONE',  ( 18.00000000000000355, 39.55064067543099071, -25.36340625197318488 ) ) ;
#18848=EDGE_LOOP ( 'NONE', ( #18154, #7561, #31316, #10066 ) ) ;
#18858=VERTEX_POINT ( 'NONE', #26786 ) ;
#18861=ORIENTED_EDGE ( 'NONE', *, *, #7402, .F. ) ;
#18869=DIRECTION ( 'NONE',  ( -1.000000000000000000, 0.000000000000000000, 0.000000000000000000 ) ) ;
#18876=DIRECTION ( 'NONE',  ( 1.000000000000000000, 0.000000000000000000, -0.000000000000000000 ) ) ;
#18877=AXIS2_PLACEMENT_3D ( 'NONE', #17430, #30709, #27662 ) ;
#18881=ORIENTED_EDGE ( 'NONE', *, *, #9173, .F. ) ;
#18884=VERTEX_POINT ( 'NONE', #9562 ) ;
#18889=ADVANCED_FACE ( 'NONE', ( #23543 ), #2761, .T. ) ;
#18896=ORIENTED_EDGE ( 'NONE', *, *, #3884, .T. ) ;
#18898=ORIENTED_EDGE ( 'NONE', *, *, #30088, .F. ) ;
#18901=CARTESIAN_POINT ( 'NONE',  ( 18.00000000000000355, -46.87740477351715640, -3.172455868805708956 ) ) ;
#18915=CIRCLE ( 'NONE', #30736, 47.49900000000000944 ) ;
#18918=ORIENTED_EDGE ( 'NONE', *, *, #40, .T. ) ;
#18936=EDGE_LOOP ( 'NONE', ( #22277, #40130, #10621, #16698 ) ) ;
#18948=CARTESIAN_POINT ( 'NONE',  ( 18.00000000000000355, 46.87740477351718482, -3.172455868805370560 ) ) ;
#18951=DIRECTION ( 'NONE',  ( -1.000000000000000000, 0.000000000000000000, -0.000000000000000000 ) ) ;
#18952=DIRECTION ( 'NONE',  ( 0.000000000000000000, -0.9980267284282708928, -0.06279051952932446223 ) ) ;
#18953=ORIENTED_EDGE ( 'NONE', *, *, #6026, .T. ) ;
#18955=VERTEX_POINT ( 'NONE', #36367 ) ;
#18958=VECTOR ( 'NONE', #39249, 1000.000000000000000 ) ;
#18960=ORIENTED_EDGE ( 'NONE', *, *, #40878, .F. ) ;
#18972=DIRECTION ( 'NONE',  ( 0.000000000000000000, 0.6845471059286846183, 0.7289686274214153272 ) ) ;
#18977=DIRECTION ( 'NONE',  ( 0.000000000000000000, 0.9048270524660175784, 0.4257792915650767673 ) ) ;
#18992=EDGE_CURVE ( 'NONE', #37965, #3869, #11031, .T. ) ;
#19004=EDGE_CURVE ( 'NONE', #10253, #17463, #4674, .T. ) ;
#19011=ORIENTED_EDGE ( 'NONE', *, *, #33933, .F. ) ;
#19019=ORIENTED_EDGE ( 'NONE', *, *, #28081, .T. ) ;
#19020=DIRECTION ( 'NONE',  ( 0.000000000000000000, 0.000000000000000000, -1.000000000000000000 ) ) ;
#19033=ORIENTED_EDGE ( 'NONE', *, *, #40077, .T. ) ;
#19037=DIRECTION ( 'NONE',  ( 0.000000000000000000, -0.9510565162951500895, -0.3090169943749581094 ) ) ;
#19038=DIRECTION ( 'NONE',  ( 0.000000000000000000, 0.5877852522924742473, -0.8090169943749466741 ) ) ;
#19041=EDGE_CURVE ( 'NONE', #33051, #34436, #3360, .T. ) ;
#19048=EDGE_CURVE ( 'NONE', #32585, #10253, #36825, .T. ) ;
#19054=ORIENTED_EDGE ( 'NONE', *, *, #11595, .F. ) ;
#19056=EDGE_LOOP ( 'NONE', ( #3323, #9135, #7392, #8179 ) ) ;
#19060=CYLINDRICAL_SURFACE ( 'NONE', #37000, 47.49900000000000233 ) ;
#19063=CARTESIAN_POINT ( 'NONE',  ( 18.00000000000000355, 0.000000000000000000, 0.000000000000000000 ) ) ;
#19107=CARTESIAN_POINT ( 'NONE',  ( 9.000000000000001776, 0.6505223195690489346, -51.99593080916757515 ) ) ;
#19113=VERTEX_POINT ( 'NONE', #34342 ) ;
#19117=CIRCLE ( 'NONE', #23281, 20.00000000000000711 ) ;
#19125=DIRECTION ( 'NONE',  ( -1.000000000000000000, -0.000000000000000000, 0.000000000000000000 ) ) ;
#19134=ORIENTED_EDGE ( 'NONE', *, *, #15135, .T. ) ;
#19135=AXIS2_PLACEMENT_3D ( 'NONE', #14179, #20524, #13755 ) ;
#19137=ORIENTED_EDGE ( 'NONE', *, *, #5296, .T. ) ;
#19138=CYLINDRICAL_SURFACE ( 'NONE', #8936, 47.49900000000000233 ) ;
#19142=DIRECTION ( 'NONE',  ( 0.000000000000000000, -0.2486898871648622888, 0.9685831611286290777 ) ) ;
#19149=DIRECTION ( 'NONE',  ( 0.000000000000000000, 0.000000000000000000, 1.000000000000000000 ) ) ;
#19161=CARTESIAN_POINT ( 'NONE',  ( 0.000000000000000000, 24.72041153920732981, 40.55929306992697292 ) ) ;
#19170=DIRECTION ( 'NONE',  ( -1.000000000000000000, -0.000000000000000000, -0.000000000000000000 ) ) ;
#19172=EDGE_CURVE ( 'NONE', #27946, #8111, #4078, .T. ) ;
#19177=ORIENTED_EDGE ( 'NONE', *, *, #40167, .T. ) ;
#19181=ORIENTED_EDGE ( 'NONE', *, *, #8687, .F. ) ;
#19187=AXIS2_PLACEMENT_3D ( 'NONE', #5605, #5399, #18763 ) ;
#19195=AXIS2_PLACEMENT_3D ( 'NONE', #26771, #33959, #10620 ) ;
#19201=DIRECTION ( 'NONE',  ( 0.000000000000000000, 0.000000000000000000, 1.000000000000000000 ) ) ;
#19211=FACE_OUTER_BOUND ( 'NONE', #39396, .T. ) ;
#19217=ORIENTED_EDGE ( 'NONE', *, *, #11419, .F. ) ;
#19218=DIRECTION ( 'NONE',  ( 0.000000000000000000, -0.1253332335642905471, -0.9921147013144795412 ) ) ;
#19219=DIRECTION ( 'NONE',  ( -1.000000000000000000, 0.000000000000000000, 0.000000000000000000 ) ) ;
#19224=CARTESIAN_POINT ( 'NONE',  ( 18.00000000000000355, 0.000000000000000000, 0.000000000000000000 ) ) ;
#19226=CARTESIAN_POINT ( 'NONE',  ( -132.0000507999999968, 0.000000000000000000, 0.000000000000000000 ) ) ;
#19250=DIRECTION ( 'NONE',  ( 0.000000000000000000, 0.9822872507286892763, -0.1873813145857214368 ) ) ;
#19257=CARTESIAN_POINT ( 'NONE',  ( 18.00000000000000355, 46.87740477351718482, 16.82754413119463166 ) ) ;
#19260=DIRECTION ( 'NONE',  ( -1.000000000000000000, 0.000000000000000000, -0.000000000000000000 ) ) ;
#19263=LINE ( 'NONE', #18649, #13963 ) ;
#19273=CARTESIAN_POINT ( 'NONE',  ( 18.00000000000000355, 0.000000000000000000, 0.000000000000000000 ) ) ;
#19276=CARTESIAN_POINT ( 'NONE',  ( 18.00000000000000355, 0.000000000000000000, 0.000000000000000000 ) ) ;
#19278=AXIS2_PLACEMENT_3D ( 'NONE', #36152, #42690, #39421 ) ;
#19282=ORIENTED_EDGE ( 'NONE', *, *, #29664, .F. ) ;
#19295=DIRECTION ( 'NONE',  ( -1.000000000000000000, -0.000000000000000000, 0.000000000000000000 ) ) ;
#19303=CIRCLE ( 'NONE', #24162, 20.00000000000000000 ) ;
#19305=ORIENTED_EDGE ( 'NONE', *, *, #25989, .T. ) ;
#19314=CYLINDRICAL_SURFACE ( 'NONE', #28289, 20.00000000000000711 ) ;
#19316=CARTESIAN_POINT ( 'NONE',  ( 18.00000000000000355, 47.32430374665962347, -21.55018039121476647 ) ) ;
#19323=CIRCLE ( 'NONE', #453, 47.49900000000000233 ) ;
#19330=PRODUCT ( 'spur gear_iso_ISO - Spur gear 2M 50T 20PA 18FW ---S50B22H150L15.0N', 'spur gear_iso_ISO - Spur gear 2M 50T 20PA 18FW ---S50B22H150L15.0N', '', ( #32927 ) ) ;
#19333=DIRECTION ( 'NONE',  ( 0.000000000000000000, 0.000000000000000000, 1.000000000000000000 ) ) ;
#19334=DIRECTION ( 'NONE',  ( 0.000000000000000000, -0.9510565162951565288, 0.3090169943749382919 ) ) ;
#19343=CIRCLE ( 'NONE', #18064, 47.49900000000000233 ) ;
#19347=AXIS2_PLACEMENT_3D ( 'NONE', #36523, #12375, #19149 ) ;
#19365=CIRCLE ( 'NONE', #1191, 20.00000000000000711 ) ;
#19373=DIRECTION ( 'NONE',  ( 0.000000000000000000, -0.7705132427757817037, -0.6374239897486988493 ) ) ;
#19376=AXIS2_PLACEMENT_3D ( 'NONE', #1837, #15198, #35213 ) ;
#19404=AXIS2_PLACEMENT_3D ( 'NONE', #2621, #15981, #29278 ) ;
#19416=DIRECTION ( 'NONE',  ( -1.000000000000000000, 0.000000000000000000, 0.000000000000000000 ) ) ;
#19418=AXIS2_PLACEMENT_3D ( 'NONE', #19981, #23462, #14272 ) ;
#19427=ORIENTED_EDGE ( 'NONE', *, *, #37947, .T. ) ;
#19428=CARTESIAN_POINT ( 'NONE',  ( -10.00000000000000000, 0.000000000000000000, 0.000000000000000000 ) ) ;
#19429=AXIS2_PLACEMENT_3D ( 'NONE', #4392, #37349, #7470 ) ;
#19439=CARTESIAN_POINT ( 'NONE',  ( 0.000000000000000000, 25.61928775981044026, 45.25098998563485964 ) ) ;
#19441=CYLINDRICAL_SURFACE ( 'NONE', #35941, 20.00000000000000355 ) ;
#19445=EDGE_CURVE ( 'NONE', #32816, #23373, #10396, .T. ) ;
#19447=ORIENTED_EDGE ( 'NONE', *, *, #18056, .F. ) ;
#19448=DIRECTION ( 'NONE',  ( -1.000000000000000000, 0.000000000000000000, 0.000000000000000000 ) ) ;
#19454=CARTESIAN_POINT ( 'NONE',  ( 18.00000000000000355, 22.82995208772688756, 41.06517797613672371 ) ) ;
#19456=ORIENTED_EDGE ( 'NONE', *, *, #7317, .F. ) ;
#19466=DIRECTION ( 'NONE',  ( -1.000000000000000000, 0.000000000000000000, 0.000000000000000000 ) ) ;
#19477=ORIENTED_EDGE ( 'NONE', *, *, #18395, .T. ) ;
#19478=ORIENTED_EDGE ( 'NONE', *, *, #42316, .T. ) ;
#19489=DIRECTION ( 'NONE',  ( 0.000000000000000000, 0.000000000000000000, 1.000000000000000000 ) ) ;
#19490=DIRECTION ( 'NONE',  ( -1.000000000000000000, -0.000000000000000000, 0.000000000000000000 ) ) ;
#19494=EDGE_CURVE ( 'NONE', #35521, #25103, #27139, .T. ) ;
#19499=ORIENTED_EDGE ( 'NONE', *, *, #39345, .T. ) ;
#19500=DIRECTION ( 'NONE',  ( 0.000000000000000000, 0.9510565162951523099, 0.3090169943749515591 ) ) ;
#19506=CIRCLE ( 'NONE', #16809, 20.00000000000001066 ) ;
#19511=AXIS2_PLACEMENT_3D ( 'NONE', #39547, #9032, #9682 ) ;
#19531=ORIENTED_EDGE ( 'NONE', *, *, #22562, .F. ) ;
#19532=ADVANCED_FACE ( 'NONE', ( #17543 ), #4841, .T. ) ;
#19534=ORIENTED_EDGE ( 'NONE', *, *, #36669, .F. ) ;
#19539=VERTEX_POINT ( 'NONE', #1341 ) ;
#19541=AXIS2_PLACEMENT_3D ( 'NONE', #27221, #121, #24185 ) ;
#19546=VERTEX_POINT ( 'NONE', #21042 ) ;
#19555=VERTEX_POINT ( 'NONE', #24734 ) ;
#19559=CARTESIAN_POINT ( 'NONE',  ( 0.000000000000000000, -30.03615769709762517, 42.44795908868979950 ) ) ;
#19565=DIRECTION ( 'NONE',  ( -1.000000000000000000, 0.000000000000000000, 0.000000000000000000 ) ) ;
#19573=CARTESIAN_POINT ( 'NONE',  ( 18.00000000000000355, 0.000000000000000000, 0.000000000000000000 ) ) ;
#19577=CARTESIAN_POINT ( 'NONE',  ( 0.000000000000000000, 35.20873326984126805, -31.88259874183992792 ) ) ;
#19581=ORIENTED_EDGE ( 'NONE', *, *, #7650, .F. ) ;
#19595=ORIENTED_EDGE ( 'NONE', *, *, #33877, .F. ) ;
#19605=EDGE_CURVE ( 'NONE', #20337, #20302, #10742, .T. ) ;
#19608=AXIS2_PLACEMENT_3D ( 'NONE', #15704, #19628, #42280 ) ;
#19609=CARTESIAN_POINT ( 'NONE',  ( 0.000000000000000000, 47.22458491092827160, -5.098390039073737334 ) ) ;
#19614=ORIENTED_EDGE ( 'NONE', *, *, #15023, .F. ) ;
#19618=EDGE_CURVE ( 'NONE', #4417, #952, #41256, .T. ) ;
#19626=CIRCLE ( 'NONE', #7033, 52.00000000000000000 ) ;
#19628=DIRECTION ( 'NONE',  ( -1.000000000000000000, -0.000000000000000000, -0.000000000000000000 ) ) ;
#19637=DIRECTION ( 'NONE',  ( -1.000000000000000000, 0.000000000000000000, 0.000000000000000000 ) ) ;
#19638=AXIS2_PLACEMENT_3D ( 'NONE', #11515, #21593, #31573 ) ;
#19641=EDGE_LOOP ( 'NONE', ( #23098, #30894, #26738, #26990 ) ) ;
#19644=AXIS2_PLACEMENT_3D ( 'NONE', #14271, #33892, #10552 ) ;
#19645=DIRECTION ( 'NONE',  ( -1.000000000000000000, -0.000000000000000000, -0.000000000000000000 ) ) ;
#19648=CARTESIAN_POINT ( 'NONE',  ( 18.00000000000000355, -51.19683565102450729, 9.104066087303294807 ) ) ;
#19654=EDGE_CURVE ( 'NONE', #501, #21663, #14596, .T. ) ;
#19656=DIRECTION ( 'NONE',  ( 1.000000000000000000, -0.000000000000000000, -0.000000000000000000 ) ) ;
#19665=ORIENTED_EDGE ( 'NONE', *, *, #29006, .T. ) ;
#19680=DIRECTION ( 'NONE',  ( 0.000000000000000000, -0.7705132427757949154, 0.6374239897486827511 ) ) ;
#19691=ORIENTED_EDGE ( 'NONE', *, *, #7534, .T. ) ;
#19718=VECTOR ( 'NONE', #41392, 1000.000000000000000 ) ;
#19720=VERTEX_POINT ( 'NONE', #35150 ) ;
#19725=CARTESIAN_POINT ( 'NONE',  ( 18.00000000000000355, 11.90021268425555512, 45.45261810511218670 ) ) ;
#19728=DIRECTION ( 'NONE',  ( -1.000000000000000000, 0.000000000000000000, 0.000000000000000000 ) ) ;
#19733=VERTEX_POINT ( 'NONE', #12056 ) ;
#19734=EDGE_CURVE ( 'NONE', #37965, #5452, #18142, .T. ) ;
#19736=DIRECTION ( 'NONE',  ( -1.000000000000000000, 0.000000000000000000, -0.000000000000000000 ) ) ;
#19740=LINE ( 'NONE', #19107, #27018 ) ;
#19741=EDGE_LOOP ( 'NONE', ( #27086, #8093, #16552, #14806 ) ) ;
#19747=VERTEX_POINT ( 'NONE', #15756 ) ;
#19750=AXIS2_PLACEMENT_3D ( 'NONE', #34591, #40911, #1637 ) ;
#19753=CARTESIAN_POINT ( 'NONE',  ( 0.000000000000000000, -24.47917365149914204, -45.87777302070959706 ) ) ;
#19760=EDGE_LOOP ( 'NONE', ( #21140, #15384, #20277, #29234 ) ) ;
#19779=AXIS2_PLACEMENT_3D ( 'NONE', #27069, #30122, #7408 ) ;
#19793=VERTEX_POINT ( 'NONE', #3673 ) ;
#19795=DIRECTION ( 'NONE',  ( 1.000000000000000000, -0.000000000000000000, -0.000000000000000000 ) ) ;
#19799=EDGE_LOOP ( 'NONE', ( #17439, #10805, #39943, #16233 ) ) ;
#19801=DIRECTION ( 'NONE',  ( -1.000000000000000000, -0.000000000000000000, 0.000000000000000000 ) ) ;
#19803=CARTESIAN_POINT ( 'NONE',  ( 18.00000000000000355, -44.61570720899106846, 14.73072383765551940 ) ) ;
#19812=VERTEX_POINT ( 'NONE', #23813 ) ;
#19815=CYLINDRICAL_SURFACE ( 'NONE', #37298, 47.49900000000000233 ) ;
#19837=DIRECTION ( 'NONE',  ( 1.000000000000000000, -0.000000000000000000, -0.000000000000000000 ) ) ;
#19840=ORIENTED_EDGE ( 'NONE', *, *, #16142, .T. ) ;
#19843=LINE ( 'NONE', #16792, #15442 ) ;
#19847=CARTESIAN_POINT ( 'NONE',  ( 18.00000000000000355, -29.60891106212762125, -37.14118181634796656 ) ) ;
#19850=DIRECTION ( 'NONE',  ( -1.000000000000000000, -0.000000000000000000, -0.000000000000000000 ) ) ;
#19852=DIRECTION ( 'NONE',  ( -1.000000000000000000, -0.000000000000000000, -0.000000000000000000 ) ) ;
#19857=ORIENTED_EDGE ( 'NONE', *, *, #25694, .F. ) ;
#19859=DIRECTION ( 'NONE',  ( -1.000000000000000000, 0.000000000000000000, 0.000000000000000000 ) ) ;
#19860=CARTESIAN_POINT ( 'NONE',  ( 18.00000000000000355, 27.43636312076376527, -38.14186064215121519 ) ) ;
#19876=EDGE_CURVE ( 'NONE', #13970, #27094, #33402, .T. ) ;
#19877=DIRECTION ( 'NONE',  ( -1.000000000000000000, -0.000000000000000000, -0.000000000000000000 ) ) ;
#19880=EDGE_CURVE ( 'NONE', #30171, #24364, #36193, .T. ) ;
#19885=VECTOR ( 'NONE', #55, 1000.000000000000000 ) ;
#19886=CARTESIAN_POINT ( 'NONE',  ( 18.00000000000000355, 0.000000000000000000, 0.000000000000000000 ) ) ;
#19888=LINE ( 'NONE', #841, #12821 ) ;
#19903=AXIS2_PLACEMENT_3D ( 'NONE', #10123, #23693, #30212 ) ;
#19911=ORIENTED_EDGE ( 'NONE', *, *, #35361, .T. ) ;
#19912=DIRECTION ( 'NONE',  ( 1.000000000000000000, -0.000000000000000000, -0.000000000000000000 ) ) ;
#19926=AXIS2_PLACEMENT_3D ( 'NONE', #19224, #35739, #28397 ) ;
#19932=CIRCLE ( 'NONE', #1067, 20.00000000000000355 ) ;
#19934=ADVANCED_FACE ( 'NONE', ( #7414 ), #14418, .T. ) ;
#19937=CARTESIAN_POINT ( 'NONE',  ( 0.000000000000000000, 0.000000000000000000, 0.000000000000000000 ) ) ;
#19941=ORIENTED_EDGE ( 'NONE', *, *, #20947, .F. ) ;
#19956=DIRECTION ( 'NONE',  ( -1.000000000000000000, 0.000000000000000000, 0.000000000000000000 ) ) ;
#19967=ORIENTED_EDGE ( 'NONE', *, *, #27345, .T. ) ;
#19977=CIRCLE ( 'NONE', #1111, 20.00000000000000711 ) ;
#19978=EDGE_LOOP ( 'NONE', ( #10063, #9636, #24652, #23560 ) ) ;
#19980=DIRECTION ( 'NONE',  ( 0.000000000000000000, 0.000000000000000000, 1.000000000000000000 ) ) ;
#19981=CARTESIAN_POINT ( 'NONE',  ( 18.00000000000000355, 0.000000000000000000, 0.000000000000000000 ) ) ;
#19984=CARTESIAN_POINT ( 'NONE',  ( 0.000000000000000000, 51.93417535146740249, 2.615612846549354664 ) ) ;
#19991=CARTESIAN_POINT ( 'NONE',  ( 18.00000000000000355, 0.000000000000000000, 0.000000000000000000 ) ) ;
#19993=VERTEX_POINT ( 'NONE', #846 ) ;
#19998=VECTOR ( 'NONE', #22159, 1000.000000000000000 ) ;
#19999=EDGE_LOOP ( 'NONE', ( #21113, #10549, #19840, #2313 ) ) ;
#20004=DIRECTION ( 'NONE',  ( -1.000000000000000000, 0.000000000000000000, 0.000000000000000000 ) ) ;
#20006=DIRECTION ( 'NONE',  ( 0.000000000000000000, 0.000000000000000000, 1.000000000000000000 ) ) ;
#20011=CIRCLE ( 'NONE', #10928, 51.99999999999999289 ) ;
#20020=EDGE_CURVE ( 'NONE', #39452, #8913, #14199, .T. ) ;
#20021=CARTESIAN_POINT ( 'NONE',  ( 0.000000000000000000, -22.82995208772658557, -41.06517797613689424 ) ) ;
#20028=CYLINDRICAL_SURFACE ( 'NONE', #39044, 51.99999999999999289 ) ;
#20031=CARTESIAN_POINT ( 'NONE',  ( 18.00000000000000355, -44.75336757549789013, 14.30704879393590012 ) ) ;
#20035=DIRECTION ( 'NONE',  ( -1.000000000000000000, -0.000000000000000000, 0.000000000000000000 ) ) ;
#20039=FACE_OUTER_BOUND ( 'NONE', #11593, .T. ) ;
#20040=ORIENTED_EDGE ( 'NONE', *, *, #41748, .T. ) ;
#20045=DIRECTION ( 'NONE',  ( -1.000000000000000000, 0.000000000000000000, -0.000000000000000000 ) ) ;
#20072=ADVANCED_FACE ( 'NONE', ( #8059 ), #4796, .T. ) ;
#20086=ORIENTED_EDGE ( 'NONE', *, *, #35757, .T. ) ;
#20092=VECTOR ( 'NONE', #6176, 1000.000000000000000 ) ;
#20093=CARTESIAN_POINT ( 'NONE',  ( 18.00000000000000355, 42.41764978026607480, -20.20639853260305685 ) ) ;
#20097=CYLINDRICAL_SURFACE ( 'NONE', #34215, 20.00000000000000000 ) ;
#20099=ORIENTED_EDGE ( 'NONE', *, *, #37764, .F. ) ;
#20101=CARTESIAN_POINT ( 'NONE',  ( 0.000000000000000000, 43.55304910509406824, 28.41006711800000062 ) ) ;
#20102=CARTESIAN_POINT ( 'NONE',  ( 0.000000000000000000, 44.75336757549779776, 14.30704879393622164 ) ) ;
#20110=EDGE_CURVE ( 'NONE', #17062, #8370, #8702, .T. ) ;
#20115=CARTESIAN_POINT ( 'NONE',  ( 18.00000000000000355, 0.000000000000000000, 0.000000000000000000 ) ) ;
#20118=LINE ( 'NONE', #1716, #3475 ) ;
#20130=AXIS2_PLACEMENT_3D ( 'NONE', #31260, #7678, #31676 ) ;
#20133=LINE ( 'NONE', #16641, #2585 ) ;
#20140=CARTESIAN_POINT ( 'NONE',  ( 0.000000000000000000, -47.49120266317495975, 0.8606222198173691940 ) ) ;
#20148=CIRCLE ( 'NONE', #6862, 20.00000000000000711 ) ;
#20159=DIRECTION ( 'NONE',  ( 1.000000000000000000, -0.000000000000000000, -0.000000000000000000 ) ) ;
#20160=VERTEX_POINT ( 'NONE', #12640 ) ;
#20167=CYLINDRICAL_SURFACE ( 'NONE', #13783, 20.00000000000000355 ) ;
#20169=EDGE_CURVE ( 'NONE', #16736, #4843, #20148, .T. ) ;
#20170=EDGE_LOOP ( 'NONE', ( #3295, #24775, #40706, #9074 ) ) ;
#20171=DIRECTION ( 'NONE',  ( -1.000000000000000000, -0.000000000000000000, -0.000000000000000000 ) ) ;
#20177=AXIS2_PLACEMENT_3D ( 'NONE', #5162, #18755, #32424 ) ;
#20186=VERTEX_POINT ( 'NONE', #12437 ) ;
#20190=ADVANCED_FACE ( 'NONE', ( #35727 ), #39008, .T. ) ;
#20198=DIRECTION ( 'NONE',  ( 0.000000000000000000, 0.2486898871648553500, -0.9685831611286310761 ) ) ;
#20199=DIRECTION ( 'NONE',  ( 0.000000000000000000, 0.000000000000000000, 1.000000000000000000 ) ) ;
#20201=CARTESIAN_POINT ( 'NONE',  ( 9.000000000000001776, 44.25018368420781911, -27.31155879685132604 ) ) ;
#20204=CYLINDRICAL_SURFACE ( 'NONE', #32370, 47.49900000000000233 ) ;
#20210=ORIENTED_EDGE ( 'NONE', *, *, #11833, .F. ) ;
#20219=DIRECTION ( 'NONE',  ( 0.000000000000000000, -0.9048270524660235736, 0.4257792915650641663 ) ) ;
#20229=DIRECTION ( 'NONE',  ( -1.000000000000000000, -0.000000000000000000, 0.000000000000000000 ) ) ;
#20230=EDGE_CURVE ( 'NONE', #11400, #34568, #40065, .T. ) ;
#20236=EDGE_CURVE ( 'NONE', #8971, #33317, #13725, .T. ) ;
#20248=DIRECTION ( 'NONE',  ( 0.000000000000000000, 0.000000000000000000, 1.000000000000000000 ) ) ;
#20256=EDGE_CURVE ( 'NONE', #12073, #1655, #36168, .T. ) ;
#20266=DIRECTION ( 'NONE',  ( 0.000000000000000000, 0.000000000000000000, 1.000000000000000000 ) ) ;
#20270=EDGE_CURVE ( 'NONE', #39541, #18421, #26386, .T. ) ;
#20277=ORIENTED_EDGE ( 'NONE', *, *, #36157, .T. ) ;
#20279=ORIENTED_EDGE ( 'NONE', *, *, #322, .T. ) ;
#20299=DIRECTION ( 'NONE',  ( -1.000000000000000000, 0.000000000000000000, 0.000000000000000000 ) ) ;
#20302=VERTEX_POINT ( 'NONE', #2769 ) ;
#20310=EDGE_CURVE ( 'NONE', #18884, #12306, #29646, .T. ) ;
#20312=EDGE_CURVE ( 'NONE', #6385, #16988, #42925, .T. ) ;
#20323=EDGE_CURVE ( 'NONE', #21384, #1441, #29434, .T. ) ;
#20325=VECTOR ( 'NONE', #26531, 1000.000000000000000 ) ;
#20329=ORIENTED_EDGE ( 'NONE', *, *, #28780, .F. ) ;
#20337=VERTEX_POINT ( 'NONE', #36377 ) ;
#20345=CARTESIAN_POINT ( 'NONE',  ( 0.000000000000000000, -51.85248208264520287, 3.914090171286016773 ) ) ;
#20348=CARTESIAN_POINT ( 'NONE',  ( 0.000000000000000000, 0.000000000000000000, 0.000000000000000000 ) ) ;
#20357=EDGE_CURVE ( 'NONE', #15352, #9771, #4788, .T. ) ;
#20362=CARTESIAN_POINT ( 'NONE',  ( 18.00000000000000355, 0.000000000000000000, 0.000000000000000000 ) ) ;
#20368=EDGE_CURVE ( 'NONE', #6747, #24285, #12471, .T. ) ;
#20369=VERTEX_POINT ( 'NONE', #36589 ) ;
#20370=CARTESIAN_POINT ( 'NONE',  ( 18.00000000000000355, 36.34385289850631295, -29.77717097092038756 ) ) ;
#20383=CIRCLE ( 'NONE', #11306, 20.00000000000000711 ) ;
#20392=EDGE_LOOP ( 'NONE', ( #39666, #13085, #35192, #3881 ) ) ;
#20405=DIRECTION ( 'NONE',  ( -1.000000000000000000, 0.000000000000000000, 0.000000000000000000 ) ) ;
#20409=EDGE_CURVE ( 'NONE', #29751, #39905, #15963, .T. ) ;
#20410=ORIENTED_EDGE ( 'NONE', *, *, #21536, .F. ) ;
#20413=DIRECTION ( 'NONE',  ( -1.000000000000000000, -0.000000000000000000, 0.000000000000000000 ) ) ;
#20421=AXIS2_PLACEMENT_3D ( 'NONE', #1963, #12036, #21874 ) ;
#20431=VERTEX_POINT ( 'NONE', #11300 ) ;
#20434=CARTESIAN_POINT ( 'NONE',  ( 0.000000000000000000, -50.95304419620816816, -10.38206564895716255 ) ) ;
#20442=VERTEX_POINT ( 'NONE', #21373 ) ;
#20457=FACE_OUTER_BOUND ( 'NONE', #1163, .T. ) ;
#20467=EDGE_LOOP ( 'NONE', ( #35159, #25358, #22776, #27595 ) ) ;
#20468=CARTESIAN_POINT ( 'NONE',  ( 0.000000000000000000, 0.000000000000000000, 0.000000000000000000 ) ) ;
#20471=CIRCLE ( 'NONE', #10661, 20.00000000000000355 ) ;
#20481=ORIENTED_EDGE ( 'NONE', *, *, #3159, .T. ) ;
#20497=CARTESIAN_POINT ( 'NONE',  ( 0.000000000000000000, -38.92705108641711576, -27.21837053747839263 ) ) ;
#20501=EDGE_CURVE ( 'NONE', #14470, #10268, #22232, .T. ) ;
#20502=CIRCLE ( 'NONE', #18427, 51.99999999999999289 ) ;
#20504=CIRCLE ( 'NONE', #13512, 20.00000000000000355 ) ;
#20510=DIRECTION ( 'NONE',  ( 0.000000000000000000, 0.000000000000000000, 1.000000000000000000 ) ) ;
#20514=DIRECTION ( 'NONE',  ( 1.000000000000000000, -0.000000000000000000, -0.000000000000000000 ) ) ;
#20515=CARTESIAN_POINT ( 'NONE',  ( 9.000000000000001776, 40.47821179127761582, -32.64221760512715775 ) ) ;
#20517=DIRECTION ( 'NONE',  ( 0.000000000000000000, 0.000000000000000000, 1.000000000000000000 ) ) ;
#20524=DIRECTION ( 'NONE',  ( -1.000000000000000000, 0.000000000000000000, 0.000000000000000000 ) ) ;
#20546=EDGE_CURVE ( 'NONE', #16328, #23341, #32684, .T. ) ;
#20547=ADVANCED_FACE ( 'NONE', ( #42012 ), #35683, .T. ) ;
#20552=EDGE_CURVE ( 'NONE', #1020, #1396, #38748, .T. ) ;
#20557=DIRECTION ( 'NONE',  ( -1.000000000000000000, 0.000000000000000000, 0.000000000000000000 ) ) ;
#20560=DIRECTION ( 'NONE',  ( -1.000000000000000000, -0.000000000000000000, 0.000000000000000000 ) ) ;
#20569=VERTEX_POINT ( 'NONE', #22008 ) ;
#20571=CARTESIAN_POINT ( 'NONE',  ( 18.00000000000000355, -13.85708833599937861, -45.43276465116677798 ) ) ;
#20573=ORIENTED_EDGE ( 'NONE', *, *, #31027, .F. ) ;
#20583=AXIS2_PLACEMENT_3D ( 'NONE', #28792, #12209, #38568 ) ;
#20589=CARTESIAN_POINT ( 'NONE',  ( 18.00000000000000355, 3.840921266749842022, 47.34345070675171030 ) ) ;
#20602=EDGE_LOOP ( 'NONE', ( #37645, #21501, #28321, #1391 ) ) ;
#20612=VECTOR ( 'NONE', #11157, 1000.000000000000000 ) ;
#20617=CARTESIAN_POINT ( 'NONE',  ( 18.00000000000000355, -5.667686777401384823, -46.64153600743609474 ) ) ;
#20618=ORIENTED_EDGE ( 'NONE', *, *, #8169, .F. ) ;
#20625=DIRECTION ( 'NONE',  ( -1.000000000000000000, -0.000000000000000000, 0.000000000000000000 ) ) ;
#20628=ORIENTED_EDGE ( 'NONE', *, *, #7879, .F. ) ;
#20631=CARTESIAN_POINT ( 'NONE',  ( 18.00000000000000355, 0.000000000000000000, 0.000000000000000000 ) ) ;
#20643=DIRECTION ( 'NONE',  ( 0.000000000000000000, 0.1253332335642974305, 0.9921147013144787641 ) ) ;
#20649=DIRECTION ( 'NONE',  ( -1.000000000000000000, 0.000000000000000000, 0.000000000000000000 ) ) ;
#20656=VECTOR ( 'NONE', #30812, 1000.000000000000000 ) ;
#20660=DIRECTION ( 'NONE',  ( -1.000000000000000000, 0.000000000000000000, 0.000000000000000000 ) ) ;
#20665=DIRECTION ( 'NONE',  ( 0.000000000000000000, 0.000000000000000000, 1.000000000000000000 ) ) ;
#20669=EDGE_CURVE ( 'NONE', #18884, #16540, #13182, .T. ) ;
#20677=AXIS2_PLACEMENT_3D ( 'NONE', #18126, #21614, #41171 ) ;
#20678=DIRECTION ( 'NONE',  ( -1.000000000000000000, 0.000000000000000000, 0.000000000000000000 ) ) ;
#20688=DIRECTION ( 'NONE',  ( 0.000000000000000000, -0.9822872507286865007, -0.1873813145857356199 ) ) ;
#20691=LINE ( 'NONE', #33316, #36510 ) ;
#20695=EDGE_CURVE ( 'NONE', #14972, #23617, #40329, .T. ) ;
#20697=CARTESIAN_POINT ( 'NONE',  ( -10.00000000000000000, 0.000000000000000000, 0.000000000000000000 ) ) ;
#20707=DIRECTION ( 'NONE',  ( -1.000000000000000000, 0.000000000000000000, 0.000000000000000000 ) ) ;
#20708=DIRECTION ( 'NONE',  ( -1.000000000000000000, -0.000000000000000000, -0.000000000000000000 ) ) ;
#20721=CYLINDRICAL_SURFACE ( 'NONE', #42933, 20.00000000000000355 ) ;
#20725=AXIS2_PLACEMENT_3D ( 'NONE', #39020, #19219, #15092 ) ;
#20729=CARTESIAN_POINT ( 'NONE',  ( 0.000000000000000000, 0.000000000000000000, 0.000000000000000000 ) ) ;
#20737=ORIENTED_EDGE ( 'NONE', *, *, #25060, .F. ) ;
#20749=AXIS2_PLACEMENT_3D ( 'NONE', #29702, #19260, #6770 ) ;
#20753=VECTOR ( 'NONE', #22005, 1000.000000000000000 ) ;
#20757=CIRCLE ( 'NONE', #10241, 52.00000000000000000 ) ;
#20759=EDGE_CURVE ( 'NONE', #18280, #11061, #26413, .T. ) ;
#20766=DIRECTION ( 'NONE',  ( 0.000000000000000000, 0.000000000000000000, 1.000000000000000000 ) ) ;
#20773=CARTESIAN_POINT ( 'NONE',  ( 18.00000000000000355, 0.000000000000000000, 0.000000000000000000 ) ) ;
#20777=DIRECTION ( 'NONE',  ( 0.000000000000000000, 0.4817536741017163782, -0.8763066800438630288 ) ) ;
#20778=DIRECTION ( 'NONE',  ( -1.000000000000000000, -0.000000000000000000, 0.000000000000000000 ) ) ;
#20779=ORIENTED_EDGE ( 'NONE', *, *, #25180, .T. ) ;
#20793=DIRECTION ( 'NONE',  ( -1.000000000000000000, 0.000000000000000000, 0.000000000000000000 ) ) ;
#20796=VECTOR ( 'NONE', #3161, 1000.000000000000000 ) ;
#20808=EDGE_CURVE ( 'NONE', #14470, #42813, #16686, .T. ) ;
#20810=EDGE_CURVE ( 'NONE', #8390, #13064, #3386, .T. ) ;
#20817=EDGE_CURVE ( 'NONE', #16988, #36583, #1345, .T. ) ;
#20818=AXIS2_PLACEMENT_3D ( 'NONE', #12295, #2011, #39280 ) ;
#20839=ORIENTED_EDGE ( 'NONE', *, *, #24981, .T. ) ;
#20851=CARTESIAN_POINT ( 'NONE',  ( 0.000000000000000000, 30.03615769709792005, -42.44795908868957923 ) ) ;
#20852=ORIENTED_EDGE ( 'NONE', *, *, #19172, .F. ) ;
#20855=CIRCLE ( 'NONE', #32635, 20.00000000000000711 ) ;
#20860=ORIENTED_EDGE ( 'NONE', *, *, #7317, .T. ) ;
#20861=FACE_OUTER_BOUND ( 'NONE', #3620, .T. ) ;
#20876=ADVANCED_FACE ( 'NONE', ( #26966 ), #40242, .T. ) ;
#20877=VERTEX_POINT ( 'NONE', #3578 ) ;
#20878=DIRECTION ( 'NONE',  ( -1.000000000000000000, 0.000000000000000000, 0.000000000000000000 ) ) ;
#20885=DIRECTION ( 'NONE',  ( 0.000000000000000000, 0.000000000000000000, 1.000000000000000000 ) ) ;
#20888=LINE ( 'NONE', #5108, #35628 ) ;
#20910=CARTESIAN_POINT ( 'NONE',  ( 0.000000000000000000, -47.00885577955406802, -6.806061952192774989 ) ) ;
#20913=DIRECTION ( 'NONE',  ( 0.000000000000000000, 0.000000000000000000, 1.000000000000000000 ) ) ;
#20917=EDGE_LOOP ( 'NONE', ( #352, #33079, #38012, #14524 ) ) ;
#20935=DIRECTION ( 'NONE',  ( 0.000000000000000000, -0.9510565162951565288, 0.3090169943749383474 ) ) ;
#20937=DIRECTION ( 'NONE',  ( 0.000000000000000000, -0.8443279255020087470, -0.5358267949790064266 ) ) ;
#20942=CARTESIAN_POINT ( 'NONE',  ( 18.00000000000000355, -9.744342220503709129, 46.48873837489794880 ) ) ;
#20945=ORIENTED_EDGE ( 'NONE', *, *, #30506, .T. ) ;
#20946=DIRECTION ( 'NONE',  ( -1.000000000000000000, -0.000000000000000000, 0.000000000000000000 ) ) ;
#20947=EDGE_CURVE ( 'NONE', #39644, #22227, #16717, .T. ) ;
#20948=ORIENTED_EDGE ( 'NONE', *, *, #15000, .F. ) ;
#20951=EDGE_CURVE ( 'NONE', #23124, #1418, #17405, .T. ) ;
#20959=CARTESIAN_POINT ( 'NONE',  ( -10.00000000000000000, 0.000000000000000000, 0.000000000000000000 ) ) ;
#20964=CARTESIAN_POINT ( 'NONE',  ( 18.00000000000000355, -29.60891106212812574, 37.14118181634756155 ) ) ;
#20969=DIRECTION ( 'NONE',  ( 0.000000000000000000, 0.000000000000000000, 1.000000000000000000 ) ) ;
#20974=EDGE_CURVE ( 'NONE', #12278, #25059, #10421, .T. ) ;
#20985=ORIENTED_EDGE ( 'NONE', *, *, #33469, .F. ) ;
#20993=AXIS2_PLACEMENT_3D ( 'NONE', #38386, #28602, #22072 ) ;
#21015=AXIS2_PLACEMENT_3D ( 'NONE', #14070, #7055, #262 ) ;
#21017=ORIENTED_EDGE ( 'NONE', *, *, #22975, .T. ) ;
#21019=CARTESIAN_POINT ( 'NONE',  ( 0.000000000000000000, 0.000000000000000000, 0.000000000000000000 ) ) ;
#21026=DIRECTION ( 'NONE',  ( 0.000000000000000000, 0.000000000000000000, -1.000000000000000000 ) ) ;
#21038=CARTESIAN_POINT ( 'NONE',  ( 0.000000000000000000, -42.41764978026621691, 20.20639853260276197 ) ) ;
#21039=ORIENTED_EDGE ( 'NONE', *, *, #15339, .F. ) ;
#21042=CARTESIAN_POINT ( 'NONE',  ( 18.00000000000000355, 47.49120266317495265, 0.8606222198176843863 ) ) ;
#21047=EDGE_LOOP ( 'NONE', ( #29239, #41131, #8798, #11552 ) ) ;
#21055=EDGE_CURVE ( 'NONE', #6447, #40171, #32016, .T. ) ;
#21064=DIRECTION ( 'NONE',  ( 0.000000000000000000, 0.000000000000000000, -1.000000000000000000 ) ) ;
#21071=CARTESIAN_POINT ( 'NONE',  ( 0.000000000000000000, 0.000000000000000000, 0.000000000000000000 ) ) ;
#21081=AXIS2_PLACEMENT_3D ( 'NONE', #37537, #7645, #24933 ) ;
#21090=VERTEX_POINT ( 'NONE', #3060 ) ;
#21098=ORIENTED_EDGE ( 'NONE', *, *, #1300, .T. ) ;
#21109=ADVANCED_FACE ( 'NONE', ( #37975 ), #30600, .T. ) ;
#21110=CARTESIAN_POINT ( 'NONE',  ( 18.00000000000000355, 41.20225022064636278, 23.63323037071415911 ) ) ;
#21113=ORIENTED_EDGE ( 'NONE', *, *, #20020, .T. ) ;
#21114=CIRCLE ( 'NONE', #14834, 52.00000000000000000 ) ;
#21128=DIRECTION ( 'NONE',  ( 0.000000000000000000, 0.000000000000000000, 1.000000000000000000 ) ) ;
#21131=VERTEX_POINT ( 'NONE', #1331 ) ;
#21140=ORIENTED_EDGE ( 'NONE', *, *, #38912, .T. ) ;
#21149=ORIENTED_EDGE ( 'NONE', *, *, #33951, .T. ) ;
#21150=CARTESIAN_POINT ( 'NONE',  ( 9.000000000000001776, -13.56094713063606783, 50.20060470671735686 ) ) ;
#21153=AXIS2_PLACEMENT_3D ( 'NONE', #31396, #7605, #1480 ) ;
#21161=CARTESIAN_POINT ( 'NONE',  ( 18.00000000000000355, -22.82995208772658557, -41.06517797613689424 ) ) ;
#21163=LINE ( 'NONE', #199, #16134 ) ;
#21165=DIRECTION ( 'NONE',  ( 1.000000000000000000, 0.000000000000000000, 0.000000000000000000 ) ) ;
#21166=EDGE_CURVE ( 'NONE', #15350, #2405, #35913, .T. ) ;
#21168=CARTESIAN_POINT ( 'NONE',  ( 18.00000000000000355, 39.55064067543064965, 25.36340625197373555 ) ) ;
#21172=EDGE_CURVE ( 'NONE', #35521, #25440, #34717, .T. ) ;
#21183=AXIS2_PLACEMENT_3D ( 'NONE', #33312, #3397, #30055 ) ;
#21188=EDGE_CURVE ( 'NONE', #31882, #2747, #14338, .T. ) ;
#21189=DIRECTION ( 'NONE',  ( -1.000000000000000000, -0.000000000000000000, -0.000000000000000000 ) ) ;
#21196=DIRECTION ( 'NONE',  ( 0.000000000000000000, 0.000000000000000000, 1.000000000000000000 ) ) ;
#21219=DIRECTION ( 'NONE',  ( 0.000000000000000000, -0.8443279255020200713, 0.5358267949789887741 ) ) ;
#21222=CARTESIAN_POINT ( 'NONE',  ( 0.000000000000000000, 0.000000000000000000, 0.000000000000000000 ) ) ;
#21229=DIRECTION ( 'NONE',  ( 0.000000000000000000, 0.000000000000000000, 1.000000000000000000 ) ) ;
#21237=DIRECTION ( 'NONE',  ( -1.000000000000000000, 0.000000000000000000, -0.000000000000000000 ) ) ;
#21264=ORIENTED_EDGE ( 'NONE', *, *, #15961, .T. ) ;
#21266=AXIS2_PLACEMENT_3D ( 'NONE', #28100, #41362, #20935 ) ;
#21272=DIRECTION ( 'NONE',  ( -1.000000000000000000, -0.000000000000000000, 0.000000000000000000 ) ) ;
#21275=CIRCLE ( 'NONE', #24758, 20.00000000000000711 ) ;
#21283=CARTESIAN_POINT ( 'NONE',  ( 18.00000000000000355, 40.47821179127715396, 32.64221760512772619 ) ) ;
#21284=ORIENTED_EDGE ( 'NONE', *, *, #4821, .F. ) ;
#21288=AXIS2_PLACEMENT_3D ( 'NONE', #18794, #22270, #32048 ) ;
#21289=CARTESIAN_POINT ( 'NONE',  ( 18.00000000000000355, 0.000000000000000000, 0.000000000000000000 ) ) ;
#21301=DIRECTION ( 'NONE',  ( 0.000000000000000000, 0.8443279255020126328, 0.5358267949790005424 ) ) ;
#21306=DIRECTION ( 'NONE',  ( 0.000000000000000000, -0.3681245526846653737, -0.9297764858882564543 ) ) ;
#21309=CARTESIAN_POINT ( 'NONE',  ( 18.00000000000000355, 35.20873326984126805, -31.88259874183992792 ) ) ;
#21310=ORIENTED_EDGE ( 'NONE', *, *, #1849, .T. ) ;
#21322=DIRECTION ( 'NONE',  ( 1.000000000000000000, 0.000000000000000000, 0.000000000000000000 ) ) ;
#21326=AXIS2_PLACEMENT_3D ( 'NONE', #36743, #7282, #20643 ) ;
#21340=DIRECTION ( 'NONE',  ( 0.000000000000000000, -0.6845471059286792892, -0.7289686274214203232 ) ) ;
#21346=LINE ( 'NONE', #27649, #7999 ) ;
#21349=CIRCLE ( 'NONE', #15746, 20.00000000000000711 ) ;
#21356=EDGE_CURVE ( 'NONE', #952, #38711, #3816, .T. ) ;
#21369=CARTESIAN_POINT ( 'NONE',  ( 0.000000000000000000, 0.000000000000000000, 0.000000000000000000 ) ) ;
#21370=ORIENTED_EDGE ( 'NONE', *, *, #7276, .F. ) ;
#21373=CARTESIAN_POINT ( 'NONE',  ( 18.00000000000000355, -5.871425383721165403, -51.66745943012288222 ) ) ;
#21384=VERTEX_POINT ( 'NONE', #31667 ) ;
#21395=DIRECTION ( 'NONE',  ( 0.000000000000000000, 0.000000000000000000, 1.000000000000000000 ) ) ;
#21431=ORIENTED_EDGE ( 'NONE', *, *, #1550, .F. ) ;
#21434=CARTESIAN_POINT ( 'NONE',  ( 18.00000000000000355, -2.123073309834832667, -47.45152853935337589 ) ) ;
#21438=VERTEX_POINT ( 'NONE', #5263 ) ;
#21442=DIRECTION ( 'NONE',  ( 1.000000000000000000, 0.000000000000000000, 0.000000000000000000 ) ) ;
#21443=VERTEX_POINT ( 'NONE', #41034 ) ;
#21445=CARTESIAN_POINT ( 'NONE',  ( 0.000000000000000000, 42.60732521687599217, -19.80331771201614544 ) ) ;
#21446=CARTESIAN_POINT ( 'NONE',  ( 0.000000000000000000, -49.65209126885751800, -15.44894276735603356 ) ) ;
#21449=CYLINDRICAL_SURFACE ( 'NONE', #21081, 20.00000000000000355 ) ;
#21454=ORIENTED_EDGE ( 'NONE', *, *, #4766, .T. ) ;
#21459=FACE_OUTER_BOUND ( 'NONE', #6243, .T. ) ;
#21463=LINE ( 'NONE', #29465, #2416 ) ;
#21465=EDGE_LOOP ( 'NONE', ( #19019, #31555, #1471, #19478 ) ) ;
#21472=VECTOR ( 'NONE', #34997, 1000.000000000000000 ) ;
#21476=EDGE_CURVE ( 'NONE', #12372, #13830, #41469, .T. ) ;
#21491=ORIENTED_EDGE ( 'NONE', *, *, #1300, .F. ) ;
#21493=DIRECTION ( 'NONE',  ( 0.000000000000000000, 0.000000000000000000, 1.000000000000000000 ) ) ;
#21501=ORIENTED_EDGE ( 'NONE', *, *, #39545, .T. ) ;
#21511=CIRCLE ( 'NONE', #33287, 52.00000000000000000 ) ;
#21515=DIRECTION ( 'NONE',  ( -1.000000000000000000, 0.000000000000000000, 0.000000000000000000 ) ) ;
#21516=CIRCLE ( 'NONE', #37456, 20.00000000000000711 ) ;
#21536=EDGE_CURVE ( 'NONE', #31395, #21384, #20504, .T. ) ;
#21538=DIRECTION ( 'NONE',  ( -1.000000000000000000, 0.000000000000000000, 0.000000000000000000 ) ) ;
#21549=ORIENTED_EDGE ( 'NONE', *, *, #21797, .T. ) ;
#21553=DIRECTION ( 'NONE',  ( -1.000000000000000000, 0.000000000000000000, 0.000000000000000000 ) ) ;
#21562=EDGE_CURVE ( 'NONE', #15819, #17013, #1115, .T. ) ;
#21563=EDGE_CURVE ( 'NONE', #30041, #27914, #27424, .T. ) ;
#21565=ORIENTED_EDGE ( 'NONE', *, *, #27559, .T. ) ;
#21574=VERTEX_POINT ( 'NONE', #39248 ) ;
#21577=ORIENTED_EDGE ( 'NONE', *, *, #20546, .T. ) ;
#21578=CYLINDRICAL_SURFACE ( 'NONE', #43046, 51.99999999999999289 ) ;
#21588=CARTESIAN_POINT ( 'NONE',  ( -132.0000507999999968, 1.347111479062088405E-15, 11.00000000000000000 ) ) ;
#21590=ORIENTED_EDGE ( 'NONE', *, *, #39009, .T. ) ;
#21592=ORIENTED_EDGE ( 'NONE', *, *, #26033, .F. ) ;
#21593=DIRECTION ( 'NONE',  ( 1.000000000000000000, 0.000000000000000000, 0.000000000000000000 ) ) ;
#21597=CARTESIAN_POINT ( 'NONE',  ( 18.00000000000000355, 0.000000000000000000, 0.000000000000000000 ) ) ;
#21601=CARTESIAN_POINT ( 'NONE',  ( 0.000000000000000000, 9.744342220503391161, 46.48873837489801275 ) ) ;
#21603=LINE ( 'NONE', #34853, #38623 ) ;
#21609=CARTESIAN_POINT ( 'NONE',  ( 18.00000000000000355, -17.08890430202782085, 43.76671000081940122 ) ) ;
#21611=EDGE_CURVE ( 'NONE', #1993, #24221, #15541, .T. ) ;
#21613=EDGE_LOOP ( 'NONE', ( #6396, #42291, #32081, #3967 ) ) ;
#21614=DIRECTION ( 'NONE',  ( 1.000000000000000000, 0.000000000000000000, 0.000000000000000000 ) ) ;
#21627=ORIENTED_EDGE ( 'NONE', *, *, #21476, .F. ) ;
#21632=DIRECTION ( 'NONE',  ( 0.000000000000000000, 0.000000000000000000, 1.000000000000000000 ) ) ;
#21637=ORIENTED_EDGE ( 'NONE', *, *, #29001, .T. ) ;
#21643=ORIENTED_EDGE ( 'NONE', *, *, #43155, .T. ) ;
#21660=LINE ( 'NONE', #865, #9188 ) ;
#21663=VERTEX_POINT ( 'NONE', #28836 ) ;
#21664=DIRECTION ( 'NONE',  ( -1.000000000000000000, 0.000000000000000000, 0.000000000000000000 ) ) ;
#21678=AXIS2_PLACEMENT_3D ( 'NONE', #10819, #43093, #36537 ) ;
#21688=CARTESIAN_POINT ( 'NONE',  ( 18.00000000000000355, 0.000000000000000000, 0.000000000000000000 ) ) ;
#21690=EDGE_LOOP ( 'NONE', ( #17816, #41145, #34526, #7941 ) ) ;
#21697=LINE ( 'NONE', #24535, #9015 ) ;
#21700=ORIENTED_EDGE ( 'NONE', *, *, #18466, .F. ) ;
#21724=CARTESIAN_POINT ( 'NONE',  ( 18.00000000000000355, 41.20225022064669673, -23.63323037071358357 ) ) ;
#21735=CARTESIAN_POINT ( 'NONE',  ( 18.00000000000000355, 0.000000000000000000, 0.000000000000000000 ) ) ;
#21741=CARTESIAN_POINT ( 'NONE',  ( 18.00000000000000355, 46.21320724403648939, 10.97699764141968970 ) ) ;
#21743=EDGE_CURVE ( 'NONE', #755, #10605, #6966, .T. ) ;
#21744=CARTESIAN_POINT ( 'NONE',  ( 0.000000000000000000, 0.000000000000000000, 0.000000000000000000 ) ) ;
#21747=CARTESIAN_POINT ( 'NONE',  ( 18.00000000000000355, 17.08890430202814059, -43.76671000081927332 ) ) ;
#21749=DIRECTION ( 'NONE',  ( 0.000000000000000000, 0.9822872507286893873, -0.1873813145857213536 ) ) ;
#21752=DIRECTION ( 'NONE',  ( 0.000000000000000000, 0.000000000000000000, 1.000000000000000000 ) ) ;
#21755=ORIENTED_EDGE ( 'NONE', *, *, #23392, .F. ) ;
#21760=CARTESIAN_POINT ( 'NONE',  ( 9.000000000000001776, -47.32430374665947426, 21.55018039121509688 ) ) ;
#21761=EDGE_CURVE ( 'NONE', #4058, #501, #19888, .T. ) ;
#21781=ORIENTED_EDGE ( 'NONE', *, *, #7062, .F. ) ;
#21787=CARTESIAN_POINT ( 'NONE',  ( 18.00000000000000355, 39.55064067543099071, -25.36340625197318488 ) ) ;
#21788=CARTESIAN_POINT ( 'NONE',  ( 18.00000000000000355, -44.61570720899084819, -14.73072383765613047 ) ) ;
#21796=EDGE_CURVE ( 'NONE', #755, #37085, #38549, .T. ) ;
#21797=EDGE_CURVE ( 'NONE', #3449, #3154, #3893, .T. ) ;
#21801=ORIENTED_EDGE ( 'NONE', *, *, #5161, .F. ) ;
#21806=VERTEX_POINT ( 'NONE', #3668 ) ;
#21811=DIRECTION ( 'NONE',  ( 0.000000000000000000, 0.000000000000000000, 1.000000000000000000 ) ) ;
#21812=DIRECTION ( 'NONE',  ( 1.000000000000000000, 0.000000000000000000, 0.000000000000000000 ) ) ;
#21844=CYLINDRICAL_SURFACE ( 'NONE', #7524, 20.00000000000000355 ) ;
#21846=ADVANCED_FACE ( 'NONE', ( #10468 ), #23808, .T. ) ;
#21849=DIRECTION ( 'NONE',  ( 1.000000000000000000, -0.000000000000000000, 0.000000000000000000 ) ) ;
#21862=ORIENTED_EDGE ( 'NONE', *, *, #18466, .T. ) ;
#21871=AXIS2_PLACEMENT_3D ( 'NONE', #15051, #34652, #41180 ) ;
#21874=DIRECTION ( 'NONE',  ( 0.000000000000000000, -0.4817536741017036661, -0.8763066800438700232 ) ) ;
#21875=DIRECTION ( 'NONE',  ( 0.000000000000000000, 0.000000000000000000, 1.000000000000000000 ) ) ;
#21882=AXIS2_PLACEMENT_3D ( 'NONE', #449, #23046, #21229 ) ;
#21884=VECTOR ( 'NONE', #18197, 1000.000000000000000 ) ;
#21885=FACE_OUTER_BOUND ( 'NONE', #34071, .T. ) ;
#21899=DIRECTION ( 'NONE',  ( -1.000000000000000000, -0.000000000000000000, 0.000000000000000000 ) ) ;
#21903=VERTEX_POINT ( 'NONE', #41198 ) ;
#21911=CARTESIAN_POINT ( 'NONE',  ( 0.000000000000000000, 20.99948489194481738, -42.60488980472760545 ) ) ;
#21916=CARTESIAN_POINT ( 'NONE',  ( 0.000000000000000000, 49.25004636492389665, 16.68630974939776834 ) ) ;
#21936=CARTESIAN_POINT ( 'NONE',  ( 18.00000000000000355, 0.000000000000000000, 0.000000000000000000 ) ) ;
#21943=CIRCLE ( 'NONE', #7976, 20.00000000000000355 ) ;
#21951=FACE_OUTER_BOUND ( 'NONE', #7255, .T. ) ;
#21955=ADVANCED_FACE ( 'NONE', ( #15297 ), #38160, .T. ) ;
#21957=ORIENTED_EDGE ( 'NONE', *, *, #19004, .T. ) ;
#21958=DIRECTION ( 'NONE',  ( -1.000000000000000000, -0.000000000000000000, -0.000000000000000000 ) ) ;
#21972=ORIENTED_EDGE ( 'NONE', *, *, #37441, .F. ) ;
#21994=CARTESIAN_POINT ( 'NONE',  ( 18.00000000000000355, 46.77034588191303044, 22.72740077717245910 ) ) ;
#21995=ORIENTED_EDGE ( 'NONE', *, *, #7647, .T. ) ;
#21999=AXIS2_PLACEMENT_3D ( 'NONE', #28127, #35499, #18552 ) ;
#22005=DIRECTION ( 'NONE',  ( 1.000000000000000000, -0.000000000000000000, -0.000000000000000000 ) ) ;
#22008=CARTESIAN_POINT ( 'NONE',  ( 18.00000000000000355, -34.03046037009278280, 33.13733193845793323 ) ) ;
#22016=DIRECTION ( 'NONE',  ( 0.000000000000000000, 0.000000000000000000, 1.000000000000000000 ) ) ;
#22037=VERTEX_POINT ( 'NONE', #5004 ) ;
#22038=CYLINDRICAL_SURFACE ( 'NONE', #16990, 51.99999999999999289 ) ;
#22044=ORIENTED_EDGE ( 'NONE', *, *, #42234, .F. ) ;
#22051=AXIS2_PLACEMENT_3D ( 'NONE', #4414, #27153, #3751 ) ;
#22052=CARTESIAN_POINT ( 'NONE',  ( 0.000000000000000000, 2.123073309835852296, -47.45152853935331905 ) ) ;
#22055=DIRECTION ( 'NONE',  ( -1.000000000000000000, 0.000000000000000000, 0.000000000000000000 ) ) ;
#22057=ADVANCED_FACE ( 'NONE', ( #18359 ), #41647, .T. ) ;
#22072=DIRECTION ( 'NONE',  ( 0.000000000000000000, 0.000000000000000000, 1.000000000000000000 ) ) ;
#22077=DIRECTION ( 'NONE',  ( 0.000000000000000000, 0.9822872507286893873, -0.1873813145857213536 ) ) ;
#22078=PRODUCT_DEFINITION_CONTEXT ( 'detailed design', #14514, 'design' ) ;
#22113=ORIENTED_EDGE ( 'NONE', *, *, #35560, .F. ) ;
#22128=VECTOR ( 'NONE', #24412, 1000.000000000000000 ) ;
#22129=LINE ( 'NONE', #8553, #7329 ) ;
#22134=VECTOR ( 'NONE', #11921, 1000.000000000000000 ) ;
#22138=DIRECTION ( 'NONE',  ( 0.000000000000000000, 0.9048270524660176894, 0.4257792915650767118 ) ) ;
#22140=EDGE_CURVE ( 'NONE', #31470, #6447, #29010, .T. ) ;
#22141=CARTESIAN_POINT ( 'NONE',  ( 18.00000000000000355, 24.47917365149946889, 45.87777302070943364 ) ) ;
#22147=FACE_OUTER_BOUND ( 'NONE', #39125, .T. ) ;
#22155=ORIENTED_EDGE ( 'NONE', *, *, #7347, .F. ) ;
#22159=DIRECTION ( 'NONE',  ( -1.000000000000000000, 0.000000000000000000, 0.000000000000000000 ) ) ;
#22162=AXIS2_PLACEMENT_3D ( 'NONE', #34132, #7732, #3776 ) ;
#22167=ORIENTED_EDGE ( 'NONE', *, *, #14770, .T. ) ;
#22171=CARTESIAN_POINT ( 'NONE',  ( 0.000000000000000000, 0.000000000000000000, 0.000000000000000000 ) ) ;
#22174=ADVANCED_FACE ( 'NONE', ( #42278 ), #38575, .T. ) ;
#22192=LINE ( 'NONE', #4917, #22134 ) ;
#22198=( NAMED_UNIT ( * ) SI_UNIT ( $, .STERADIAN. ) SOLID_ANGLE_UNIT ( ) );
#22201=VECTOR ( 'NONE', #16306, 1000.000000000000000 ) ;
#22204=FACE_OUTER_BOUND ( 'NONE', #137, .T. ) ;
#22207=DIRECTION ( 'NONE',  ( 0.000000000000000000, 0.000000000000000000, 1.000000000000000000 ) ) ;
#22212=CIRCLE ( 'NONE', #33997, 20.00000000000000000 ) ;
#22220=DIRECTION ( 'NONE',  ( 0.000000000000000000, 0.3681245526846786964, -0.9297764858882511252 ) ) ;
#22221=CIRCLE ( 'NONE', #39559, 7.500000000000000000 ) ;
#22227=VERTEX_POINT ( 'NONE', #40501 ) ;
#22231=CARTESIAN_POINT ( 'NONE',  ( 9.000000000000001776, 49.25004636492388244, 16.68630974939776834 ) ) ;
#22232=LINE ( 'NONE', #34841, #29216 ) ;
#22240=CARTESIAN_POINT ( 'NONE',  ( 18.00000000000000355, -49.25004636492376164, -16.68630974939811651 ) ) ;
#22250=DIRECTION ( 'NONE',  ( -1.000000000000000000, 0.000000000000000000, 0.000000000000000000 ) ) ;
#22257=DIRECTION ( 'NONE',  ( 0.000000000000000000, 0.000000000000000000, 1.000000000000000000 ) ) ;
#22258=EDGE_LOOP ( 'NONE', ( #12915, #37004, #18918, #34586 ) ) ;
#22264=EDGE_LOOP ( 'NONE', ( #25201, #29781, #26338, #12876 ) ) ;
#22270=DIRECTION ( 'NONE',  ( -1.000000000000000000, 0.000000000000000000, 0.000000000000000000 ) ) ;
#22272=AXIS2_PLACEMENT_3D ( 'NONE', #13026, #16290, #19373 ) ;
#22273=CARTESIAN_POINT ( 'NONE',  ( 18.00000000000000355, 50.95304419620838132, -10.38206564895608786 ) ) ;
#22277=ORIENTED_EDGE ( 'NONE', *, *, #8866, .F. ) ;
#22286=CARTESIAN_POINT ( 'NONE',  ( 18.00000000000000355, 46.77034588191335729, -22.72740077717179474 ) ) ;
#22287=ORIENTED_EDGE ( 'NONE', *, *, #26625, .T. ) ;
#22291=CARTESIAN_POINT ( 'NONE',  ( 18.00000000000000355, 0.000000000000000000, 51.99999999999999289 ) ) ;
#22297=ORIENTED_EDGE ( 'NONE', *, *, #42674, .T. ) ;
#22305=DIRECTION ( 'NONE',  ( 0.000000000000000000, 0.000000000000000000, 1.000000000000000000 ) ) ;
#22307=VERTEX_POINT ( 'NONE', #37239 ) ;
#22308=CYLINDRICAL_SURFACE ( 'NONE', #25505, 20.00000000000000355 ) ;
#22314=DIRECTION ( 'NONE',  ( -1.000000000000000000, -0.000000000000000000, -0.000000000000000000 ) ) ;
#22319=EDGE_LOOP ( 'NONE', ( #21264, #1158, #34575, #13455 ) ) ;
#22326=EDGE_CURVE ( 'NONE', #41828, #21131, #35821, .T. ) ;
#22350=AXIS2_PLACEMENT_3D ( 'NONE', #41414, #25322, #1713 ) ;
#22353=CIRCLE ( 'NONE', #40416, 20.00000000000000355 ) ;
#22357=ORIENTED_EDGE ( 'NONE', *, *, #34915, .F. ) ;
#22380=ORIENTED_EDGE ( 'NONE', *, *, #1131, .F. ) ;
#22384=FACE_OUTER_BOUND ( 'NONE', #37592, .T. ) ;
#22385=VECTOR ( 'NONE', #32432, 1000.000000000000000 ) ;
#22389=CIRCLE ( 'NONE', #10540, 20.00000000000001066 ) ;
#22391=AXIS2_PLACEMENT_3D ( 'NONE', #12864, #19645, #32911 ) ;
#22394=CIRCLE ( 'NONE', #27953, 47.49900000000000233 ) ;
#22395=EDGE_CURVE ( 'NONE', #33958, #4060, #22653, .T. ) ;
#22406=FACE_OUTER_BOUND ( 'NONE', #37098, .T. ) ;
#22423=AXIS2_PLACEMENT_3D ( 'NONE', #40314, #43159, #10448 ) ;
#22426=ORIENTED_EDGE ( 'NONE', *, *, #7710, .F. ) ;
#22430=ORIENTED_EDGE ( 'NONE', *, *, #34223, .T. ) ;
#22433=EDGE_CURVE ( 'NONE', #2044, #22037, #24049, .T. ) ;
#22449=ADVANCED_FACE ( 'NONE', ( #24198 ), #38107, .T. ) ;
#22451=VECTOR ( 'NONE', #28271, 1000.000000000000000 ) ;
#22455=ORIENTED_EDGE ( 'NONE', *, *, #35361, .F. ) ;
#22461=CYLINDRICAL_SURFACE ( 'NONE', #9291, 47.49900000000000233 ) ;
#22462=ORIENTED_EDGE ( 'NONE', *, *, #12858, .F. ) ;
#22465=CARTESIAN_POINT ( 'NONE',  ( 9.000000000000001776, 36.06787431788676912, 37.45808914225501951 ) ) ;
#22474=LINE ( 'NONE', #16784, #42931 ) ;
#22482=DIRECTION ( 'NONE',  ( -1.000000000000000000, -0.000000000000000000, 0.000000000000000000 ) ) ;
#22489=DIRECTION ( 'NONE',  ( 0.000000000000000000, 0.000000000000000000, 1.000000000000000000 ) ) ;
#22490=ADVANCED_FACE ( 'NONE', ( #27672 ), #17657, .T. ) ;
#22497=DIRECTION ( 'NONE',  ( 0.000000000000000000, 0.6845471059286899473, -0.7289686274214103312 ) ) ;
#22508=DIRECTION ( 'NONE',  ( 0.000000000000000000, 0.000000000000000000, 1.000000000000000000 ) ) ;
#22511=EDGE_CURVE ( 'NONE', #23668, #9628, #21943, .T. ) ;
#22519=EDGE_CURVE ( 'NONE', #23124, #16711, #23331, .T. ) ;
#22524=CARTESIAN_POINT ( 'NONE',  ( 18.00000000000000355, 22.43957647427161461, 41.27978878573636479 ) ) ;
#22531=DIRECTION ( 'NONE',  ( 0.000000000000000000, 0.2486898871648552389, -0.9685831611286309650 ) ) ;
#22532=LINE ( 'NONE', #2614, #43052 ) ;
#22535=DIRECTION ( 'NONE',  ( 0.000000000000000000, 0.000000000000000000, 1.000000000000000000 ) ) ;
#22555=FACE_OUTER_BOUND ( 'NONE', #12780, .T. ) ;
#22562=EDGE_CURVE ( 'NONE', #37276, #7995, #13575, .T. ) ;
#22570=FILL_AREA_STYLE ('',( #15796 ) ) ;
#22572=CARTESIAN_POINT ( 'NONE',  ( 18.00000000000000355, -27.79676263918163315, -37.88001506494799031 ) ) ;
#22580=CARTESIAN_POINT ( 'NONE',  ( 18.00000000000000355, -46.21320724403641833, -10.97699764142002188 ) ) ;
#22581=ORIENTED_EDGE ( 'NONE', *, *, #4307, .T. ) ;
#22584=AXIS2_PLACEMENT_3D ( 'NONE', #35407, #5723, #28672 ) ;
#22587=FACE_OUTER_BOUND ( 'NONE', #35341, .T. ) ;
#22588=ORIENTED_EDGE ( 'NONE', *, *, #42000, .F. ) ;
#22590=ORIENTED_EDGE ( 'NONE', *, *, #41748, .F. ) ;
#22602=CYLINDRICAL_SURFACE ( 'NONE', #23099, 19.99999999999999645 ) ;
#22610=DIRECTION ( 'NONE',  ( 0.000000000000000000, -0.5877852522924624790, -0.8090169943749551118 ) ) ;
#22613=CARTESIAN_POINT ( 'NONE',  ( 18.00000000000000355, 17.50309955389674954, -43.60271849949345579 ) ) ;
#22619=DIRECTION ( 'NONE',  ( -1.000000000000000000, 0.000000000000000000, 0.000000000000000000 ) ) ;
#22625=AXIS2_PLACEMENT_3D ( 'NONE', #38795, #22482, #28795 ) ;
#22627=CARTESIAN_POINT ( 'NONE',  ( 18.00000000000000355, -49.25004636492399612, 16.68630974939742018 ) ) ;
#22628=LINE ( 'NONE', #36097, #27638 ) ;
#22634=DIRECTION ( 'NONE',  ( -1.000000000000000000, -0.000000000000000000, 0.000000000000000000 ) ) ;
#22637=CARTESIAN_POINT ( 'NONE',  ( 18.00000000000000355, 11.46872990052444408, -45.56340405422433548 ) ) ;
#22640=CARTESIAN_POINT ( 'NONE',  ( 18.00000000000000355, -42.03146605346771025, -22.12489237027361000 ) ) ;
#22646=ORIENTED_EDGE ( 'NONE', *, *, #35990, .T. ) ;
#22651=CARTESIAN_POINT ( 'NONE',  ( 18.00000000000000355, -39.78933988720098114, -24.98727647985043276 ) ) ;
#22653=CIRCLE ( 'NONE', #34440, 47.49900000000000233 ) ;
#22654=VERTEX_POINT ( 'NONE', #9724 ) ;
#22658=DIRECTION ( 'NONE',  ( -1.000000000000000000, 0.000000000000000000, 0.000000000000000000 ) ) ;
#22661=VERTEX_POINT ( 'NONE', #20434 ) ;
#22669=EDGE_CURVE ( 'NONE', #11369, #20569, #30319, .T. ) ;
#22671=AXIS2_PLACEMENT_3D ( 'NONE', #20031, #43098, #26340 ) ;
#22680=CIRCLE ( 'NONE', #8688, 20.00000000000000000 ) ;
#22685=EDGE_CURVE ( 'NONE', #2260, #28849, #10823, .T. ) ;
#22686=DIRECTION ( 'NONE',  ( -1.000000000000000000, -0.000000000000000000, -0.000000000000000000 ) ) ;
#22695=VECTOR ( 'NONE', #30597, 1000.000000000000000 ) ;
#22698=CYLINDRICAL_SURFACE ( 'NONE', #40539, 51.99999999999999289 ) ;
#22702=EDGE_CURVE ( 'NONE', #21663, #14485, #29815, .T. ) ;
#22709=CARTESIAN_POINT ( 'NONE',  ( 18.00000000000000355, 0.000000000000000000, 0.000000000000000000 ) ) ;
#22714=LINE ( 'NONE', #42714, #29377 ) ;
#22716=ORIENTED_EDGE ( 'NONE', *, *, #17777, .T. ) ;
#22717=DIRECTION ( 'NONE',  ( 0.000000000000000000, 0.000000000000000000, 1.000000000000000000 ) ) ;
#22720=EDGE_CURVE ( 'NONE', #3516, #21806, #8006, .T. ) ;
#22721=CARTESIAN_POINT ( 'NONE',  ( 0.000000000000000000, 0.000000000000000000, 0.000000000000000000 ) ) ;
#22731=AXIS2_PLACEMENT_3D ( 'NONE', #20631, #17577, #24342 ) ;
#22737=CARTESIAN_POINT ( 'NONE',  ( 0.000000000000000000, -36.05989434073592292, -30.12041790338656710 ) ) ;
#22745=FACE_OUTER_BOUND ( 'NONE', #12317, .T. ) ;
#22755=AXIS2_PLACEMENT_3D ( 'NONE', #16607, #3656, #33362 ) ;
#22760=ORIENTED_EDGE ( 'NONE', *, *, #34824, .T. ) ;
#22762=CARTESIAN_POINT ( 'NONE',  ( 18.00000000000000355, 0.000000000000000000, 0.000000000000000000 ) ) ;
#22764=CIRCLE ( 'NONE', #3888, 20.00000000000000711 ) ;
#22769=AXIS2_PLACEMENT_3D ( 'NONE', #14661, #7864, #11372 ) ;
#22772=ORIENTED_EDGE ( 'NONE', *, *, #21188, .T. ) ;
#22776=ORIENTED_EDGE ( 'NONE', *, *, #14431, .F. ) ;
#22779=EDGE_LOOP ( 'NONE', ( #34377, #26482, #20279, #5097 ) ) ;
#22781=DIRECTION ( 'NONE',  ( -1.000000000000000000, -0.000000000000000000, -0.000000000000000000 ) ) ;
#22785=VERTEX_POINT ( 'NONE', #23916 ) ;
#22803=AXIS2_PLACEMENT_3D ( 'NONE', #27436, #20707, #17216 ) ;
#22808=ORIENTED_EDGE ( 'NONE', *, *, #23628, .F. ) ;
#22810=AXIS2_PLACEMENT_3D ( 'NONE', #29663, #12865, #23565 ) ;
#22812=VERTEX_POINT ( 'NONE', #23072 ) ;
#22821=CARTESIAN_POINT ( 'NONE',  ( 18.00000000000000355, 43.55304910509445904, -28.41006711799937889 ) ) ;
#22823=ORIENTED_EDGE ( 'NONE', *, *, #3683, .T. ) ;
#22829=ORIENTED_EDGE ( 'NONE', *, *, #6008, .T. ) ;
#22837=CYLINDRICAL_SURFACE ( 'NONE', #31006, 51.99999999999999289 ) ;
#22844=CYLINDRICAL_SURFACE ( 'NONE', #5932, 51.99999999999999289 ) ;
#22847=CIRCLE ( 'NONE', #6075, 20.00000000000000711 ) ;
#22849=DIRECTION ( 'NONE',  ( 0.000000000000000000, 0.5877852522924685852, 0.8090169943749506709 ) ) ;
#22855=FACE_BOUND ( 'NONE', #36917, .T. ) ;
#22856=ORIENTED_EDGE ( 'NONE', *, *, #8804, .F. ) ;
#22857=CARTESIAN_POINT ( 'NONE',  ( 18.00000000000000355, -22.82995208772658557, -41.06517797613689424 ) ) ;
#22862=DIRECTION ( 'NONE',  ( -1.000000000000000000, -0.000000000000000000, 0.000000000000000000 ) ) ;
#22868=CIRCLE ( 'NONE', #28434, 20.00000000000000711 ) ;
#22877=EDGE_CURVE ( 'NONE', #9735, #14673, #5907, .T. ) ;
#22879=CARTESIAN_POINT ( 'NONE',  ( -10.00000000000000000, 0.000000000000000000, 0.000000000000000000 ) ) ;
#22882=DIRECTION ( 'NONE',  ( 0.000000000000000000, 0.2486898871648552389, -0.9685831611286309650 ) ) ;
#22888=CARTESIAN_POINT ( 'NONE',  ( 18.00000000000000355, 0.000000000000000000, 0.000000000000000000 ) ) ;
#22891=DIRECTION ( 'NONE',  ( 0.000000000000000000, -0.5877852522924802425, 0.8090169943749421222 ) ) ;
#22892=VERTEX_POINT ( 'NONE', #34789 ) ;
#22897=DIRECTION ( 'NONE',  ( -1.000000000000000000, -0.000000000000000000, -0.000000000000000000 ) ) ;
#22904=AXIS2_PLACEMENT_3D ( 'NONE', #18234, #8355, #37379 ) ;
#22922=DIRECTION ( 'NONE',  ( 1.000000000000000000, 0.000000000000000000, 0.000000000000000000 ) ) ;
#22926=AXIS2_PLACEMENT_3D ( 'NONE', #38856, #6126, #35376 ) ;
#22928=CARTESIAN_POINT ( 'NONE',  ( 18.00000000000000355, -42.60732521687585006, 19.80331771201644031 ) ) ;
#22931=ADVANCED_FACE ( 'NONE', ( #7520 ), #14301, .T. ) ;
#22933=CIRCLE ( 'NONE', #6150, 52.00000000000000000 ) ;
#22937=ORIENTED_EDGE ( 'NONE', *, *, #9278, .T. ) ;
#22938=AXIS2_PLACEMENT_3D ( 'NONE', #36468, #3074, #42588 ) ;
#22943=ORIENTED_EDGE ( 'NONE', *, *, #12667, .F. ) ;
#22967=ORIENTED_EDGE ( 'NONE', *, *, #42552, .F. ) ;
#22969=CARTESIAN_POINT ( 'NONE',  ( 18.00000000000000355, 47.22458491092827160, -5.098390039073737334 ) ) ;
#22975=EDGE_CURVE ( 'NONE', #4068, #42073, #3830, .T. ) ;
#22981=AXIS2_PLACEMENT_3D ( 'NONE', #19937, #22781, #3505 ) ;
#22984=VECTOR ( 'NONE', #31032, 1000.000000000000000 ) ;
#22986=EDGE_CURVE ( 'NONE', #19747, #36818, #12944, .T. ) ;
#22989=EDGE_CURVE ( 'NONE', #170, #17173, #23385, .T. ) ;
#22993=ORIENTED_EDGE ( 'NONE', *, *, #29593, .F. ) ;
#22999=VERTEX_POINT ( 'NONE', #28495 ) ;
#23007=CARTESIAN_POINT ( 'NONE',  ( 18.00000000000000355, 22.43957647427161461, 41.27978878573636479 ) ) ;
#23013=CARTESIAN_POINT ( 'NONE',  ( 18.00000000000000355, 0.000000000000000000, 0.000000000000000000 ) ) ;
#23014=ORIENTED_EDGE ( 'NONE', *, *, #12087, .F. ) ;
#23017=DIRECTION ( 'NONE',  ( 1.000000000000000000, 0.000000000000000000, 0.000000000000000000 ) ) ;
#23018=ADVANCED_FACE ( 'NONE', ( #22587 ), #19314, .T. ) ;
#23020=VERTEX_POINT ( 'NONE', #2240 ) ;
#23024=DIRECTION ( 'NONE',  ( 0.000000000000000000, 0.000000000000000000, 1.000000000000000000 ) ) ;
#23030=DIRECTION ( 'NONE',  ( -1.000000000000000000, 0.000000000000000000, 0.000000000000000000 ) ) ;
#23033=CARTESIAN_POINT ( 'NONE',  ( 0.000000000000000000, 3.840921266749842022, 47.34345070675171030 ) ) ;
#23036=CIRCLE ( 'NONE', #18877, 52.00000000000000000 ) ;
#23040=DIRECTION ( 'NONE',  ( -1.000000000000000000, 0.000000000000000000, 0.000000000000000000 ) ) ;
#23046=DIRECTION ( 'NONE',  ( -1.000000000000000000, -0.000000000000000000, -0.000000000000000000 ) ) ;
#23049=DIRECTION ( 'NONE',  ( 0.000000000000000000, 0.000000000000000000, 1.000000000000000000 ) ) ;
#23052=DIRECTION ( 'NONE',  ( 0.000000000000000000, 0.000000000000000000, 1.000000000000000000 ) ) ;
#23053=ADVANCED_FACE ( 'NONE', ( #25228 ), #28902, .T. ) ;
#23061=CARTESIAN_POINT ( 'NONE',  ( 0.000000000000000000, 0.000000000000000000, 0.000000000000000000 ) ) ;
#23062=AXIS2_PLACEMENT_3D ( 'NONE', #37207, #36783, #40261 ) ;
#23063=CARTESIAN_POINT ( 'NONE',  ( 0.000000000000000000, 39.78933988720115877, 24.98727647985016276 ) ) ;
#23068=CARTESIAN_POINT ( 'NONE',  ( 18.00000000000000355, 43.83938735307268075, 18.28286404005813637 ) ) ;
#23072=CARTESIAN_POINT ( 'NONE',  ( 0.000000000000000000, 31.08872492060014281, -41.68322423723068226 ) ) ;
#23089=CARTESIAN_POINT ( 'NONE',  ( 18.00000000000000355, 22.82995208772688756, 41.06517797613672371 ) ) ;
#23091=ADVANCED_FACE ( 'NONE', ( #8816 ), #9025, .T. ) ;
#23096=ORIENTED_EDGE ( 'NONE', *, *, #3344, .F. ) ;
#23098=ORIENTED_EDGE ( 'NONE', *, *, #20230, .T. ) ;
#23099=AXIS2_PLACEMENT_3D ( 'NONE', #42819, #9891, #2466 ) ;
#23105=ORIENTED_EDGE ( 'NONE', *, *, #8126, .F. ) ;
#23111=DIRECTION ( 'NONE',  ( 1.000000000000000000, 0.000000000000000000, 0.000000000000000000 ) ) ;
#23115=VECTOR ( 'NONE', #20159, 1000.000000000000000 ) ;
#23119=LINE ( 'NONE', #6273, #11771 ) ;
#23124=VERTEX_POINT ( 'NONE', #31735 ) ;
#23126=ADVANCED_FACE ( 'NONE', ( #21951 ), #15399, .T. ) ;
#23128=DIRECTION ( 'NONE',  ( -1.000000000000000000, -0.000000000000000000, 0.000000000000000000 ) ) ;
#23135=ADVANCED_FACE ( 'NONE', ( #42393 ), #12111, .T. ) ;
#23156=AXIS2_PLACEMENT_3D ( 'NONE', #13678, #6886, #26755 ) ;
#23163=VECTOR ( 'NONE', #6124, 1000.000000000000000 ) ;
#23167=DIRECTION ( 'NONE',  ( -1.000000000000000000, -0.000000000000000000, 0.000000000000000000 ) ) ;
#23168=LINE ( 'NONE', #16387, #18958 ) ;
#23172=DIRECTION ( 'NONE',  ( -1.000000000000000000, 0.000000000000000000, -0.000000000000000000 ) ) ;
#23182=ORIENTED_EDGE ( 'NONE', *, *, #18839, .F. ) ;
#23188=AXIS2_PLACEMENT_3D ( 'NONE', #3205, #29229, #29883 ) ;
#23191=ORIENTED_EDGE ( 'NONE', *, *, #10735, .T. ) ;
#23196=FACE_OUTER_BOUND ( 'NONE', #20917, .T. ) ;
#23198=VERTEX_POINT ( 'NONE', #26690 ) ;
#23204=ORIENTED_EDGE ( 'NONE', *, *, #13057, .T. ) ;
#23214=SURFACE_STYLE_FILL_AREA ( #22570 ) ;
#23215=CARTESIAN_POINT ( 'NONE',  ( 18.00000000000000355, -19.44205635905511897, -43.33776004284629124 ) ) ;
#23217=CARTESIAN_POINT ( 'NONE',  ( 18.00000000000000355, -43.83938735307280865, 18.28286404005783083 ) ) ;
#23220=ORIENTED_EDGE ( 'NONE', *, *, #7050, .F. ) ;
#23221=DIRECTION ( 'NONE',  ( 0.000000000000000000, 0.9822872507286879440, 0.1873813145857286533 ) ) ;
#23230=ORIENTED_EDGE ( 'NONE', *, *, #10666, .F. ) ;
#23233=DIRECTION ( 'NONE',  ( 0.000000000000000000, 0.000000000000000000, 1.000000000000000000 ) ) ;
#23242=ORIENTED_EDGE ( 'NONE', *, *, #24633, .F. ) ;
#23247=CARTESIAN_POINT ( 'NONE',  ( 0.000000000000000000, -12.30077720129063046, -50.52416135122093976 ) ) ;
#23250=STYLED_ITEM ( 'NONE', ( #25455 ), #1547 ) ;
#23253=DIRECTION ( 'NONE',  ( 1.000000000000000000, 0.000000000000000000, -0.000000000000000000 ) ) ;
#23262=CYLINDRICAL_SURFACE ( 'NONE', #1132, 47.49900000000000233 ) ;
#23270=FACE_OUTER_BOUND ( 'NONE', #2591, .T. ) ;
#23271=VERTEX_POINT ( 'NONE', #16454 ) ;
#23272=DIRECTION ( 'NONE',  ( 1.000000000000000000, 0.000000000000000000, -0.000000000000000000 ) ) ;
#23279=CARTESIAN_POINT ( 'NONE',  ( 18.00000000000000355, 0.000000000000000000, 0.000000000000000000 ) ) ;
#23281=AXIS2_PLACEMENT_3D ( 'NONE', #11493, #4928, #17416 ) ;
#23282=LINE ( 'NONE', #27187, #27826 ) ;
#23287=DIRECTION ( 'NONE',  ( 0.000000000000000000, -0.5877852522924624790, -0.8090169943749551118 ) ) ;
#23289=ORIENTED_EDGE ( 'NONE', *, *, #15160, .T. ) ;
#23298=ORIENTED_EDGE ( 'NONE', *, *, #29852, .T. ) ;
#23304=DIRECTION ( 'NONE',  ( 1.000000000000000000, 0.000000000000000000, -0.000000000000000000 ) ) ;
#23307=ADVANCED_FACE ( 'NONE', ( #16900 ), #30180, .T. ) ;
#23308=DIRECTION ( 'NONE',  ( -1.000000000000000000, 0.000000000000000000, 0.000000000000000000 ) ) ;
#23323=DIRECTION ( 'NONE',  ( 0.000000000000000000, 0.000000000000000000, 1.000000000000000000 ) ) ;
#23324=CIRCLE ( 'NONE', #12203, 20.00000000000000355 ) ;
#23331=CIRCLE ( 'NONE', #8659, 20.00000000000000711 ) ;
#23333=DIRECTION ( 'NONE',  ( 0.000000000000000000, -0.2486898871648622611, 0.9685831611286290777 ) ) ;
#23341=VERTEX_POINT ( 'NONE', #30825 ) ;
#23344=CYLINDRICAL_SURFACE ( 'NONE', #22810, 20.00000000000000355 ) ;
#23358=AXIS2_PLACEMENT_3D ( 'NONE', #9958, #23308, #6690 ) ;
#23359=FACE_OUTER_BOUND ( 'NONE', #32868, .T. ) ;
#23372=CARTESIAN_POINT ( 'NONE',  ( 0.000000000000000000, 0.000000000000000000, 0.000000000000000000 ) ) ;
#23373=VERTEX_POINT ( 'NONE', #1125 ) ;
#23377=AXIS2_PLACEMENT_3D ( 'NONE', #35312, #2133, #31410 ) ;
#23382=VERTEX_POINT ( 'NONE', #28002 ) ;
#23385=CIRCLE ( 'NONE', #10854, 20.00000000000000711 ) ;
#23392=EDGE_CURVE ( 'NONE', #30637, #37240, #17866, .T. ) ;
#23419=VECTOR ( 'NONE', #40397, 1000.000000000000000 ) ;
#23426=DIRECTION ( 'NONE',  ( -1.000000000000000000, 0.000000000000000000, 0.000000000000000000 ) ) ;
#23427=EDGE_LOOP ( 'NONE', ( #10675, #35922, #11960, #18652 ) ) ;
#23434=AXIS2_PLACEMENT_3D ( 'NONE', #26929, #37590, #23890 ) ;
#23452=EDGE_CURVE ( 'NONE', #8111, #21090, #7682, .T. ) ;
#23454=CIRCLE ( 'NONE', #8101, 47.49900000000000233 ) ;
#23461=CARTESIAN_POINT ( 'NONE',  ( 18.00000000000000355, 0.000000000000000000, 0.000000000000000000 ) ) ;
#23462=DIRECTION ( 'NONE',  ( -1.000000000000000000, 0.000000000000000000, 0.000000000000000000 ) ) ;
#23463=EDGE_CURVE ( 'NONE', #40767, #12187, #28438, .T. ) ;
#23464=DIRECTION ( 'NONE',  ( 0.000000000000000000, -0.5877852522924624790, -0.8090169943749551118 ) ) ;
#23468=CARTESIAN_POINT ( 'NONE',  ( 18.00000000000000355, 34.03046037009303149, -33.13733193845768454 ) ) ;
#23470=DIRECTION ( 'NONE',  ( 0.000000000000000000, 0.5877852522924685852, 0.8090169943749506709 ) ) ;
#23477=FACE_OUTER_BOUND ( 'NONE', #11657, .T. ) ;
#23487=ORIENTED_EDGE ( 'NONE', *, *, #11207, .F. ) ;
#23488=DIRECTION ( 'NONE',  ( -1.000000000000000000, -0.000000000000000000, 0.000000000000000000 ) ) ;
#23500=VERTEX_POINT ( 'NONE', #41707 ) ;
#23504=EDGE_CURVE ( 'NONE', #976, #235, #26204, .T. ) ;
#23508=DIRECTION ( 'NONE',  ( -1.000000000000000000, 0.000000000000000000, 0.000000000000000000 ) ) ;
#23509=CARTESIAN_POINT ( 'NONE',  ( 18.00000000000000355, -26.17370628620681927, 39.63700417846155233 ) ) ;
#23521=CARTESIAN_POINT ( 'NONE',  ( 0.000000000000000000, 42.60732521687572927, 19.80331771201673519 ) ) ;
#23523=CIRCLE ( 'NONE', #40913, 20.00000000000000711 ) ;
#23526=CARTESIAN_POINT ( 'NONE',  ( 18.00000000000000355, 15.49408907645234201, -44.90087086784576087 ) ) ;
#23528=CARTESIAN_POINT ( 'NONE',  ( 18.00000000000000355, 27.43636312076376527, -38.14186064215121519 ) ) ;
#23531=ORIENTED_EDGE ( 'NONE', *, *, #15160, .F. ) ;
#23538=AXIS2_PLACEMENT_3D ( 'NONE', #39486, #42748, #3256 ) ;
#23543=FACE_OUTER_BOUND ( 'NONE', #11410, .T. ) ;
#23545=AXIS2_PLACEMENT_3D ( 'NONE', #25848, #39310, #16027 ) ;
#23554=DIRECTION ( 'NONE',  ( -1.000000000000000000, -0.000000000000000000, 0.000000000000000000 ) ) ;
#23560=ORIENTED_EDGE ( 'NONE', *, *, #28285, .F. ) ;
#23565=DIRECTION ( 'NONE',  ( 0.000000000000000000, 0.000000000000000000, 1.000000000000000000 ) ) ;
#23569=ORIENTED_EDGE ( 'NONE', *, *, #7014, .T. ) ;
#23573=ADVANCED_FACE ( 'NONE', ( #2572 ), #15930, .T. ) ;
#23576=AXIS2_PLACEMENT_3D ( 'NONE', #8377, #18252, #8808 ) ;
#23580=ORIENTED_EDGE ( 'NONE', *, *, #926, .T. ) ;
#23581=CARTESIAN_POINT ( 'NONE',  ( 18.00000000000000355, -30.03615769709703898, -42.44795908869020451 ) ) ;
#23587=CIRCLE ( 'NONE', #18037, 20.00000000000000711 ) ;
#23598=ORIENTED_EDGE ( 'NONE', *, *, #36496, .F. ) ;
#23608=VECTOR ( 'NONE', #6815, 1000.000000000000000 ) ;
#23613=ORIENTED_EDGE ( 'NONE', *, *, #36054, .T. ) ;
#23617=VERTEX_POINT ( 'NONE', #36593 ) ;
#23624=ORIENTED_EDGE ( 'NONE', *, *, #10125, .F. ) ;
#23628=EDGE_CURVE ( 'NONE', #23271, #31610, #27031, .T. ) ;
#23643=DIRECTION ( 'NONE',  ( 0.000000000000000000, 0.9980267284282717810, -0.06279051952930990443 ) ) ;
#23652=ORIENTED_EDGE ( 'NONE', *, *, #33877, .T. ) ;
#23654=ORIENTED_EDGE ( 'NONE', *, *, #9986, .T. ) ;
#23655=CARTESIAN_POINT ( 'NONE',  ( 18.00000000000000355, 0.000000000000000000, 0.000000000000000000 ) ) ;
#23658=AXIS2_PLACEMENT_3D ( 'NONE', #24805, #28058, #31531 ) ;
#23668=VERTEX_POINT ( 'NONE', #20497 ) ;
#23673=CARTESIAN_POINT ( 'NONE',  ( 18.00000000000000355, -15.49408907645141653, -44.90087086784608061 ) ) ;
#23675=DIRECTION ( 'NONE',  ( -1.000000000000000000, 0.000000000000000000, 0.000000000000000000 ) ) ;
#23681=DIRECTION ( 'NONE',  ( 0.000000000000000000, -0.9048270524660145808, -0.4257792915650830956 ) ) ;
#23682=DIRECTION ( 'NONE',  ( 1.000000000000000000, -0.000000000000000000, -0.000000000000000000 ) ) ;
#23683=ORIENTED_EDGE ( 'NONE', *, *, #11798, .T. ) ;
#23686=AXIS2_PLACEMENT_3D ( 'NONE', #373, #33771, #43152 ) ;
#23690=AXIS2_PLACEMENT_3D ( 'NONE', #32772, #26027, #29512 ) ;
#23693=DIRECTION ( 'NONE',  ( -1.000000000000000000, 0.000000000000000000, 0.000000000000000000 ) ) ;
#23696=CARTESIAN_POINT ( 'NONE',  ( 18.00000000000000355, -17.50309955389642269, 43.60271849949357659 ) ) ;
#23697=DIRECTION ( 'NONE',  ( -1.000000000000000000, 0.000000000000000000, 0.000000000000000000 ) ) ;
#23703=ORIENTED_EDGE ( 'NONE', *, *, #37791, .F. ) ;
#23710=ORIENTED_EDGE ( 'NONE', *, *, #3548, .F. ) ;
#23717=AXIS2_PLACEMENT_3D ( 'NONE', #6909, #997, #36804 ) ;
#23725=DIRECTION ( 'NONE',  ( -1.000000000000000000, 0.000000000000000000, 0.000000000000000000 ) ) ;
#23737=CYLINDRICAL_SURFACE ( 'NONE', #19195, 51.99999999999999289 ) ;
#23748=ADVANCED_FACE ( 'NONE', ( #40069 ), #20721, .T. ) ;
#23753=LINE ( 'NONE', #37021, #11666 ) ;
#23755=LINE ( 'NONE', #4061, #35313 ) ;
#23761=DIRECTION ( 'NONE',  ( -1.000000000000000000, 0.000000000000000000, 0.000000000000000000 ) ) ;
#23776=CARTESIAN_POINT ( 'NONE',  ( 18.00000000000000355, 46.21320724403648939, 10.97699764141968970 ) ) ;
#23787=VERTEX_POINT ( 'NONE', #9985 ) ;
#23798=EDGE_CURVE ( 'NONE', #10925, #25151, #35953, .T. ) ;
#23802=CARTESIAN_POINT ( 'NONE',  ( 18.00000000000000355, 22.43957647427220081, -41.27978878573604504 ) ) ;
#23807=ORIENTED_EDGE ( 'NONE', *, *, #15826, .F. ) ;
#23808=CYLINDRICAL_SURFACE ( 'NONE', #39963, 20.00000000000000355 ) ;
#23809=CARTESIAN_POINT ( 'NONE',  ( 0.000000000000000000, 26.17370628620709638, -39.63700417846136048 ) ) ;
#23813=CARTESIAN_POINT ( 'NONE',  ( 18.00000000000000355, -31.08872492059984793, 41.68322423723088832 ) ) ;
#23816=ORIENTED_EDGE ( 'NONE', *, *, #33627, .T. ) ;
#23823=CIRCLE ( 'NONE', #4987, 47.49900000000000233 ) ;
#23834=CIRCLE ( 'NONE', #61, 47.49900000000000233 ) ;
#23837=CARTESIAN_POINT ( 'NONE',  ( 0.000000000000000000, 0.000000000000000000, 0.000000000000000000 ) ) ;
#23848=CARTESIAN_POINT ( 'NONE',  ( 18.00000000000000355, 0.2227391519116599106, 46.98410307550730636 ) ) ;
#23865=CIRCLE ( 'NONE', #5025, 20.00000000000000355 ) ;
#23870=ADVANCED_FACE ( 'NONE', ( #38325 ), #8239, .T. ) ;
#23882=ORIENTED_EDGE ( 'NONE', *, *, #8734, .F. ) ;
#23889=CARTESIAN_POINT ( 'NONE',  ( 0.000000000000000000, 0.000000000000000000, 0.000000000000000000 ) ) ;
#23890=DIRECTION ( 'NONE',  ( 0.000000000000000000, -0.8443279255020087470, -0.5358267949790065376 ) ) ;
#23896=DIRECTION ( 'NONE',  ( 0.000000000000000000, 0.4817536741017100499, 0.8763066800438663595 ) ) ;
#23900=ORIENTED_EDGE ( 'NONE', *, *, #12858, .T. ) ;
#23901=AXIS2_PLACEMENT_3D ( 'NONE', #7799, #8241, #41154 ) ;
#23907=CARTESIAN_POINT ( 'NONE',  ( 0.000000000000000000, 0.6505223195690489346, -51.99593080916756804 ) ) ;
#23910=VERTEX_POINT ( 'NONE', #18316 ) ;
#23916=CARTESIAN_POINT ( 'NONE',  ( 18.00000000000000355, -30.93515269692137792, 36.04401931830242489 ) ) ;
#23928=( GEOMETRIC_REPRESENTATION_CONTEXT ( 3 ) GLOBAL_UNCERTAINTY_ASSIGNED_CONTEXT ( ( #6302 ) ) GLOBAL_UNIT_ASSIGNED_CONTEXT ( ( #25879, #2263, #22198 ) ) REPRESENTATION_CONTEXT ( 'NONE', 'WORKASPACE' ) );
#23932=CARTESIAN_POINT ( 'NONE',  ( 9.000000000000001776, 39.64889472655731595, 33.64468972902522381 ) ) ;
#23940=ADVANCED_FACE ( 'NONE', ( #25082 ), #31159, .T. ) ;
#23941=CARTESIAN_POINT ( 'NONE',  ( 0.000000000000000000, -0.2227391519119825691, 46.98410307550729215 ) ) ;
#23943=DIRECTION ( 'NONE',  ( -1.000000000000000000, -0.000000000000000000, -0.000000000000000000 ) ) ;
#23949=ORIENTED_EDGE ( 'NONE', *, *, #34721, .F. ) ;
#23957=DIRECTION ( 'NONE',  ( -1.000000000000000000, 0.000000000000000000, 0.000000000000000000 ) ) ;
#23960=CARTESIAN_POINT ( 'NONE',  ( 18.00000000000000355, 36.34385289850590794, 29.77717097092089205 ) ) ;
#23964=CARTESIAN_POINT ( 'NONE',  ( 18.00000000000000355, -47.49120266317495975, 0.8606222198173691940 ) ) ;
#23969=EDGE_CURVE ( 'NONE', #31070, #28304, #7411, .T. ) ;
#23974=ORIENTED_EDGE ( 'NONE', *, *, #11617, .F. ) ;
#23983=CIRCLE ( 'NONE', #37204, 51.99999999999999289 ) ;
#23985=LINE ( 'NONE', #40304, #33735 ) ;
#23991=LINE ( 'NONE', #27458, #5619 ) ;
#23996=ORIENTED_EDGE ( 'NONE', *, *, #37912, .F. ) ;
#24000=EDGE_CURVE ( 'NONE', #8370, #19993, #14415, .T. ) ;
#24015=CIRCLE ( 'NONE', #19135, 20.00000000000000000 ) ;
#24025=ORIENTED_EDGE ( 'NONE', *, *, #35990, .F. ) ;
#24030=ORIENTED_EDGE ( 'NONE', *, *, #22511, .T. ) ;
#24038=DIRECTION ( 'NONE',  ( 0.000000000000000000, -0.6845471059286952764, 0.7289686274214055572 ) ) ;
#24039=ORIENTED_EDGE ( 'NONE', *, *, #18345, .T. ) ;
#24042=CARTESIAN_POINT ( 'NONE',  ( -132.0000507999999968, 0.000000000000000000, 0.000000000000000000 ) ) ;
#24044=CARTESIAN_POINT ( 'NONE',  ( 0.000000000000000000, 0.000000000000000000, 0.000000000000000000 ) ) ;
#24049=CIRCLE ( 'NONE', #21266, 20.00000000000000711 ) ;
#24052=DIRECTION ( 'NONE',  ( -1.000000000000000000, 0.000000000000000000, -0.000000000000000000 ) ) ;
#24054=EDGE_CURVE ( 'NONE', #13970, #23910, #19977, .T. ) ;
#24057=DIRECTION ( 'NONE',  ( 0.000000000000000000, -6.938893903907226800E-15, 1.000000000000000000 ) ) ;
#24069=AXIS2_PLACEMENT_3D ( 'NONE', #10655, #40311, #7374 ) ;
#24070=CIRCLE ( 'NONE', #5228, 51.99999999999999289 ) ;
#24077=ORIENTED_EDGE ( 'NONE', *, *, #4522, .T. ) ;
#24080=DIRECTION ( 'NONE',  ( 0.000000000000000000, 0.000000000000000000, 1.000000000000000000 ) ) ;
#24081=ADVANCED_FACE ( 'NONE', ( #10703 ), #7639, .T. ) ;
#24095=DIRECTION ( 'NONE',  ( -1.000000000000000000, 0.000000000000000000, 0.000000000000000000 ) ) ;
#24096=AXIS2_PLACEMENT_3D ( 'NONE', #24044, #13799, #27092 ) ;
#24101=LINE ( 'NONE', #40199, #13330 ) ;
#24112=CARTESIAN_POINT ( 'NONE',  ( 0.000000000000000000, 22.82995208772746665, -41.06517797613638976 ) ) ;
#24113=DIRECTION ( 'NONE',  ( -1.000000000000000000, 0.000000000000000000, 0.000000000000000000 ) ) ;
#24128=VERTEX_POINT ( 'NONE', #37093 ) ;
#24129=FACE_OUTER_BOUND ( 'NONE', #13852, .T. ) ;
#24137=ORIENTED_EDGE ( 'NONE', *, *, #30353, .F. ) ;
#24146=ADVANCED_FACE ( 'NONE', ( #41667 ), #32071, .T. ) ;
#24149=EDGE_CURVE ( 'NONE', #38578, #31578, #38088, .T. ) ;
#24162=AXIS2_PLACEMENT_3D ( 'NONE', #31557, #1650, #14346 ) ;
#24163=ORIENTED_EDGE ( 'NONE', *, *, #6612, .F. ) ;
#24180=FACE_OUTER_BOUND ( 'NONE', #18253, .T. ) ;
#24185=DIRECTION ( 'NONE',  ( 0.000000000000000000, 0.000000000000000000, 1.000000000000000000 ) ) ;
#24188=ORIENTED_EDGE ( 'NONE', *, *, #34031, .F. ) ;
#24193=CIRCLE ( 'NONE', #3226, 20.00000000000000711 ) ;
#24198=FACE_OUTER_BOUND ( 'NONE', #407, .T. ) ;
#24201=CARTESIAN_POINT ( 'NONE',  ( 18.00000000000000355, 0.000000000000000000, 0.000000000000000000 ) ) ;
#24216=DIRECTION ( 'NONE',  ( 0.000000000000000000, 0.000000000000000000, 1.000000000000000000 ) ) ;
#24221=VERTEX_POINT ( 'NONE', #15723 ) ;
#24222=CARTESIAN_POINT ( 'NONE',  ( 0.000000000000000000, 6.109652351741791776, 46.58570277113511793 ) ) ;
#24225=EDGE_CURVE ( 'NONE', #8904, #31415, #9540, .T. ) ;
#24234=AXIS2_PLACEMENT_3D ( 'NONE', #14912, #12062, #15349 ) ;
#24243=DIRECTION ( 'NONE',  ( 0.000000000000000000, -0.5877852522924624790, -0.8090169943749551118 ) ) ;
#24252=CARTESIAN_POINT ( 'NONE',  ( 18.00000000000000355, -36.34385289850569478, -29.77717097092114429 ) ) ;
#24261=CARTESIAN_POINT ( 'NONE',  ( 18.00000000000000355, -18.53613841426823328, 48.58406706613896375 ) ) ;
#24263=VERTEX_POINT ( 'NONE', #16354 ) ;
#24265=ADVANCED_FACE ( 'NONE', ( #29446 ), #33355, .T. ) ;
#24266=EDGE_LOOP ( 'NONE', ( #1220, #5604, #8401, #7194 ) ) ;
#24268=DIRECTION ( 'NONE',  ( 0.000000000000000000, -0.2486898871648416942, -0.9685831611286345177 ) ) ;
#24270=VECTOR ( 'NONE', #20649, 1000.000000000000000 ) ;
#24272=DIRECTION ( 'NONE',  ( 1.000000000000000000, -0.000000000000000000, -0.000000000000000000 ) ) ;
#24273=EDGE_LOOP ( 'NONE', ( #23487, #15219, #37477, #8113 ) ) ;
#24275=CIRCLE ( 'NONE', #15881, 20.00000000000000355 ) ;
#24278=ORIENTED_EDGE ( 'NONE', *, *, #18158, .F. ) ;
#24280=CIRCLE ( 'NONE', #13114, 20.00000000000000355 ) ;
#24284=ADVANCED_FACE ( 'NONE', ( #12654 ), #23344, .T. ) ;
#24285=VERTEX_POINT ( 'NONE', #2991 ) ;
#24299=CIRCLE ( 'NONE', #29854, 20.00000000000000711 ) ;
#24321=VERTEX_POINT ( 'NONE', #19439 ) ;
#24325=ORIENTED_EDGE ( 'NONE', *, *, #29534, .F. ) ;
#24330=ORIENTED_EDGE ( 'NONE', *, *, #9253, .T. ) ;
#24342=DIRECTION ( 'NONE',  ( 0.000000000000000000, 0.000000000000000000, 1.000000000000000000 ) ) ;
#24343=FACE_OUTER_BOUND ( 'NONE', #16822, .T. ) ;
#24345=CARTESIAN_POINT ( 'NONE',  ( 0.000000000000000000, -43.83938735307255286, -18.28286404005844901 ) ) ;
#24364=VERTEX_POINT ( 'NONE', #43153 ) ;
#24367=CARTESIAN_POINT ( 'NONE',  ( 18.00000000000000355, 27.79676263918241119, -37.88001506494740056 ) ) ;
#24370=ORIENTED_EDGE ( 'NONE', *, *, #2149, .F. ) ;
#24372=ORIENTED_EDGE ( 'NONE', *, *, #37838, .F. ) ;
#24375=LINE ( 'NONE', #21760, #25160 ) ;
#24382=AXIS2_PLACEMENT_3D ( 'NONE', #36901, #36034, #39292 ) ;
#24392=CARTESIAN_POINT ( 'NONE',  ( 0.000000000000000000, 0.000000000000000000, 0.000000000000000000 ) ) ;
#24393=CARTESIAN_POINT ( 'NONE',  ( 0.000000000000000000, 19.44205635905542096, 43.33776004284615624 ) ) ;
#24408=ORIENTED_EDGE ( 'NONE', *, *, #20669, .F. ) ;
#24412=DIRECTION ( 'NONE',  ( -1.000000000000000000, 0.000000000000000000, 0.000000000000000000 ) ) ;
#24416=DIRECTION ( 'NONE',  ( -1.000000000000000000, 0.000000000000000000, -0.000000000000000000 ) ) ;
#24419=EDGE_CURVE ( 'NONE', #2932, #4859, #14764, .T. ) ;
#24427=DIRECTION ( 'NONE',  ( -1.000000000000000000, -0.000000000000000000, -0.000000000000000000 ) ) ;
#24432=DIRECTION ( 'NONE',  ( -1.000000000000000000, 0.000000000000000000, -0.000000000000000000 ) ) ;
#24434=ORIENTED_EDGE ( 'NONE', *, *, #34060, .F. ) ;
#24436=DIRECTION ( 'NONE',  ( -1.000000000000000000, 0.000000000000000000, 0.000000000000000000 ) ) ;
#24437=VERTEX_POINT ( 'NONE', #4693 ) ;
#24444=EDGE_CURVE ( 'NONE', #40202, #2894, #1413, .T. ) ;
#24446=DIRECTION ( 'NONE',  ( -1.000000000000000000, 0.000000000000000000, 0.000000000000000000 ) ) ;
#24456=EDGE_CURVE ( 'NONE', #42289, #19812, #36017, .T. ) ;
#24457=ADVANCED_FACE ( 'NONE', ( #35015 ), #24815, .T. ) ;
#24465=FACE_OUTER_BOUND ( 'NONE', #43059, .T. ) ;
#24466=EDGE_CURVE ( 'NONE', #38673, #17173, #13661, .T. ) ;
#24467=ORIENTED_EDGE ( 'NONE', *, *, #34297, .F. ) ;
#24470=VECTOR ( 'NONE', #38120, 1000.000000000000000 ) ;
#24475=CARTESIAN_POINT ( 'NONE',  ( 0.000000000000000000, -2.123073309834832667, -47.45152853935337589 ) ) ;
#24494=ADVANCED_FACE ( 'NONE', ( #27041 ), #40310, .T. ) ;
#24498=VECTOR ( 'NONE', #39980, 1000.000000000000000 ) ;
#24499=DIRECTION ( 'NONE',  ( 0.000000000000000000, 0.8443279255020164076, -0.5358267949789947693 ) ) ;
#24505=EDGE_LOOP ( 'NONE', ( #31191, #30997, #36207, #30937 ) ) ;
#24516=CYLINDRICAL_SURFACE ( 'NONE', #36006, 20.00000000000000355 ) ;
#24519=DIRECTION ( 'NONE',  ( 0.000000000000000000, 0.000000000000000000, 1.000000000000000000 ) ) ;
#24522=VERTEX_POINT ( 'NONE', #7456 ) ;
#24523=DIRECTION ( 'NONE',  ( 0.000000000000000000, 0.000000000000000000, 1.000000000000000000 ) ) ;
#24524=CARTESIAN_POINT ( 'NONE',  ( 18.00000000000000355, -43.83938735307255286, -18.28286404005844901 ) ) ;
#24529=FACE_OUTER_BOUND ( 'NONE', #40891, .T. ) ;
#24530=EDGE_CURVE ( 'NONE', #8821, #7115, #3864, .T. ) ;
#24532=AXIS2_PLACEMENT_3D ( 'NONE', #17127, #14265, #254 ) ;
#24535=CARTESIAN_POINT ( 'NONE',  ( 18.00000000000000355, -38.92705108641749945, 27.21837053747784552 ) ) ;
#24551=ORIENTED_EDGE ( 'NONE', *, *, #36496, .T. ) ;
#24554=CARTESIAN_POINT ( 'NONE',  ( 18.00000000000000355, 0.000000000000000000, 0.000000000000000000 ) ) ;
#24567=AXIS2_PLACEMENT_3D ( 'NONE', #36382, #25956, #43146 ) ;
#24571=ORIENTED_EDGE ( 'NONE', *, *, #8542, .T. ) ;
#24572=DIRECTION ( 'NONE',  ( -1.000000000000000000, 0.000000000000000000, -0.000000000000000000 ) ) ;
#24576=DIRECTION ( 'NONE',  ( -1.000000000000000000, 0.000000000000000000, -0.000000000000000000 ) ) ;
#24579=ORIENTED_EDGE ( 'NONE', *, *, #40387, .T. ) ;
#24587=CYLINDRICAL_SURFACE ( 'NONE', #11241, 47.49900000000000233 ) ;
#24588=DIRECTION ( 'NONE',  ( -1.000000000000000000, 0.000000000000000000, 0.000000000000000000 ) ) ;
#24597=CARTESIAN_POINT ( 'NONE',  ( 18.00000000000000355, 0.000000000000000000, 0.000000000000000000 ) ) ;
#24607=ADVANCED_FACE ( 'NONE', ( #22855, #16280 ), #27327, .T. ) ;
#24608=EDGE_CURVE ( 'NONE', #6919, #23668, #37340, .T. ) ;
#24614=CARTESIAN_POINT ( 'NONE',  ( -132.0000507999999968, 9.184850993605147944E-16, -7.500000000000000000 ) ) ;
#24622=ORIENTED_EDGE ( 'NONE', *, *, #36251, .T. ) ;
#24629=ORIENTED_EDGE ( 'NONE', *, *, #40403, .F. ) ;
#24633=EDGE_CURVE ( 'NONE', #14673, #2894, #29081, .T. ) ;
#24641=CARTESIAN_POINT ( 'NONE',  ( -10.00000000000000000, 0.000000000000000000, 0.000000000000000000 ) ) ;
#24642=VERTEX_POINT ( 'NONE', #26517 ) ;
#24643=CARTESIAN_POINT ( 'NONE',  ( 0.000000000000000000, -25.61928775981012762, -45.25098998563503727 ) ) ;
#24645=CARTESIAN_POINT ( 'NONE',  ( 18.00000000000000355, 0.000000000000000000, 0.000000000000000000 ) ) ;
#24652=ORIENTED_EDGE ( 'NONE', *, *, #11673, .F. ) ;
#24664=AXIS2_PLACEMENT_3D ( 'NONE', #40688, #10838, #20913 ) ;
#24665=ORIENTED_EDGE ( 'NONE', *, *, #26802, .T. ) ;
#24686=FACE_OUTER_BOUND ( 'NONE', #20392, .T. ) ;
#24690=ORIENTED_EDGE ( 'NONE', *, *, #22140, .T. ) ;
#24698=CARTESIAN_POINT ( 'NONE',  ( 18.00000000000000355, -42.60732521687585006, 19.80331771201644031 ) ) ;
#24710=CARTESIAN_POINT ( 'NONE',  ( 9.000000000000001776, -12.30077720129062868, -50.52416135122093976 ) ) ;
#24720=CARTESIAN_POINT ( 'NONE',  ( -10.00000000000000000, 0.000000000000000000, 0.000000000000000000 ) ) ;
#24724=CIRCLE ( 'NONE', #30262, 51.99999999999999289 ) ;
#24734=CARTESIAN_POINT ( 'NONE',  ( 0.000000000000000000, 8.053585752062561554, -46.81126742072013514 ) ) ;
#24741=EDGE_CURVE ( 'NONE', #23020, #25565, #6072, .T. ) ;
#24743=CIRCLE ( 'NONE', #5875, 20.00000000000001066 ) ;
#24745=ORIENTED_EDGE ( 'NONE', *, *, #7125, .T. ) ;
#24758=AXIS2_PLACEMENT_3D ( 'NONE', #11223, #28244, #18029 ) ;
#24764=CARTESIAN_POINT ( 'NONE',  ( 18.00000000000000355, 38.92705108641732892, 27.21837053747810842 ) ) ;
#24769=ORIENTED_EDGE ( 'NONE', *, *, #26411, .T. ) ;
#24775=ORIENTED_EDGE ( 'NONE', *, *, #4245, .T. ) ;
#24786=DIRECTION ( 'NONE',  ( -1.000000000000000000, -0.000000000000000000, 0.000000000000000000 ) ) ;
#24788=CARTESIAN_POINT ( 'NONE',  ( 18.00000000000000355, -17.08890430202718491, -43.76671000081963570 ) ) ;
#24791=CARTESIAN_POINT ( 'NONE',  ( 18.00000000000000355, -13.85708833599999856, 45.43276465116660745 ) ) ;
#24803=ORIENTED_EDGE ( 'NONE', *, *, #8126, .T. ) ;
#24805=CARTESIAN_POINT ( 'NONE',  ( 18.00000000000000355, 5.667686777402355602, -46.64153600743599526 ) ) ;
#24810=AXIS2_PLACEMENT_3D ( 'NONE', #30434, #30652, #13431 ) ;
#24815=CYLINDRICAL_SURFACE ( 'NONE', #32453, 20.00000000000000711 ) ;
#24819=ORIENTED_EDGE ( 'NONE', *, *, #20817, .T. ) ;
#24822=VECTOR ( 'NONE', #18876, 1000.000000000000000 ) ;
#24824=DIRECTION ( 'NONE',  ( -1.000000000000000000, 0.000000000000000000, 0.000000000000000000 ) ) ;
#24826=CYLINDRICAL_SURFACE ( 'NONE', #24664, 20.00000000000000355 ) ;
#24830=EDGE_CURVE ( 'NONE', #35106, #4068, #16204, .T. ) ;
#24846=DIRECTION ( 'NONE',  ( -1.000000000000000000, -0.000000000000000000, 0.000000000000000000 ) ) ;
#24848=FACE_OUTER_BOUND ( 'NONE', #6701, .T. ) ;
#24860=DIRECTION ( 'NONE',  ( -1.000000000000000000, 0.000000000000000000, 0.000000000000000000 ) ) ;
#24863=CIRCLE ( 'NONE', #35939, 20.00000000000000711 ) ;
#24871=VERTEX_POINT ( 'NONE', #30358 ) ;
#24875=DIRECTION ( 'NONE',  ( -1.000000000000000000, 0.000000000000000000, 0.000000000000000000 ) ) ;
#24887=CYLINDRICAL_SURFACE ( 'NONE', #21999, 51.99999999999999289 ) ;
#24894=AXIS2_PLACEMENT_3D ( 'NONE', #20102, #6510, #29087 ) ;
#24899=ORIENTED_EDGE ( 'NONE', *, *, #8717, .T. ) ;
#24907=EDGE_CURVE ( 'NONE', #28617, #4417, #406, .T. ) ;
#24916=ORIENTED_EDGE ( 'NONE', *, *, #15991, .T. ) ;
#24917=LINE ( 'NONE', #28385, #14809 ) ;
#24920=DIRECTION ( 'NONE',  ( 0.000000000000000000, 0.4817536741017162116, -0.8763066800438631399 ) ) ;
#24927=EDGE_CURVE ( 'NONE', #39541, #39644, #23454, .T. ) ;
#24933=DIRECTION ( 'NONE',  ( 0.000000000000000000, 0.000000000000000000, 1.000000000000000000 ) ) ;
#24936=CARTESIAN_POINT ( 'NONE',  ( 18.00000000000000355, 44.25018368420742831, 27.31155879685195842 ) ) ;
#24942=DIRECTION ( 'NONE',  ( 0.000000000000000000, 0.000000000000000000, 1.000000000000000000 ) ) ;
#24945=ORIENTED_EDGE ( 'NONE', *, *, #35297, .F. ) ;
#24959=CIRCLE ( 'NONE', #33968, 20.00000000000000711 ) ;
#24968=AXIS2_PLACEMENT_3D ( 'NONE', #42639, #23488, #42856 ) ;
#24970=ORIENTED_EDGE ( 'NONE', *, *, #31719, .T. ) ;
#24981=EDGE_CURVE ( 'NONE', #3009, #3818, #204, .T. ) ;
#24991=CIRCLE ( 'NONE', #36069, 47.49900000000000233 ) ;
#25005=VECTOR ( 'NONE', #40123, 1000.000000000000000 ) ;
#25013=DIRECTION ( 'NONE',  ( -1.000000000000000000, 0.000000000000000000, 0.000000000000000000 ) ) ;
#25019=CARTESIAN_POINT ( 'NONE',  ( 0.000000000000000000, -46.87740477351715640, -3.172455868805708956 ) ) ;
#25027=ORIENTED_EDGE ( 'NONE', *, *, #38337, .T. ) ;
#25028=CARTESIAN_POINT ( 'NONE',  ( 9.000000000000001776, -31.08872492059985859, 41.68322423723089543 ) ) ;
#25033=ORIENTED_EDGE ( 'NONE', *, *, #15432, .T. ) ;
#25035=VERTEX_POINT ( 'NONE', #25349 ) ;
#25037=EDGE_CURVE ( 'NONE', #28849, #29751, #18589, .T. ) ;
#25043=DIRECTION ( 'NONE',  ( 0.000000000000000000, 0.7705132427757861446, 0.6374239897486934092 ) ) ;
#25047=ORIENTED_EDGE ( 'NONE', *, *, #28812, .T. ) ;
#25059=VERTEX_POINT ( 'NONE', #18175 ) ;
#25060=EDGE_CURVE ( 'NONE', #28014, #5537, #5298, .T. ) ;
#25066=DIRECTION ( 'NONE',  ( 0.000000000000000000, 0.000000000000000000, 1.000000000000000000 ) ) ;
#25072=ORIENTED_EDGE ( 'NONE', *, *, #40596, .T. ) ;
#25082=FACE_OUTER_BOUND ( 'NONE', #8737, .T. ) ;
#25103=VERTEX_POINT ( 'NONE', #24936 ) ;
#25117=DIRECTION ( 'NONE',  ( -1.000000000000000000, -0.000000000000000000, 0.000000000000000000 ) ) ;
#25121=CARTESIAN_POINT ( 'NONE',  ( 9.000000000000001776, 51.85248208264523129, -3.914090171285650843 ) ) ;
#25129=DIRECTION ( 'NONE',  ( 0.000000000000000000, 0.000000000000000000, 1.000000000000000000 ) ) ;
#25133=EDGE_LOOP ( 'NONE', ( #33611, #24629, #13434, #806 ) ) ;
#25141=VERTEX_POINT ( 'NONE', #14874 ) ;
#25142=FACE_OUTER_BOUND ( 'NONE', #13619, .T. ) ;
#25144=ORIENTED_EDGE ( 'NONE', *, *, #43102, .T. ) ;
#25146=EDGE_CURVE ( 'NONE', #38699, #15576, #34474, .T. ) ;
#25151=VERTEX_POINT ( 'NONE', #28819 ) ;
#25160=VECTOR ( 'NONE', #11470, 1000.000000000000000 ) ;
#25162=ADVANCED_FACE ( 'NONE', ( #34701 ), #8513, .T. ) ;
#25180=EDGE_CURVE ( 'NONE', #16988, #12470, #42620, .T. ) ;
#25185=ORIENTED_EDGE ( 'NONE', *, *, #20974, .T. ) ;
#25189=CYLINDRICAL_SURFACE ( 'NONE', #27304, 51.99999999999999289 ) ;
#25194=VECTOR ( 'NONE', #24875, 1000.000000000000000 ) ;
#25197=AXIS2_PLACEMENT_3D ( 'NONE', #42491, #12636, #32899 ) ;
#25198=DIRECTION ( 'NONE',  ( 0.000000000000000000, 0.000000000000000000, 1.000000000000000000 ) ) ;
#25200=EDGE_CURVE ( 'NONE', #25141, #12154, #16924, .T. ) ;
#25201=ORIENTED_EDGE ( 'NONE', *, *, #33457, .T. ) ;
#25203=DIRECTION ( 'NONE',  ( 0.000000000000000000, 0.000000000000000000, -1.000000000000000000 ) ) ;
#25209=ORIENTED_EDGE ( 'NONE', *, *, #22326, .T. ) ;
#25223=AXIS2_PLACEMENT_3D ( 'NONE', #41323, #8603, #8829 ) ;
#25225=AXIS2_PLACEMENT_3D ( 'NONE', #39068, #35782, #6136 ) ;
#25228=FACE_OUTER_BOUND ( 'NONE', #285, .T. ) ;
#25236=ORIENTED_EDGE ( 'NONE', *, *, #38015, .F. ) ;
#25266=ADVANCED_FACE ( 'NONE', ( #42515 ), #12237, .T. ) ;
#25277=CARTESIAN_POINT ( 'NONE',  ( 9.000000000000001776, -30.03615769709762517, 42.44795908868979240 ) ) ;
#25281=AXIS2_PLACEMENT_3D ( 'NONE', #30043, #13465, #40027 ) ;
#25288=EDGE_CURVE ( 'NONE', #27234, #9752, #37062, .T. ) ;
#25289=AXIS2_PLACEMENT_3D ( 'NONE', #1940, #15305, #25129 ) ;
#25291=CARTESIAN_POINT ( 'NONE',  ( 0.000000000000000000, 46.90537658765334328, -2.727856614653797251 ) ) ;
#25293=DIRECTION ( 'NONE',  ( -1.000000000000000000, -0.000000000000000000, -0.000000000000000000 ) ) ;
#25302=ORIENTED_EDGE ( 'NONE', *, *, #28694, .T. ) ;
#25322=DIRECTION ( 'NONE',  ( -1.000000000000000000, -0.000000000000000000, -0.000000000000000000 ) ) ;
#25329=VERTEX_POINT ( 'NONE', #32710 ) ;
#25331=CARTESIAN_POINT ( 'NONE',  ( 18.00000000000000355, 6.109652351742432153, -46.58570277113501845 ) ) ;
#25334=EDGE_CURVE ( 'NONE', #27883, #31415, #21114, .T. ) ;
#25335=DIRECTION ( 'NONE',  ( -1.000000000000000000, 0.000000000000000000, -0.000000000000000000 ) ) ;
#25337=EDGE_CURVE ( 'NONE', #2405, #16540, #33361, .T. ) ;
#25347=CYLINDRICAL_SURFACE ( 'NONE', #4979, 11.00000000000000000 ) ;
#25348=VECTOR ( 'NONE', #2952, 1000.000000000000000 ) ;
#25349=CARTESIAN_POINT ( 'NONE',  ( 0.000000000000000000, -47.22458491092822896, 5.098390039074067737 ) ) ;
#25350=ADVANCED_FACE ( 'NONE', ( #10452 ), #6948, .T. ) ;
#25352=CARTESIAN_POINT ( 'NONE',  ( 18.00000000000000355, -22.43957647427189528, 41.27978878573620847 ) ) ;
#25358=ORIENTED_EDGE ( 'NONE', *, *, #7894, .T. ) ;
#25370=ORIENTED_EDGE ( 'NONE', *, *, #27374, .F. ) ;
#25375=CARTESIAN_POINT ( 'NONE',  ( 0.000000000000000000, 40.47821179127715396, 32.64221760512772619 ) ) ;
#25376=ORIENTED_EDGE ( 'NONE', *, *, #24225, .F. ) ;
#25382=AXIS2_PLACEMENT_3D ( 'NONE', #39962, #478, #10325 ) ;
#25396=ADVANCED_FACE ( 'NONE', ( #37054 ), #37492, .T. ) ;
#25400=DIRECTION ( 'NONE',  ( 1.000000000000000000, -0.000000000000000000, -0.000000000000000000 ) ) ;
#25416=DIRECTION ( 'NONE',  ( -1.000000000000000000, -0.000000000000000000, -0.000000000000000000 ) ) ;
#25417=CARTESIAN_POINT ( 'NONE',  ( 9.000000000000001776, -51.85248208264514602, -3.914090171286729980 ) ) ;
#25420=DIRECTION ( 'NONE',  ( 0.000000000000000000, 0.000000000000000000, 1.000000000000000000 ) ) ;
#25424=CARTESIAN_POINT ( 'NONE',  ( 9.000000000000001776, 36.06787431788731624, -37.45808914225450081 ) ) ;
#25426=DIRECTION ( 'NONE',  ( 1.000000000000000000, 0.000000000000000000, 0.000000000000000000 ) ) ;
#25430=CARTESIAN_POINT ( 'NONE',  ( 18.00000000000000355, 36.34385289850631295, -29.77717097092038756 ) ) ;
#25440=VERTEX_POINT ( 'NONE', #20101 ) ;
#25442=CIRCLE ( 'NONE', #22671, 20.00000000000000711 ) ;
#25447=CIRCLE ( 'NONE', #27511, 47.49900000000000233 ) ;
#25450=AXIS2_PLACEMENT_3D ( 'NONE', #25463, #12779, #22207 ) ;
#25451=CYLINDRICAL_SURFACE ( 'NONE', #38686, 51.99999999999999289 ) ;
#25455=PRESENTATION_STYLE_ASSIGNMENT (( #9052 ) ) ;
#25463=CARTESIAN_POINT ( 'NONE',  ( 18.00000000000000355, -5.667686777401384823, -46.64153600743609474 ) ) ;
#25471=CIRCLE ( 'NONE', #34489, 47.49899999999999523 ) ;
#25480=CARTESIAN_POINT ( 'NONE',  ( 18.00000000000000355, 0.000000000000000000, 0.000000000000000000 ) ) ;
#25486=LINE ( 'NONE', #22231, #31157 ) ;
#25504=CIRCLE ( 'NONE', #24096, 52.00000000000000000 ) ;
#25505=AXIS2_PLACEMENT_3D ( 'NONE', #19454, #28828, #16163 ) ;
#25506=CYLINDRICAL_SURFACE ( 'NONE', #40833, 20.00000000000000355 ) ;
#25514=DIRECTION ( 'NONE',  ( 1.000000000000000000, 0.000000000000000000, -0.000000000000000000 ) ) ;
#25517=ORIENTED_EDGE ( 'NONE', *, *, #13797, .F. ) ;
#25524=EDGE_CURVE ( 'NONE', #25059, #10533, #1909, .T. ) ;
#25555=DIRECTION ( 'NONE',  ( 0.000000000000000000, -0.7705132427757949154, 0.6374239897486827511 ) ) ;
#25557=EDGE_CURVE ( 'NONE', #21131, #4386, #31562, .T. ) ;
#25560=ORIENTED_EDGE ( 'NONE', *, *, #8717, .F. ) ;
#25562=ORIENTED_EDGE ( 'NONE', *, *, #27668, .T. ) ;
#25563=DIRECTION ( 'NONE',  ( -1.000000000000000000, 0.000000000000000000, -0.000000000000000000 ) ) ;
#25564=AXIS2_PLACEMENT_3D ( 'NONE', #7920, #11870, #25198 ) ;
#25565=VERTEX_POINT ( 'NONE', #28567 ) ;
#25574=MECHANICAL_DESIGN_GEOMETRIC_PRESENTATION_REPRESENTATION('',(#2525),#17230);
#25592=EDGE_LOOP ( 'NONE', ( #10591, #40713, #39591, #40683 ) ) ;
#25598=EDGE_LOOP ( 'NONE', ( #28443, #25948, #31184, #34124 ) ) ;
#25599=CARTESIAN_POINT ( 'NONE',  ( 18.00000000000000355, -12.30077720129062868, -50.52416135122093976 ) ) ;
#25617=DIRECTION ( 'NONE',  ( 0.000000000000000000, 0.000000000000000000, 1.000000000000000000 ) ) ;
#25636=DIRECTION ( 'NONE',  ( -1.000000000000000000, -0.000000000000000000, -0.000000000000000000 ) ) ;
#25664=DIRECTION ( 'NONE',  ( 0.000000000000000000, 0.000000000000000000, 1.000000000000000000 ) ) ;
#25668=AXIS2_PLACEMENT_3D ( 'NONE', #680, #14041, #40824 ) ;
#25669=LINE ( 'NONE', #36494, #2850 ) ;
#25673=CARTESIAN_POINT ( 'NONE',  ( 150.0000507999999968, 9.184850993605147944E-16, -7.500000000000000000 ) ) ;
#25677=CARTESIAN_POINT ( 'NONE',  ( 18.00000000000000355, 0.000000000000000000, 0.000000000000000000 ) ) ;
#25688=AXIS2_PLACEMENT_3D ( 'NONE', #8977, #21899, #22535 ) ;
#25692=DIRECTION ( 'NONE',  ( 0.000000000000000000, 0.000000000000000000, 1.000000000000000000 ) ) ;
#25694=EDGE_CURVE ( 'NONE', #7587, #39801, #32920, .T. ) ;
#25710=EDGE_LOOP ( 'NONE', ( #24278, #23580, #33025, #19447 ) ) ;
#25714=CARTESIAN_POINT ( 'NONE',  ( 18.00000000000000355, 42.41764978026607480, -20.20639853260305685 ) ) ;
#25717=DIRECTION ( 'NONE',  ( -1.000000000000000000, 0.000000000000000000, -0.000000000000000000 ) ) ;
#25728=ORIENTED_EDGE ( 'NONE', *, *, #36157, .F. ) ;
#25748=AXIS2_PLACEMENT_3D ( 'NONE', #31799, #35264, #38959 ) ;
#25759=EDGE_LOOP ( 'NONE', ( #5603, #22808, #39067, #1397 ) ) ;
#25760=ORIENTED_EDGE ( 'NONE', *, *, #35616, .F. ) ;
#25764=CARTESIAN_POINT ( 'NONE',  ( 0.000000000000000000, 0.000000000000000000, 0.000000000000000000 ) ) ;
#25770=CARTESIAN_POINT ( 'NONE',  ( 0.000000000000000000, -34.03046037009278280, 33.13733193845793323 ) ) ;
#25772=DIRECTION ( 'NONE',  ( 0.000000000000000000, 0.1253332335642974305, 0.9921147013144787641 ) ) ;
#25774=AXIS2_PLACEMENT_3D ( 'NONE', #16084, #39377, #29384 ) ;
#25776=FACE_OUTER_BOUND ( 'NONE', #18936, .T. ) ;
#25779=ADVANCED_FACE ( 'NONE', ( #39621, #42672 ), #12822, .F. ) ;
#25810=ORIENTED_EDGE ( 'NONE', *, *, #16704, .F. ) ;
#25836=ORIENTED_EDGE ( 'NONE', *, *, #662, .F. ) ;
#25838=LINE ( 'NONE', #25417, #13754 ) ;
#25843=DIRECTION ( 'NONE',  ( -1.000000000000000000, 0.000000000000000000, 0.000000000000000000 ) ) ;
#25848=CARTESIAN_POINT ( 'NONE',  ( 18.00000000000000355, 0.000000000000000000, 0.000000000000000000 ) ) ;
#25851=DIRECTION ( 'NONE',  ( -1.000000000000000000, 0.000000000000000000, -0.000000000000000000 ) ) ;
#25858=ORIENTED_EDGE ( 'NONE', *, *, #18370, .F. ) ;
#25879=( LENGTH_UNIT ( ) NAMED_UNIT ( * ) SI_UNIT ( .MILLI., .METRE. ) );
#25881=FACE_OUTER_BOUND ( 'NONE', #20602, .T. ) ;
#25912=DIRECTION ( 'NONE',  ( 0.000000000000000000, 0.000000000000000000, 1.000000000000000000 ) ) ;
#25921=AXIS2_PLACEMENT_3D ( 'NONE', #27840, #11250, #4446 ) ;
#25929=EDGE_CURVE ( 'NONE', #37461, #17463, #20471, .T. ) ;
#25947=CARTESIAN_POINT ( 'NONE',  ( 0.000000000000000000, -13.56094713063537327, -50.20060470671754871 ) ) ;
#25948=ORIENTED_EDGE ( 'NONE', *, *, #41784, .F. ) ;
#25951=VERTEX_POINT ( 'NONE', #26555 ) ;
#25956=DIRECTION ( 'NONE',  ( -1.000000000000000000, 0.000000000000000000, -0.000000000000000000 ) ) ;
#25962=DIRECTION ( 'NONE',  ( 0.000000000000000000, 0.000000000000000000, -1.000000000000000000 ) ) ;
#25970=CIRCLE ( 'NONE', #31541, 20.00000000000001066 ) ;
#25972=ADVANCED_FACE ( 'NONE', ( #36554 ), #6895, .T. ) ;
#25982=DIRECTION ( 'NONE',  ( -1.000000000000000000, 0.000000000000000000, 0.000000000000000000 ) ) ;
#25988=LINE ( 'NONE', #39247, #40239 ) ;
#25989=EDGE_CURVE ( 'NONE', #1619, #10863, #33662, .T. ) ;
#25991=DIRECTION ( 'NONE',  ( -1.000000000000000000, 0.000000000000000000, -0.000000000000000000 ) ) ;
#25993=EDGE_LOOP ( 'NONE', ( #5071, #19581, #22581, #21098 ) ) ;
#25996=CARTESIAN_POINT ( 'NONE',  ( 9.000000000000001776, -47.32430374665916162, -21.55018039121577544 ) ) ;
#26004=CARTESIAN_POINT ( 'NONE',  ( 18.00000000000000355, 18.53613841426788866, 48.58406706613909876 ) ) ;
#26027=DIRECTION ( 'NONE',  ( -1.000000000000000000, 0.000000000000000000, 0.000000000000000000 ) ) ;
#26032=VERTEX_POINT ( 'NONE', #20910 ) ;
#26033=EDGE_CURVE ( 'NONE', #22307, #3223, #5788, .T. ) ;
#26035=DIRECTION ( 'NONE',  ( -1.000000000000000000, 0.000000000000000000, 0.000000000000000000 ) ) ;
#26037=ADVANCED_FACE ( 'NONE', ( #31765 ), #37640, .T. ) ;
#26044=CARTESIAN_POINT ( 'NONE',  ( 0.000000000000000000, -37.91532898920899441, -28.61088654061679648 ) ) ;
#26045=ORIENTED_EDGE ( 'NONE', *, *, #19876, .F. ) ;
#26095=EDGE_CURVE ( 'NONE', #2698, #16742, #4375, .T. ) ;
#26100=CARTESIAN_POINT ( 'NONE',  ( 18.00000000000000355, 46.87740477351718482, -3.172455868805370560 ) ) ;
#26101=ORIENTED_EDGE ( 'NONE', *, *, #1133, .T. ) ;
#26102=DIRECTION ( 'NONE',  ( 0.000000000000000000, 0.000000000000000000, 1.000000000000000000 ) ) ;
#26103=ORIENTED_EDGE ( 'NONE', *, *, #12910, .F. ) ;
#26105=LINE ( 'NONE', #33279, #17960 ) ;
#26106=DIRECTION ( 'NONE',  ( 1.000000000000000000, 0.000000000000000000, 0.000000000000000000 ) ) ;
#26107=DIRECTION ( 'NONE',  ( 0.000000000000000000, 0.000000000000000000, -1.000000000000000000 ) ) ;
#26110=CIRCLE ( 'NONE', #18481, 52.00000000000000000 ) ;
#26127=CARTESIAN_POINT ( 'NONE',  ( 0.000000000000000000, -49.65209126885774538, 15.44894276735533190 ) ) ;
#26136=AXIS2_PLACEMENT_3D ( 'NONE', #35586, #15561, #5707 ) ;
#26139=CIRCLE ( 'NONE', #12901, 47.49900000000000944 ) ;
#26141=VERTEX_POINT ( 'NONE', #11270 ) ;
#26163=DIRECTION ( 'NONE',  ( 0.000000000000000000, 0.000000000000000000, 1.000000000000000000 ) ) ;
#26166=CIRCLE ( 'NONE', #7328, 47.49900000000000233 ) ;
#26179=DIRECTION ( 'NONE',  ( -1.000000000000000000, 0.000000000000000000, 0.000000000000000000 ) ) ;
#26180=AXIS2_PLACEMENT_3D ( 'NONE', #1179, #25851, #21749 ) ;
#26184=CARTESIAN_POINT ( 'NONE',  ( 0.000000000000000000, 35.11945359308163006, -38.34871548465977753 ) ) ;
#26198=CARTESIAN_POINT ( 'NONE',  ( 0.000000000000000000, 0.6505223195683064175, 51.99593080916758225 ) ) ;
#26204=CIRCLE ( 'NONE', #31787, 52.00000000000000000 ) ;
#26213=ORIENTED_EDGE ( 'NONE', *, *, #2954, .F. ) ;
#26215=ORIENTED_EDGE ( 'NONE', *, *, #20236, .F. ) ;
#26219=EDGE_LOOP ( 'NONE', ( #18469, #9688, #30993, #17113 ) ) ;
#26240=ORIENTED_EDGE ( 'NONE', *, *, #34899, .T. ) ;
#26241=LINE ( 'NONE', #36452, #24822 ) ;
#26242=CARTESIAN_POINT ( 'NONE',  ( 18.00000000000000355, 42.60732521687599217, -19.80331771201614544 ) ) ;
#26243=ORIENTED_EDGE ( 'NONE', *, *, #11897, .T. ) ;
#26244=AXIS2_PLACEMENT_3D ( 'NONE', #26507, #30650, #33262 ) ;
#26255=CIRCLE ( 'NONE', #40142, 20.00000000000001421 ) ;
#26259=CARTESIAN_POINT ( 'NONE',  ( 0.000000000000000000, -7.162210897275391730, -51.50439529848834042 ) ) ;
#26261=DIRECTION ( 'NONE',  ( 0.000000000000000000, 0.000000000000000000, 1.000000000000000000 ) ) ;
#26288=DIRECTION ( 'NONE',  ( 0.000000000000000000, 0.9980267284282712259, 0.06279051952931685721 ) ) ;
#26297=VECTOR ( 'NONE', #24846, 1000.000000000000000 ) ;
#26298=CARTESIAN_POINT ( 'NONE',  ( 18.00000000000000355, 0.000000000000000000, 0.000000000000000000 ) ) ;
#26299=DIRECTION ( 'NONE',  ( 0.000000000000000000, -0.3681245526846654847, -0.9297764858882564543 ) ) ;
#26302=DIRECTION ( 'NONE',  ( -1.000000000000000000, 0.000000000000000000, 0.000000000000000000 ) ) ;
#26319=CYLINDRICAL_SURFACE ( 'NONE', #43013, 20.00000000000000355 ) ;
#26321=LINE ( 'NONE', #9923, #38826 ) ;
#26326=ORIENTED_EDGE ( 'NONE', *, *, #28684, .T. ) ;
#26330=AXIS2_PLACEMENT_3D ( 'NONE', #16729, #30020, #29810 ) ;
#26333=CARTESIAN_POINT ( 'NONE',  ( 18.00000000000000355, 6.109652351741791776, 46.58570277113511793 ) ) ;
#26335=ADVANCED_FACE ( 'NONE', ( #2063 ), #9262, .T. ) ;
#26338=ORIENTED_EDGE ( 'NONE', *, *, #24419, .F. ) ;
#26339=VERTEX_POINT ( 'NONE', #17966 ) ;
#26340=DIRECTION ( 'NONE',  ( 0.000000000000000000, 0.6845471059286846183, 0.7289686274214153272 ) ) ;
#26346=EDGE_CURVE ( 'NONE', #30436, #7181, #30220, .T. ) ;
#26347=LINE ( 'NONE', #13255, #22201 ) ;
#26378=ORIENTED_EDGE ( 'NONE', *, *, #41790, .F. ) ;
#26382=VERTEX_POINT ( 'NONE', #7870 ) ;
#26386=CIRCLE ( 'NONE', #2664, 20.00000000000000711 ) ;
#26387=EDGE_LOOP ( 'NONE', ( #2553, #15947, #13326, #28129 ) ) ;
#26391=EDGE_LOOP ( 'NONE', ( #8338, #18645, #18953, #9878 ) ) ;
#26396=ADVANCED_FACE ( 'NONE', ( #27312 ), #4590, .T. ) ;
#26397=EDGE_CURVE ( 'NONE', #10253, #38578, #20502, .T. ) ;
#26411=EDGE_CURVE ( 'NONE', #33890, #34535, #28145, .T. ) ;
#26413=CIRCLE ( 'NONE', #7586, 51.99999999999999289 ) ;
#26428=CYLINDRICAL_SURFACE ( 'NONE', #20749, 20.00000000000000355 ) ;
#26435=AXIS2_PLACEMENT_3D ( 'NONE', #10538, #16463, #13402 ) ;
#26438=EDGE_CURVE ( 'NONE', #9587, #11400, #8589, .T. ) ;
#26446=CARTESIAN_POINT ( 'NONE',  ( 18.00000000000000355, -11.46872990052349550, -45.56340405422456286 ) ) ;
#26447=ORIENTED_EDGE ( 'NONE', *, *, #22989, .F. ) ;
#26448=EDGE_CURVE ( 'NONE', #10279, #13305, #17697, .T. ) ;
#26452=CARTESIAN_POINT ( 'NONE',  ( 0.000000000000000000, -35.11945359308084136, -38.34871548466050939 ) ) ;
#26453=EDGE_CURVE ( 'NONE', #8821, #36472, #30797, .T. ) ;
#26459=AXIS2_PLACEMENT_3D ( 'NONE', #23089, #16535, #6248 ) ;
#26466=CARTESIAN_POINT ( 'NONE',  ( 18.00000000000000355, -35.20873326984102647, 31.88259874184018372 ) ) ;
#26467=CARTESIAN_POINT ( 'NONE',  ( 0.000000000000000000, -39.78933988720098114, -24.98727647985043276 ) ) ;
#26478=VERTEX_POINT ( 'NONE', #10504 ) ;
#26482=ORIENTED_EDGE ( 'NONE', *, *, #25037, .T. ) ;
#26486=VERTEX_POINT ( 'NONE', #20571 ) ;
#26500=ORIENTED_EDGE ( 'NONE', *, *, #15296, .T. ) ;
#26507=CARTESIAN_POINT ( 'NONE',  ( 0.000000000000000000, 0.000000000000000000, 0.000000000000000000 ) ) ;
#26510=AXIS2_PLACEMENT_3D ( 'NONE', #35347, #28409, #28822 ) ;
#26511=VERTEX_POINT ( 'NONE', #1532 ) ;
#26513=CARTESIAN_POINT ( 'NONE',  ( 18.00000000000000355, 0.000000000000000000, 0.000000000000000000 ) ) ;
#26517=CARTESIAN_POINT ( 'NONE',  ( 0.000000000000000000, -36.06787431788703913, 37.45808914225474950 ) ) ;
#26519=CYLINDRICAL_SURFACE ( 'NONE', #27051, 51.99999999999999289 ) ;
#26525=CIRCLE ( 'NONE', #37627, 20.00000000000000711 ) ;
#26526=EDGE_CURVE ( 'NONE', #192, #39608, #28831, .T. ) ;
#26531=DIRECTION ( 'NONE',  ( -1.000000000000000000, 0.000000000000000000, 0.000000000000000000 ) ) ;
#26533=CARTESIAN_POINT ( 'NONE',  ( 18.00000000000000355, 0.000000000000000000, 0.000000000000000000 ) ) ;
#26551=LINE ( 'NONE', #10606, #36233 ) ;
#26552=ORIENTED_EDGE ( 'NONE', *, *, #40589, .T. ) ;
#26555=CARTESIAN_POINT ( 'NONE',  ( 18.00000000000000355, 51.85248208264522418, -3.914090171285654396 ) ) ;
#26566=CIRCLE ( 'NONE', #7049, 20.00000000000000711 ) ;
#26573=ORIENTED_EDGE ( 'NONE', *, *, #3322, .F. ) ;
#26577=CARTESIAN_POINT ( 'NONE',  ( 0.000000000000000000, 0.000000000000000000, 0.000000000000000000 ) ) ;
#26589=AXIS2_PLACEMENT_3D ( 'NONE', #20617, #33888, #30839 ) ;
#26593=CARTESIAN_POINT ( 'NONE',  ( 0.000000000000000000, 0.000000000000000000, 0.000000000000000000 ) ) ;
#26596=VERTEX_POINT ( 'NONE', #38833 ) ;
#26599=CIRCLE ( 'NONE', #7773, 20.00000000000000000 ) ;
#26600=FACE_OUTER_BOUND ( 'NONE', #14515, .T. ) ;
#26601=DIRECTION ( 'NONE',  ( 0.000000000000000000, 0.000000000000000000, 1.000000000000000000 ) ) ;
#26608=ADVANCED_FACE ( 'NONE', ( #5469 ), #31654, .T. ) ;
#26610=EDGE_CURVE ( 'NONE', #39801, #11061, #31237, .T. ) ;
#26625=EDGE_CURVE ( 'NONE', #15847, #33890, #4823, .T. ) ;
#26627=ADVANCED_FACE ( 'NONE', ( #21459 ), #28182, .T. ) ;
#26629=DIRECTION ( 'NONE',  ( 1.000000000000000000, -0.000000000000000000, -0.000000000000000000 ) ) ;
#26641=CYLINDRICAL_SURFACE ( 'NONE', #23538, 20.00000000000000711 ) ;
#26657=DIRECTION ( 'NONE',  ( 0.000000000000000000, -0.6845471059286952764, 0.7289686274214055572 ) ) ;
#26658=FACE_OUTER_BOUND ( 'NONE', #3657, .T. ) ;
#26673=EDGE_LOOP ( 'NONE', ( #35084, #1097, #30490, #39017 ) ) ;
#26675=( LENGTH_UNIT ( ) NAMED_UNIT ( * ) SI_UNIT ( .MILLI., .METRE. ) );
#26678=AXIS2_PLACEMENT_3D ( 'NONE', #37471, #1016, #30086 ) ;
#26681=CARTESIAN_POINT ( 'NONE',  ( 18.00000000000000355, 13.85708833599968770, 45.43276465116669982 ) ) ;
#26683=CYLINDRICAL_SURFACE ( 'NONE', #9649, 51.99999999999999289 ) ;
#26690=CARTESIAN_POINT ( 'NONE',  ( 0.000000000000000000, 47.32430374665931794, 21.55018039121544149 ) ) ;
#26701=ORIENTED_EDGE ( 'NONE', *, *, #5293, .T. ) ;
#26703=ORIENTED_EDGE ( 'NONE', *, *, #9040, .F. ) ;
#26715=CARTESIAN_POINT ( 'NONE',  ( 18.00000000000000355, -24.47917365149977798, 45.87777302070926311 ) ) ;
#26720=DIRECTION ( 'NONE',  ( 0.000000000000000000, 0.000000000000000000, 1.000000000000000000 ) ) ;
#26737=CARTESIAN_POINT ( 'NONE',  ( 0.000000000000000000, 0.000000000000000000, 0.000000000000000000 ) ) ;
#26738=ORIENTED_EDGE ( 'NONE', *, *, #39782, .T. ) ;
#26739=ORIENTED_EDGE ( 'NONE', *, *, #40740, .T. ) ;
#26740=CARTESIAN_POINT ( 'NONE',  ( 18.00000000000000355, 34.03046037009255542, 33.13733193845817482 ) ) ;
#26747=EDGE_LOOP ( 'NONE', ( #18750, #36652, #8615, #36075 ) ) ;
#26750=DIRECTION ( 'NONE',  ( 0.000000000000000000, 0.000000000000000000, 1.000000000000000000 ) ) ;
#26751=DIRECTION ( 'NONE',  ( -1.000000000000000000, 0.000000000000000000, 0.000000000000000000 ) ) ;
#26755=DIRECTION ( 'NONE',  ( 0.000000000000000000, 0.000000000000000000, 1.000000000000000000 ) ) ;
#26758=CARTESIAN_POINT ( 'NONE',  ( 0.000000000000000000, -45.78515115856051665, 12.64416602183649374 ) ) ;
#26768=LINE ( 'NONE', #13477, #7193 ) ;
#26771=CARTESIAN_POINT ( 'NONE',  ( -10.00000000000000000, 0.000000000000000000, 0.000000000000000000 ) ) ;
#26776=DIRECTION ( 'NONE',  ( -1.000000000000000000, -0.000000000000000000, 0.000000000000000000 ) ) ;
#26786=CARTESIAN_POINT ( 'NONE',  ( 18.00000000000000355, 37.91532898920961969, -28.61088654061597936 ) ) ;
#26787=DIRECTION ( 'NONE',  ( -1.000000000000000000, -0.000000000000000000, 0.000000000000000000 ) ) ;
#26793=DIRECTION ( 'NONE',  ( -1.000000000000000000, 0.000000000000000000, -0.000000000000000000 ) ) ;
#26797=DIRECTION ( 'NONE',  ( -1.000000000000000000, 0.000000000000000000, 0.000000000000000000 ) ) ;
#26800=EDGE_CURVE ( 'NONE', #34203, #39186, #23983, .T. ) ;
#26802=EDGE_CURVE ( 'NONE', #37957, #16711, #5139, .T. ) ;
#26804=AXIS2_PLACEMENT_3D ( 'NONE', #33675, #3990, #23896 ) ;
#26809=CARTESIAN_POINT ( 'NONE',  ( 0.000000000000000000, -17.08890430202782085, 43.76671000081940122 ) ) ;
#26812=CARTESIAN_POINT ( 'NONE',  ( 9.000000000000001776, 46.77034588191303754, 22.72740077717245910 ) ) ;
#26814=ORIENTED_EDGE ( 'NONE', *, *, #15328, .F. ) ;
#26817=VECTOR ( 'NONE', #5864, 1000.000000000000000 ) ;
#26822=ADVANCED_FACE ( 'NONE', ( #10459 ), #40100, .T. ) ;
#26850=EDGE_CURVE ( 'NONE', #1556, #38673, #24015, .T. ) ;
#26854=EDGE_LOOP ( 'NONE', ( #18302, #33864, #6823, #16709 ) ) ;
#26867=AXIS2_PLACEMENT_3D ( 'NONE', #3056, #39090, #42572 ) ;
#26880=AXIS2_PLACEMENT_3D ( 'NONE', #8102, #27321, #3938 ) ;
#26882=ORIENTED_EDGE ( 'NONE', *, *, #6605, .F. ) ;
#26884=CYLINDRICAL_SURFACE ( 'NONE', #5182, 47.49900000000000233 ) ;
#26897=ORIENTED_EDGE ( 'NONE', *, *, #33671, .T. ) ;
#26905=CARTESIAN_POINT ( 'NONE',  ( 18.00000000000000355, -0.2227391519113303131, -46.98410307550732057 ) ) ;
#26907=FACE_OUTER_BOUND ( 'NONE', #10335, .T. ) ;
#26915=EDGE_LOOP ( 'NONE', ( #38764, #9081, #6613, #1597 ) ) ;
#26929=CARTESIAN_POINT ( 'NONE',  ( 0.000000000000000000, 5.667686777402355602, -46.64153600743599526 ) ) ;
#26930=ORIENTED_EDGE ( 'NONE', *, *, #15351, .T. ) ;
#26931=LINE ( 'NONE', #20201, #24498 ) ;
#26935=DIRECTION ( 'NONE',  ( 0.000000000000000000, 0.000000000000000000, 1.000000000000000000 ) ) ;
#26951=CARTESIAN_POINT ( 'NONE',  ( 18.00000000000000355, -2.123073309835499245, 47.45152853935333326 ) ) ;
#26954=DIRECTION ( 'NONE',  ( -1.000000000000000000, -0.000000000000000000, -0.000000000000000000 ) ) ;
#26964=LINE ( 'NONE', #26740, #20325 ) ;
#26966=FACE_OUTER_BOUND ( 'NONE', #40802, .T. ) ;
#26982=AXIS2_PLACEMENT_3D ( 'NONE', #18696, #31954, #2038 ) ;
#26990=ORIENTED_EDGE ( 'NONE', *, *, #26438, .T. ) ;
#27005=FACE_OUTER_BOUND ( 'NONE', #3153, .T. ) ;
#27006=FACE_OUTER_BOUND ( 'NONE', #8864, .T. ) ;
#27007=VECTOR ( 'NONE', #21538, 1000.000000000000000 ) ;
#27018=VECTOR ( 'NONE', #9455, 1000.000000000000000 ) ;
#27031=LINE ( 'NONE', #27236, #41508 ) ;
#27041=FACE_OUTER_BOUND ( 'NONE', #15342, .T. ) ;
#27044=ORIENTED_EDGE ( 'NONE', *, *, #27471, .T. ) ;
#27051=AXIS2_PLACEMENT_3D ( 'NONE', #286, #26954, #9504 ) ;
#27057=DIRECTION ( 'NONE',  ( 0.000000000000000000, 0.000000000000000000, 1.000000000000000000 ) ) ;
#27067=AXIS2_PLACEMENT_3D ( 'NONE', #30337, #40342, #39479 ) ;
#27069=CARTESIAN_POINT ( 'NONE',  ( 18.00000000000000355, 0.000000000000000000, 0.000000000000000000 ) ) ;
#27080=CIRCLE ( 'NONE', #34728, 20.00000000000000711 ) ;
#27085=DIRECTION ( 'NONE',  ( -1.000000000000000000, 0.000000000000000000, 0.000000000000000000 ) ) ;
#27086=ORIENTED_EDGE ( 'NONE', *, *, #21476, .T. ) ;
#27092=DIRECTION ( 'NONE',  ( 0.000000000000000000, 0.000000000000000000, 1.000000000000000000 ) ) ;
#27094=VERTEX_POINT ( 'NONE', #8039 ) ;
#27115=DIRECTION ( 'NONE',  ( -1.000000000000000000, -0.000000000000000000, -0.000000000000000000 ) ) ;
#27119=DIRECTION ( 'NONE',  ( 0.000000000000000000, -0.9048270524660145808, -0.4257792915650832066 ) ) ;
#27129=CIRCLE ( 'NONE', #4103, 20.00000000000000711 ) ;
#27135=CARTESIAN_POINT ( 'NONE',  ( 9.000000000000001776, 49.25004636492411692, -16.68630974939707556 ) ) ;
#27139=CIRCLE ( 'NONE', #18828, 51.99999999999999289 ) ;
#27152=DIRECTION ( 'NONE',  ( 1.000000000000000000, -0.000000000000000000, -0.000000000000000000 ) ) ;
#27153=DIRECTION ( 'NONE',  ( -1.000000000000000000, 0.000000000000000000, 0.000000000000000000 ) ) ;
#27157=EDGE_CURVE ( 'NONE', #17321, #16407, #24743, .T. ) ;
#27187=CARTESIAN_POINT ( 'NONE',  ( 9.000000000000001776, 7.162210897276454880, -51.50439529848819831 ) ) ;
#27189=CIRCLE ( 'NONE', #18167, 20.00000000000000355 ) ;
#27195=ORIENTED_EDGE ( 'NONE', *, *, #35282, .F. ) ;
#27201=EDGE_LOOP ( 'NONE', ( #5651, #8004, #28188, #13221 ) ) ;
#27214=VECTOR ( 'NONE', #21849, 1000.000000000000000 ) ;
#27221=CARTESIAN_POINT ( 'NONE',  ( -10.00000000000000000, 0.000000000000000000, 0.000000000000000000 ) ) ;
#27234=VERTEX_POINT ( 'NONE', #3176 ) ;
#27236=CARTESIAN_POINT ( 'NONE',  ( 18.00000000000000355, -24.72041153920704204, -40.55929306992713634 ) ) ;
#27240=EDGE_CURVE ( 'NONE', #11938, #2698, #12828, .T. ) ;
#27245=DIRECTION ( 'NONE',  ( -1.000000000000000000, -0.000000000000000000, -0.000000000000000000 ) ) ;
#27246=DIRECTION ( 'NONE',  ( 0.000000000000000000, 0.000000000000000000, 1.000000000000000000 ) ) ;
#27254=DIRECTION ( 'NONE',  ( -1.000000000000000000, 0.000000000000000000, -0.000000000000000000 ) ) ;
#27255=ORIENTED_EDGE ( 'NONE', *, *, #3409, .F. ) ;
#27281=VERTEX_POINT ( 'NONE', #19609 ) ;
#27288=DIRECTION ( 'NONE',  ( -1.000000000000000000, -0.000000000000000000, -0.000000000000000000 ) ) ;
#27296=DIRECTION ( 'NONE',  ( 0.000000000000000000, 0.000000000000000000, -1.000000000000000000 ) ) ;
#27297=EDGE_CURVE ( 'NONE', #24263, #38578, #39193, .T. ) ;
#27298=EDGE_LOOP ( 'NONE', ( #32797, #4400, #11386, #8150 ) ) ;
#27301=DIRECTION ( 'NONE',  ( 0.000000000000000000, 0.000000000000000000, 1.000000000000000000 ) ) ;
#27304=AXIS2_PLACEMENT_3D ( 'NONE', #38010, #41275, #18431 ) ;
#27308=AXIS2_PLACEMENT_3D ( 'NONE', #38272, #8386, #21752 ) ;
#27312=FACE_OUTER_BOUND ( 'NONE', #24273, .T. ) ;
#27315=AXIS2_PLACEMENT_3D ( 'NONE', #13151, #29085, #39713 ) ;
#27317=LINE ( 'NONE', #4153, #38616 ) ;
#27318=EDGE_CURVE ( 'NONE', #28779, #19793, #4266, .T. ) ;
#27319=CARTESIAN_POINT ( 'NONE',  ( 18.00000000000000355, 49.25004636492388954, 16.68630974939776834 ) ) ;
#27320=ORIENTED_EDGE ( 'NONE', *, *, #38485, .F. ) ;
#27321=DIRECTION ( 'NONE',  ( 1.000000000000000000, 0.000000000000000000, 0.000000000000000000 ) ) ;
#27327=PLANE ( 'NONE',  #4669 ) ;
#27334=CIRCLE ( 'NONE', #16893, 47.49900000000000233 ) ;
#27336=CIRCLE ( 'NONE', #39141, 52.00000000000000000 ) ;
#27338=DIRECTION ( 'NONE',  ( 0.000000000000000000, 0.000000000000000000, 1.000000000000000000 ) ) ;
#27343=VERTEX_POINT ( 'NONE', #27422 ) ;
#27345=EDGE_CURVE ( 'NONE', #26382, #28779, #14251, .T. ) ;
#27356=DIRECTION ( 'NONE',  ( 0.000000000000000000, -0.2486898871648415554, -0.9685831611286345177 ) ) ;
#27366=DIRECTION ( 'NONE',  ( 0.000000000000000000, -0.5877852522924624790, -0.8090169943749551118 ) ) ;
#27370=EDGE_CURVE ( 'NONE', #14587, #26032, #20691, .T. ) ;
#27372=ORIENTED_EDGE ( 'NONE', *, *, #26802, .F. ) ;
#27374=EDGE_CURVE ( 'NONE', #18374, #33890, #23324, .T. ) ;
#27381=DIRECTION ( 'NONE',  ( 0.000000000000000000, 0.000000000000000000, -1.000000000000000000 ) ) ;
#27388=DIRECTION ( 'NONE',  ( 0.000000000000000000, 0.8443279255020164076, -0.5358267949789947693 ) ) ;
#27390=ORIENTED_EDGE ( 'NONE', *, *, #30943, .T. ) ;
#27392=DIRECTION ( 'NONE',  ( 0.000000000000000000, -0.9822872507286865007, -0.1873813145857354812 ) ) ;
#27393=ADVANCED_FACE ( 'NONE', ( #4046 ), #23737, .T. ) ;
#27404=DIRECTION ( 'NONE',  ( -1.000000000000000000, 0.000000000000000000, 0.000000000000000000 ) ) ;
#27420=ADVANCED_FACE ( 'NONE', ( #34166 ), #39834, .T. ) ;
#27422=CARTESIAN_POINT ( 'NONE',  ( 18.00000000000000355, 8.053585752062561554, -46.81126742072013514 ) ) ;
#27424=CIRCLE ( 'NONE', #18432, 20.00000000000000000 ) ;
#27427=CARTESIAN_POINT ( 'NONE',  ( 18.00000000000000355, 8.053585752061904302, 46.81126742072025593 ) ) ;
#27432=DIRECTION ( 'NONE',  ( 0.000000000000000000, 0.000000000000000000, -1.000000000000000000 ) ) ;
#27436=CARTESIAN_POINT ( 'NONE',  ( 18.00000000000000355, 0.000000000000000000, 0.000000000000000000 ) ) ;
#27447=DIRECTION ( 'NONE',  ( 0.000000000000000000, 0.000000000000000000, 1.000000000000000000 ) ) ;
#27458=CARTESIAN_POINT ( 'NONE',  ( 18.00000000000000355, 44.47301969247445186, 16.68249143361925491 ) ) ;
#27460=CARTESIAN_POINT ( 'NONE',  ( 18.00000000000000355, -36.06787431788649911, -37.45808914225526820 ) ) ;
#27463=CYLINDRICAL_SURFACE ( 'NONE', #13371, 51.99999999999999289 ) ;
#27465=ORIENTED_EDGE ( 'NONE', *, *, #12742, .F. ) ;
#27471=EDGE_CURVE ( 'NONE', #291, #192, #22680, .T. ) ;
#27476=AXIS2_PLACEMENT_3D ( 'NONE', #31866, #32274, #8505 ) ;
#27480=VERTEX_POINT ( 'NONE', #40918 ) ;
#27496=CARTESIAN_POINT ( 'NONE',  ( 9.000000000000001776, -18.53613841426822972, 48.58406706613897086 ) ) ;
#27497=VECTOR ( 'NONE', #1536, 1000.000000000000000 ) ;
#27510=ORIENTED_EDGE ( 'NONE', *, *, #40986, .T. ) ;
#27511=AXIS2_PLACEMENT_3D ( 'NONE', #3300, #34233, #27720 ) ;
#27516=CARTESIAN_POINT ( 'NONE',  ( 18.00000000000000355, -43.83938735307255286, -18.28286404005844901 ) ) ;
#27524=DIRECTION ( 'NONE',  ( 0.000000000000000000, -0.3681245526846854133, 0.9297764858882485717 ) ) ;
#27530=VERTEX_POINT ( 'NONE', #41791 ) ;
#27533=DIRECTION ( 'NONE',  ( -1.000000000000000000, 0.000000000000000000, 0.000000000000000000 ) ) ;
#27541=EDGE_CURVE ( 'NONE', #18546, #8390, #21346, .T. ) ;
#27559=EDGE_CURVE ( 'NONE', #39944, #24642, #5365, .T. ) ;
#27569=AXIS2_PLACEMENT_3D ( 'NONE', #18489, #38292, #34810 ) ;
#27570=AXIS2_PLACEMENT_3D ( 'NONE', #5234, #15094, #32076 ) ;
#27579=CARTESIAN_POINT ( 'NONE',  ( 0.000000000000000000, 37.91532898920922889, 28.61088654061651937 ) ) ;
#27595=ORIENTED_EDGE ( 'NONE', *, *, #30132, .F. ) ;
#27596=DIRECTION ( 'NONE',  ( 0.000000000000000000, 0.9980267284282717810, -0.06279051952930989056 ) ) ;
#27611=CIRCLE ( 'NONE', #32451, 51.99999999999999289 ) ;
#27612=DIRECTION ( 'NONE',  ( -1.000000000000000000, 0.000000000000000000, -0.000000000000000000 ) ) ;
#27616=ORIENTED_EDGE ( 'NONE', *, *, #11207, .T. ) ;
#27617=CYLINDRICAL_SURFACE ( 'NONE', #25921, 20.00000000000000355 ) ;
#27628=DIRECTION ( 'NONE',  ( -1.000000000000000000, 0.000000000000000000, -0.000000000000000000 ) ) ;
#27633=DIRECTION ( 'NONE',  ( -1.000000000000000000, 0.000000000000000000, 0.000000000000000000 ) ) ;
#27638=VECTOR ( 'NONE', #33685, 1000.000000000000000 ) ;
#27649=CARTESIAN_POINT ( 'NONE',  ( 18.00000000000000355, -3.840921266749491192, -47.34345070675175293 ) ) ;
#27655=DIRECTION ( 'NONE',  ( 0.000000000000000000, 0.000000000000000000, 1.000000000000000000 ) ) ;
#27656=ADVANCED_FACE ( 'NONE', ( #2909 ), #15850, .T. ) ;
#27657=DIRECTION ( 'NONE',  ( -1.000000000000000000, 0.000000000000000000, 0.000000000000000000 ) ) ;
#27662=DIRECTION ( 'NONE',  ( 0.000000000000000000, 0.000000000000000000, 1.000000000000000000 ) ) ;
#27666=CARTESIAN_POINT ( 'NONE',  ( 18.00000000000000355, -42.03146605346801579, 22.12489237027304512 ) ) ;
#27668=EDGE_CURVE ( 'NONE', #7181, #16426, #3793, .T. ) ;
#27672=FACE_OUTER_BOUND ( 'NONE', #22319, .T. ) ;
#27680=ADVANCED_FACE ( 'NONE', ( #9268 ), #22844, .T. ) ;
#27682=AXIS2_PLACEMENT_3D ( 'NONE', #10858, #3834, #13929 ) ;
#27694=CARTESIAN_POINT ( 'NONE',  ( 18.00000000000000355, -39.55064067543082018, 25.36340625197346199 ) ) ;
#27696=DIRECTION ( 'NONE',  ( 0.000000000000000000, 0.000000000000000000, 1.000000000000000000 ) ) ;
#27720=DIRECTION ( 'NONE',  ( 0.000000000000000000, -0.8443279255020200713, 0.5358267949789887741 ) ) ;
#27722=ORIENTED_EDGE ( 'NONE', *, *, #19445, .F. ) ;
#27734=EDGE_CURVE ( 'NONE', #14255, #14013, #11548, .T. ) ;
#27737=ORIENTED_EDGE ( 'NONE', *, *, #5161, .T. ) ;
#27751=VERTEX_POINT ( 'NONE', #13870 ) ;
#27756=CARTESIAN_POINT ( 'NONE',  ( 0.000000000000000000, 0.000000000000000000, 0.000000000000000000 ) ) ;
#27762=ORIENTED_EDGE ( 'NONE', *, *, #9664, .F. ) ;
#27765=DIRECTION ( 'NONE',  ( 1.000000000000000000, 0.000000000000000000, 0.000000000000000000 ) ) ;
#27769=EDGE_CURVE ( 'NONE', #40629, #32031, #14315, .T. ) ;
#27773=AXIS2_PLACEMENT_3D ( 'NONE', #9062, #4936, #31992 ) ;
#27801=ADVANCED_FACE ( 'NONE', ( #23477 ), #3996, .T. ) ;
#27802=CYLINDRICAL_SURFACE ( 'NONE', #39327, 20.00000000000000711 ) ;
#27804=EDGE_LOOP ( 'NONE', ( #13337, #32042, #29668, #13597 ) ) ;
#27806=FACE_OUTER_BOUND ( 'NONE', #1876, .T. ) ;
#27822=VERTEX_POINT ( 'NONE', #17145 ) ;
#27826=VECTOR ( 'NONE', #16952, 1000.000000000000000 ) ;
#27830=VECTOR ( 'NONE', #7464, 1000.000000000000000 ) ;
#27831=ORIENTED_EDGE ( 'NONE', *, *, #21356, .F. ) ;
#27840=CARTESIAN_POINT ( 'NONE',  ( 18.00000000000000355, -32.32520163883560826, -34.09746168776070618 ) ) ;
#27847=CARTESIAN_POINT ( 'NONE',  ( 18.00000000000000355, -47.49120266317494554, -0.8606222198180160099 ) ) ;
#27849=CARTESIAN_POINT ( 'NONE',  ( 18.00000000000000355, -37.91532898920940653, 28.61088654061626357 ) ) ;
#27883=VERTEX_POINT ( 'NONE', #23907 ) ;
#27905=CARTESIAN_POINT ( 'NONE',  ( -10.00000000000000000, 0.000000000000000000, 0.000000000000000000 ) ) ;
#27910=EDGE_CURVE ( 'NONE', #15791, #14923, #1767, .T. ) ;
#27912=EDGE_CURVE ( 'NONE', #26032, #19113, #28283, .T. ) ;
#27914=VERTEX_POINT ( 'NONE', #6861 ) ;
#27920=CARTESIAN_POINT ( 'NONE',  ( 18.00000000000000355, 15.49408907645234201, -44.90087086784576087 ) ) ;
#27939=DIRECTION ( 'NONE',  ( -1.000000000000000000, -0.000000000000000000, -0.000000000000000000 ) ) ;
#27945=CARTESIAN_POINT ( 'NONE',  ( 0.000000000000000000, -11.46872990052412788, 45.56340405422441364 ) ) ;
#27946=VERTEX_POINT ( 'NONE', #13650 ) ;
#27951=DIRECTION ( 'NONE',  ( 0.000000000000000000, -0.9510565162951565288, 0.3090169943749383474 ) ) ;
#27953=AXIS2_PLACEMENT_3D ( 'NONE', #24201, #7577, #20937 ) ;
#27979=DIRECTION ( 'NONE',  ( -1.000000000000000000, -0.000000000000000000, -0.000000000000000000 ) ) ;
#27984=EDGE_CURVE ( 'NONE', #24128, #7783, #4535, .T. ) ;
#27999=FACE_OUTER_BOUND ( 'NONE', #14611, .T. ) ;
#28000=ORIENTED_EDGE ( 'NONE', *, *, #2848, .T. ) ;
#28002=CARTESIAN_POINT ( 'NONE',  ( 0.000000000000000000, 9.744342220504043084, -46.48873837489787064 ) ) ;
#28011=DIRECTION ( 'NONE',  ( 0.000000000000000000, 0.000000000000000000, 1.000000000000000000 ) ) ;
#28014=VERTEX_POINT ( 'NONE', #31078 ) ;
#28018=CIRCLE ( 'NONE', #15475, 52.00000000000000000 ) ;
#28020=CARTESIAN_POINT ( 'NONE',  ( 9.000000000000001776, -51.93417535146739539, -2.615612846549718817 ) ) ;
#28036=ORIENTED_EDGE ( 'NONE', *, *, #1849, .F. ) ;
#28038=VERTEX_POINT ( 'NONE', #11449 ) ;
#28043=EDGE_CURVE ( 'NONE', #14260, #6747, #27611, .T. ) ;
#28048=AXIS2_PLACEMENT_3D ( 'NONE', #19276, #29292, #12504 ) ;
#28051=DIRECTION ( 'NONE',  ( 0.000000000000000000, 0.9048270524660205760, -0.4257792915650702170 ) ) ;
#28058=DIRECTION ( 'NONE',  ( -1.000000000000000000, -0.000000000000000000, 0.000000000000000000 ) ) ;
#28081=EDGE_CURVE ( 'NONE', #17165, #22037, #28257, .T. ) ;
#28085=DIRECTION ( 'NONE',  ( 0.000000000000000000, 0.000000000000000000, 1.000000000000000000 ) ) ;
#28090=ADVANCED_FACE ( 'NONE', ( #1818 ), #11674, .T. ) ;
#28098=DIRECTION ( 'NONE',  ( 0.000000000000000000, 0.000000000000000000, -1.000000000000000000 ) ) ;
#28100=CARTESIAN_POINT ( 'NONE',  ( 0.000000000000000000, -32.32520163883560826, -34.09746168776070618 ) ) ;
#28114=VERTEX_POINT ( 'NONE', #4665 ) ;
#28118=ADVANCED_FACE ( 'NONE', ( #31302 ), #14734, .T. ) ;
#28127=CARTESIAN_POINT ( 'NONE',  ( -10.00000000000000000, 0.000000000000000000, 0.000000000000000000 ) ) ;
#28129=ORIENTED_EDGE ( 'NONE', *, *, #4821, .T. ) ;
#28131=LINE ( 'NONE', #29153, #2542 ) ;
#28134=VERTEX_POINT ( 'NONE', #5732 ) ;
#28141=DIRECTION ( 'NONE',  ( -1.000000000000000000, -0.000000000000000000, -0.000000000000000000 ) ) ;
#28145=CIRCLE ( 'NONE', #911, 52.00000000000000000 ) ;
#28147=ORIENTED_EDGE ( 'NONE', *, *, #17656, .T. ) ;
#28149=CARTESIAN_POINT ( 'NONE',  ( 18.00000000000000355, 36.34385289850590794, 29.77717097092089205 ) ) ;
#28154=ORIENTED_EDGE ( 'NONE', *, *, #3051, .F. ) ;
#28163=CIRCLE ( 'NONE', #16321, 47.49900000000000233 ) ;
#28171=AXIS2_PLACEMENT_3D ( 'NONE', #21161, #20946, #40516 ) ;
#28175=CARTESIAN_POINT ( 'NONE',  ( 18.00000000000000355, 0.000000000000000000, 0.000000000000000000 ) ) ;
#28182=CYLINDRICAL_SURFACE ( 'NONE', #39957, 20.00000000000001066 ) ;
#28185=EDGE_LOOP ( 'NONE', ( #15231, #12233, #12964, #4773 ) ) ;
#28188=ORIENTED_EDGE ( 'NONE', *, *, #37060, .T. ) ;
#28205=EDGE_LOOP ( 'NONE', ( #23220, #354, #24690, #487 ) ) ;
#28206=DIRECTION ( 'NONE',  ( -1.000000000000000000, -0.000000000000000000, -0.000000000000000000 ) ) ;
#28208=AXIS2_PLACEMENT_3D ( 'NONE', #7401, #3069, #16443 ) ;
#28209=EDGE_LOOP ( 'NONE', ( #30718, #33378, #6820, #1987 ) ) ;
#28210=EDGE_CURVE ( 'NONE', #15422, #15847, #15750, .T. ) ;
#28216=ORIENTED_EDGE ( 'NONE', *, *, #13847, .T. ) ;
#28217=AXIS2_PLACEMENT_3D ( 'NONE', #30923, #24416, #7788 ) ;
#28244=DIRECTION ( 'NONE',  ( 1.000000000000000000, 0.000000000000000000, 0.000000000000000000 ) ) ;
#28251=AXIS2_PLACEMENT_3D ( 'NONE', #3779, #16734, #40008 ) ;
#28257=LINE ( 'NONE', #11233, #40810 ) ;
#28262=DIRECTION ( 'NONE',  ( -1.000000000000000000, 0.000000000000000000, 0.000000000000000000 ) ) ;
#28265=CARTESIAN_POINT ( 'NONE',  ( 18.00000000000000355, -32.00046193115124282, -34.40241257139720688 ) ) ;
#28271=DIRECTION ( 'NONE',  ( -1.000000000000000000, 0.000000000000000000, 0.000000000000000000 ) ) ;
#28274=AXIS2_PLACEMENT_3D ( 'NONE', #32246, #23111, #29416 ) ;
#28275=ORIENTED_EDGE ( 'NONE', *, *, #41992, .F. ) ;
#28283=CIRCLE ( 'NONE', #7339, 20.00000000000000355 ) ;
#28284=EDGE_CURVE ( 'NONE', #18858, #28923, #30374, .T. ) ;
#28285=EDGE_CURVE ( 'NONE', #22037, #30654, #14348, .T. ) ;
#28286=CYLINDRICAL_SURFACE ( 'NONE', #25223, 20.00000000000000711 ) ;
#28289=AXIS2_PLACEMENT_3D ( 'NONE', #35829, #5547, #15597 ) ;
#28295=EDGE_LOOP ( 'NONE', ( #480, #15534, #3529, #14264 ) ) ;
#28300=EDGE_CURVE ( 'NONE', #170, #17739, #4565, .T. ) ;
#28302=CARTESIAN_POINT ( 'NONE',  ( 18.00000000000000355, 0.000000000000000000, 0.000000000000000000 ) ) ;
#28304=VERTEX_POINT ( 'NONE', #10679 ) ;
#28310=DIRECTION ( 'NONE',  ( -1.000000000000000000, -0.000000000000000000, -0.000000000000000000 ) ) ;
#28320=DIRECTION ( 'NONE',  ( 0.000000000000000000, 0.000000000000000000, 1.000000000000000000 ) ) ;
#28321=ORIENTED_EDGE ( 'NONE', *, *, #20020, .F. ) ;
#28322=DIRECTION ( 'NONE',  ( -1.000000000000000000, 0.000000000000000000, -0.000000000000000000 ) ) ;
#28323=FACE_OUTER_BOUND ( 'NONE', #29551, .T. ) ;
#28338=CARTESIAN_POINT ( 'NONE',  ( 0.000000000000000000, -43.83938735307280865, 18.28286404005783083 ) ) ;
#28341=ORIENTED_EDGE ( 'NONE', *, *, #27240, .F. ) ;
#28347=EDGE_CURVE ( 'NONE', #33317, #30585, #5331, .T. ) ;
#28350=ORIENTED_EDGE ( 'NONE', *, *, #14875, .F. ) ;
#28365=ORIENTED_EDGE ( 'NONE', *, *, #3078, .T. ) ;
#28368=CIRCLE ( 'NONE', #33905, 20.00000000000000355 ) ;
#28369=CIRCLE ( 'NONE', #2517, 52.00000000000000000 ) ;
#28372=AXIS2_PLACEMENT_3D ( 'NONE', #5092, #25636, #34550 ) ;
#28375=CARTESIAN_POINT ( 'NONE',  ( 0.000000000000000000, -42.60732521687585006, 19.80331771201644031 ) ) ;
#28379=LINE ( 'NONE', #38161, #29306 ) ;
#28384=ORIENTED_EDGE ( 'NONE', *, *, #12742, .T. ) ;
#28385=CARTESIAN_POINT ( 'NONE',  ( 9.000000000000001776, -35.11945359308084136, -38.34871548466050228 ) ) ;
#28390=ORIENTED_EDGE ( 'NONE', *, *, #11595, .T. ) ;
#28394=DIRECTION ( 'NONE',  ( -1.000000000000000000, 0.000000000000000000, -0.000000000000000000 ) ) ;
#28397=DIRECTION ( 'NONE',  ( 0.000000000000000000, 0.000000000000000000, 1.000000000000000000 ) ) ;
#28406=EDGE_LOOP ( 'NONE', ( #9547, #6448, #33502, #30929 ) ) ;
#28409=DIRECTION ( 'NONE',  ( -1.000000000000000000, 0.000000000000000000, 0.000000000000000000 ) ) ;
#28416=DIRECTION ( 'NONE',  ( 0.000000000000000000, 0.000000000000000000, 1.000000000000000000 ) ) ;
#28425=DIRECTION ( 'NONE',  ( -1.000000000000000000, -0.000000000000000000, 0.000000000000000000 ) ) ;
#28434=AXIS2_PLACEMENT_3D ( 'NONE', #40929, #37663, #34181 ) ;
#28438=LINE ( 'NONE', #29438, #15087 ) ;
#28439=ORIENTED_EDGE ( 'NONE', *, *, #27374, .T. ) ;
#28443=ORIENTED_EDGE ( 'NONE', *, *, #40167, .F. ) ;
#28444=DIRECTION ( 'NONE',  ( -1.000000000000000000, -0.000000000000000000, -0.000000000000000000 ) ) ;
#28458=DIRECTION ( 'NONE',  ( 0.000000000000000000, 0.000000000000000000, -1.000000000000000000 ) ) ;
#28462=ORIENTED_EDGE ( 'NONE', *, *, #10671, .T. ) ;
#28463=CIRCLE ( 'NONE', #27773, 20.00000000000001066 ) ;
#28471=CARTESIAN_POINT ( 'NONE',  ( 9.000000000000001776, 24.47917365149946534, 45.87777302070942653 ) ) ;
#28476=ADVANCED_FACE ( 'NONE', ( #5632 ), #12206, .T. ) ;
#28477=ORIENTED_EDGE ( 'NONE', *, *, #24741, .F. ) ;
#28482=CIRCLE ( 'NONE', #19418, 47.49900000000000233 ) ;
#28494=DIRECTION ( 'NONE',  ( 0.000000000000000000, -0.6845471059286791782, -0.7289686274214204342 ) ) ;
#28495=CARTESIAN_POINT ( 'NONE',  ( 0.000000000000000000, 41.20225022064636278, 23.63323037071415911 ) ) ;
#28506=ORIENTED_EDGE ( 'NONE', *, *, #34824, .F. ) ;
#28517=ORIENTED_EDGE ( 'NONE', *, *, #4140, .F. ) ;
#28524=ORIENTED_EDGE ( 'NONE', *, *, #7235, .T. ) ;
#28535=ADVANCED_FACE ( 'NONE', ( #11788 ), #15698, .T. ) ;
#28557=DIRECTION ( 'NONE',  ( 0.000000000000000000, 0.000000000000000000, -1.000000000000000000 ) ) ;
#28561=DIRECTION ( 'NONE',  ( 0.000000000000000000, 0.000000000000000000, 1.000000000000000000 ) ) ;
#28565=CARTESIAN_POINT ( 'NONE',  ( 9.000000000000001776, 50.95304419620823921, 10.38206564895679307 ) ) ;
#28566=EDGE_LOOP ( 'NONE', ( #18881, #29653, #28154, #14317 ) ) ;
#28567=CARTESIAN_POINT ( 'NONE',  ( 0.000000000000000000, -35.20873326984057883, -31.88259874184068465 ) ) ;
#28602=DIRECTION ( 'NONE',  ( -1.000000000000000000, -0.000000000000000000, -0.000000000000000000 ) ) ;
#28603=CIRCLE ( 'NONE', #9044, 20.00000000000000711 ) ;
#28607=CYLINDRICAL_SURFACE ( 'NONE', #19926, 47.49900000000000233 ) ;
#28617=VERTEX_POINT ( 'NONE', #5842 ) ;
#28634=ORIENTED_EDGE ( 'NONE', *, *, #7944, .T. ) ;
#28639=CARTESIAN_POINT ( 'NONE',  ( 18.00000000000000355, -34.03046037009231384, -33.13733193845841640 ) ) ;
#28640=EDGE_CURVE ( 'NONE', #37184, #170, #22474, .T. ) ;
#28651=DIRECTION ( 'NONE',  ( -1.000000000000000000, 0.000000000000000000, 0.000000000000000000 ) ) ;
#28659=EDGE_CURVE ( 'NONE', #20160, #4825, #15781, .T. ) ;
#28666=ORIENTED_EDGE ( 'NONE', *, *, #12087, .T. ) ;
#28672=DIRECTION ( 'NONE',  ( 0.000000000000000000, -0.3681245526846653737, -0.9297764858882564543 ) ) ;
#28679=VERTEX_POINT ( 'NONE', #16123 ) ;
#28680=CYLINDRICAL_SURFACE ( 'NONE', #14375, 47.49900000000000233 ) ;
#28684=EDGE_CURVE ( 'NONE', #24642, #7094, #15116, .T. ) ;
#28689=ORIENTED_EDGE ( 'NONE', *, *, #6964, .T. ) ;
#28692=DIRECTION ( 'NONE',  ( -1.000000000000000000, -0.000000000000000000, -0.000000000000000000 ) ) ;
#28694=EDGE_CURVE ( 'NONE', #30637, #27094, #23755, .T. ) ;
#28697=DIRECTION ( 'NONE',  ( -1.000000000000000000, 0.000000000000000000, 0.000000000000000000 ) ) ;
#28698=ADVANCED_FACE ( 'NONE', ( #14145 ), #10417, .T. ) ;
#28699=ORIENTED_EDGE ( 'NONE', *, *, #650, .F. ) ;
#28702=CIRCLE ( 'NONE', #29405, 52.00000000000000000 ) ;
#28705=ORIENTED_EDGE ( 'NONE', *, *, #28210, .F. ) ;
#28710=ORIENTED_EDGE ( 'NONE', *, *, #40596, .F. ) ;
#28712=EDGE_CURVE ( 'NONE', #38951, #27883, #40871, .T. ) ;
#28716=EDGE_CURVE ( 'NONE', #35102, #31882, #33973, .T. ) ;
#28729=EDGE_LOOP ( 'NONE', ( #40425, #42932, #10258, #34251 ) ) ;
#28730=VECTOR ( 'NONE', #39906, 1000.000000000000000 ) ;
#28736=CYLINDRICAL_SURFACE ( 'NONE', #3446, 47.49900000000000233 ) ;
#28737=EDGE_CURVE ( 'NONE', #16328, #11213, #17435, .T. ) ;
#28745=CARTESIAN_POINT ( 'NONE',  ( 0.000000000000000000, -46.19362259308827845, -8.585149169758995669 ) ) ;
#28756=FACE_OUTER_BOUND ( 'NONE', #9940, .T. ) ;
#28758=ORIENTED_EDGE ( 'NONE', *, *, #24530, .F. ) ;
#28761=AXIS2_PLACEMENT_3D ( 'NONE', #25352, #19448, #32713 ) ;
#28768=EDGE_CURVE ( 'NONE', #31266, #1103, #40286, .T. ) ;
#28777=ORIENTED_EDGE ( 'NONE', *, *, #26850, .F. ) ;
#28779=VERTEX_POINT ( 'NONE', #33746 ) ;
#28780=EDGE_CURVE ( 'NONE', #39186, #31919, #14409, .T. ) ;
#28791=DIRECTION ( 'NONE',  ( -1.000000000000000000, -0.000000000000000000, -0.000000000000000000 ) ) ;
#28792=CARTESIAN_POINT ( 'NONE',  ( 0.000000000000000000, 0.000000000000000000, 0.000000000000000000 ) ) ;
#28795=DIRECTION ( 'NONE',  ( 0.000000000000000000, 0.000000000000000000, 1.000000000000000000 ) ) ;
#28812=EDGE_CURVE ( 'NONE', #36747, #41807, #38518, .T. ) ;
#28813=FACE_OUTER_BOUND ( 'NONE', #4284, .T. ) ;
#28817=ORIENTED_EDGE ( 'NONE', *, *, #32254, .T. ) ;
#28819=CARTESIAN_POINT ( 'NONE',  ( 18.00000000000000355, -49.65209126885751800, -15.44894276735603178 ) ) ;
#28822=DIRECTION ( 'NONE',  ( 0.000000000000000000, 0.000000000000000000, 1.000000000000000000 ) ) ;
#28828=DIRECTION ( 'NONE',  ( -1.000000000000000000, 0.000000000000000000, 0.000000000000000000 ) ) ;
#28829=ADVANCED_FACE ( 'NONE', ( #24848 ), #4946, .T. ) ;
#28831=CIRCLE ( 'NONE', #7209, 51.99999999999999289 ) ;
#28836=CARTESIAN_POINT ( 'NONE',  ( 18.00000000000000355, 45.78515115856043138, 12.64416602183680993 ) ) ;
#28849=VERTEX_POINT ( 'NONE', #12157 ) ;
#28852=CYLINDRICAL_SURFACE ( 'NONE', #18170, 51.99999999999999289 ) ;
#28856=VECTOR ( 'NONE', #14884, 1000.000000000000000 ) ;
#28862=DIRECTION ( 'NONE',  ( 0.000000000000000000, 0.7705132427757861446, 0.6374239897486935202 ) ) ;
#28880=CIRCLE ( 'NONE', #34430, 20.00000000000000355 ) ;
#28894=ORIENTED_EDGE ( 'NONE', *, *, #13539, .T. ) ;
#28895=CARTESIAN_POINT ( 'NONE',  ( 0.000000000000000000, 0.000000000000000000, 0.000000000000000000 ) ) ;
#28896=VERTEX_POINT ( 'NONE', #38740 ) ;
#28902=CYLINDRICAL_SURFACE ( 'NONE', #31755, 20.00000000000000711 ) ;
#28913=CIRCLE ( 'NONE', #30987, 20.00000000000000711 ) ;
#28923=VERTEX_POINT ( 'NONE', #29378 ) ;
#28935=VECTOR ( 'NONE', #5307, 1000.000000000000000 ) ;
#28945=ORIENTED_EDGE ( 'NONE', *, *, #30231, .F. ) ;
#28965=CARTESIAN_POINT ( 'NONE',  ( 18.00000000000000355, 25.61928775981044026, 45.25098998563485964 ) ) ;
#28966=VERTEX_POINT ( 'NONE', #13231 ) ;
#28968=DIRECTION ( 'NONE',  ( -1.000000000000000000, -0.000000000000000000, -0.000000000000000000 ) ) ;
#28975=DIRECTION ( 'NONE',  ( -1.000000000000000000, 0.000000000000000000, -0.000000000000000000 ) ) ;
#28985=AXIS2_PLACEMENT_3D ( 'NONE', #7320, #4260, #7762 ) ;
#28990=AXIS2_PLACEMENT_3D ( 'NONE', #10465, #3665, #8046 ) ;
#28999=VERTEX_POINT ( 'NONE', #23068 ) ;
#29001=EDGE_CURVE ( 'NONE', #31415, #39812, #26321, .T. ) ;
#29003=DIRECTION ( 'NONE',  ( -1.000000000000000000, 0.000000000000000000, 0.000000000000000000 ) ) ;
#29004=EDGE_CURVE ( 'NONE', #40767, #18955, #41604, .T. ) ;
#29006=EDGE_CURVE ( 'NONE', #29967, #5490, #26105, .T. ) ;
#29010=LINE ( 'NONE', #29219, #8625 ) ;
#29012=LINE ( 'NONE', #12847, #10514 ) ;
#29025=ORIENTED_EDGE ( 'NONE', *, *, #17151, .T. ) ;
#29031=CARTESIAN_POINT ( 'NONE',  ( 18.00000000000000355, 47.22458491092827160, -5.098390039073737334 ) ) ;
#29032=UNCERTAINTY_MEASURE_WITH_UNIT (LENGTH_MEASURE( 1.000000000000000082E-05 ), #12352, 'distance_accuracy_value', 'NONE');
#29036=CIRCLE ( 'NONE', #429, 47.49900000000000233 ) ;
#29038=CARTESIAN_POINT ( 'NONE',  ( 18.00000000000000355, -19.74581912682875284, 48.10512059033386123 ) ) ;
#29041=VECTOR ( 'NONE', #20678, 1000.000000000000000 ) ;
#29042=CIRCLE ( 'NONE', #3920, 20.00000000000000711 ) ;
#29048=ORIENTED_EDGE ( 'NONE', *, *, #12799, .T. ) ;
#29065=CIRCLE ( 'NONE', #13032, 47.49900000000000233 ) ;
#29073=CIRCLE ( 'NONE', #37423, 47.49900000000000233 ) ;
#29079=ORIENTED_EDGE ( 'NONE', *, *, #41089, .T. ) ;
#29080=DIRECTION ( 'NONE',  ( 0.000000000000000000, 0.4817536741017102164, 0.8763066800438664705 ) ) ;
#29081=CIRCLE ( 'NONE', #15180, 20.00000000000000711 ) ;
#29083=AXIS2_PLACEMENT_3D ( 'NONE', #3981, #33459, #36495 ) ;
#29085=DIRECTION ( 'NONE',  ( -1.000000000000000000, 0.000000000000000000, -0.000000000000000000 ) ) ;
#29087=DIRECTION ( 'NONE',  ( 0.000000000000000000, 0.6845471059286899473, -0.7289686274214103312 ) ) ;
#29102=ORIENTED_EDGE ( 'NONE', *, *, #12238, .F. ) ;
#29114=CARTESIAN_POINT ( 'NONE',  ( 18.00000000000000355, 11.90021268425555512, 45.45261810511218670 ) ) ;
#29137=EDGE_LOOP ( 'NONE', ( #36688, #40641, #8163, #26378 ) ) ;
#29138=AXIS2_PLACEMENT_3D ( 'NONE', #26446, #39716, #29945 ) ;
#29145=DIRECTION ( 'NONE',  ( -1.000000000000000000, -0.000000000000000000, -0.000000000000000000 ) ) ;
#29147=EDGE_CURVE ( 'NONE', #28134, #1396, #11675, .T. ) ;
#29153=CARTESIAN_POINT ( 'NONE',  ( 18.00000000000000355, 26.17370628620709638, -39.63700417846136048 ) ) ;
#29176=ORIENTED_EDGE ( 'NONE', *, *, #29222, .F. ) ;
#29182=DIRECTION ( 'NONE',  ( 0.000000000000000000, 0.9510565162951521989, 0.3090169943749515036 ) ) ;
#29216=VECTOR ( 'NONE', #5390, 1000.000000000000000 ) ;
#29219=CARTESIAN_POINT ( 'NONE',  ( -132.0000507999999968, 0.000000000000000000, -11.00000000000000000 ) ) ;
#29222=EDGE_CURVE ( 'NONE', #12187, #26511, #20757, .T. ) ;
#29225=DIRECTION ( 'NONE',  ( -1.000000000000000000, 0.000000000000000000, 0.000000000000000000 ) ) ;
#29227=DIRECTION ( 'NONE',  ( 0.000000000000000000, 0.000000000000000000, 1.000000000000000000 ) ) ;
#29229=DIRECTION ( 'NONE',  ( 1.000000000000000000, 0.000000000000000000, 0.000000000000000000 ) ) ;
#29234=ORIENTED_EDGE ( 'NONE', *, *, #9204, .T. ) ;
#29238=DIRECTION ( 'NONE',  ( 0.000000000000000000, 0.000000000000000000, 1.000000000000000000 ) ) ;
#29239=ORIENTED_EDGE ( 'NONE', *, *, #26610, .T. ) ;
#29248=AXIS2_PLACEMENT_3D ( 'NONE', #16215, #10298, #23643 ) ;
#29253=DIRECTION ( 'NONE',  ( 0.000000000000000000, 0.8443279255020126328, 0.5358267949790005424 ) ) ;
#29266=EDGE_CURVE ( 'NONE', #30887, #31904, #1892, .T. ) ;
#29269=DIRECTION ( 'NONE',  ( 0.000000000000000000, 0.2486898871648552389, -0.9685831611286310761 ) ) ;
#29275=CARTESIAN_POINT ( 'NONE',  ( 18.00000000000000355, 19.44205635905601781, -43.33776004284589334 ) ) ;
#29278=DIRECTION ( 'NONE',  ( 0.000000000000000000, 0.000000000000000000, 1.000000000000000000 ) ) ;
#29281=CARTESIAN_POINT ( 'NONE',  ( 18.00000000000000355, 0.000000000000000000, 0.000000000000000000 ) ) ;
#29284=FACE_OUTER_BOUND ( 'NONE', #28209, .T. ) ;
#29286=DIRECTION ( 'NONE',  ( -1.000000000000000000, -0.000000000000000000, -0.000000000000000000 ) ) ;
#29290=DIRECTION ( 'NONE',  ( -1.000000000000000000, 0.000000000000000000, 0.000000000000000000 ) ) ;
#29291=ADVANCED_FACE ( 'NONE', ( #8587 ), #18047, .T. ) ;
#29292=DIRECTION ( 'NONE',  ( -1.000000000000000000, -0.000000000000000000, -0.000000000000000000 ) ) ;
#29296=DIRECTION ( 'NONE',  ( 0.000000000000000000, 0.000000000000000000, 1.000000000000000000 ) ) ;
#29306=VECTOR ( 'NONE', #37935, 1000.000000000000000 ) ;
#29316=CARTESIAN_POINT ( 'NONE',  ( 18.00000000000000355, -2.123073309835499245, 47.45152853935333326 ) ) ;
#29318=CARTESIAN_POINT ( 'NONE',  ( 9.000000000000001776, -24.47917365149977798, 45.87777302070926311 ) ) ;
#29326=ORIENTED_EDGE ( 'NONE', *, *, #17310, .F. ) ;
#29327=CARTESIAN_POINT ( 'NONE',  ( 18.00000000000000355, -22.82995208772716467, 41.06517797613655318 ) ) ;
#29332=AXIS2_PLACEMENT_3D ( 'NONE', #39811, #35896, #23287 ) ;
#29349=EDGE_CURVE ( 'NONE', #9628, #38193, #2559, .T. ) ;
#29357=CARTESIAN_POINT ( 'NONE',  ( 0.000000000000000000, 0.000000000000000000, 0.000000000000000000 ) ) ;
#29360=CARTESIAN_POINT ( 'NONE',  ( 18.00000000000000355, -17.08890430202718491, -43.76671000081963570 ) ) ;
#29361=ORIENTED_EDGE ( 'NONE', *, *, #34845, .F. ) ;
#29368=DIRECTION ( 'NONE',  ( -1.000000000000000000, 0.000000000000000000, 0.000000000000000000 ) ) ;
#29376=EDGE_LOOP ( 'NONE', ( #6011, #29767, #12489, #12132 ) ) ;
#29377=VECTOR ( 'NONE', #26179, 1000.000000000000000 ) ;
#29378=CARTESIAN_POINT ( 'NONE',  ( 18.00000000000000355, 40.47821179127761582, -32.64221760512715065 ) ) ;
#29384=DIRECTION ( 'NONE',  ( 0.000000000000000000, 0.1253332335643045359, -0.9921147013144778759 ) ) ;
#29386=ORIENTED_EDGE ( 'NONE', *, *, #31777, .T. ) ;
#29394=DIRECTION ( 'NONE',  ( -1.000000000000000000, 0.000000000000000000, 0.000000000000000000 ) ) ;
#29401=CARTESIAN_POINT ( 'NONE',  ( 9.000000000000001776, -44.25018368420761306, 27.31155879685165644 ) ) ;
#29405=AXIS2_PLACEMENT_3D ( 'NONE', #6616, #29778, #12985 ) ;
#29407=CARTESIAN_POINT ( 'NONE',  ( 18.00000000000000355, 51.19683565102443623, 9.104066087303637644 ) ) ;
#29416=DIRECTION ( 'NONE',  ( 0.000000000000000000, 0.000000000000000000, -1.000000000000000000 ) ) ;
#29421=AXIS2_PLACEMENT_3D ( 'NONE', #9361, #12458, #6304 ) ;
#29427=CIRCLE ( 'NONE', #34989, 47.49899999999999523 ) ;
#29434=LINE ( 'NONE', #39858, #13150 ) ;
#29435=EDGE_CURVE ( 'NONE', #38773, #30637, #17995, .T. ) ;
#29438=CARTESIAN_POINT ( 'NONE',  ( 9.000000000000001776, 13.56094713063641599, -50.20060470671725739 ) ) ;
#29446=FACE_OUTER_BOUND ( 'NONE', #1134, .T. ) ;
#29447=LINE ( 'NONE', #6090, #26817 ) ;
#29450=DIRECTION ( 'NONE',  ( 1.000000000000000000, -0.000000000000000000, -0.000000000000000000 ) ) ;
#29457=DIRECTION ( 'NONE',  ( -1.000000000000000000, -0.000000000000000000, -0.000000000000000000 ) ) ;
#29461=EDGE_CURVE ( 'NONE', #9021, #25059, #11711, .T. ) ;
#29465=CARTESIAN_POINT ( 'NONE',  ( 150.0000507999999968, 0.000000000000000000, 7.500000000000000000 ) ) ;
#29470=CARTESIAN_POINT ( 'NONE',  ( 18.00000000000000355, 32.32520163883631170, -34.09746168776002406 ) ) ;
#29473=DIRECTION ( 'NONE',  ( 0.000000000000000000, 0.2486898871648483278, 0.9685831611286327414 ) ) ;
#29484=VERTEX_POINT ( 'NONE', #12321 ) ;
#29486=ORIENTED_EDGE ( 'NONE', *, *, #14932, .F. ) ;
#29505=VECTOR ( 'NONE', #9815, 1000.000000000000000 ) ;
#29507=ORIENTED_EDGE ( 'NONE', *, *, #3562, .T. ) ;
#29512=DIRECTION ( 'NONE',  ( 0.000000000000000000, 0.8443279255020126328, 0.5358267949790005424 ) ) ;
#29522=DIRECTION ( 'NONE',  ( 0.000000000000000000, 0.000000000000000000, 1.000000000000000000 ) ) ;
#29527=CARTESIAN_POINT ( 'NONE',  ( 0.000000000000000000, 46.87740477351712798, 3.172455868806036694 ) ) ;
#29532=CARTESIAN_POINT ( 'NONE',  ( 18.00000000000000355, -11.90021268425586953, 45.45261810511210143 ) ) ;
#29534=EDGE_CURVE ( 'NONE', #3223, #7181, #30820, .T. ) ;
#29538=DIRECTION ( 'NONE',  ( 0.000000000000000000, 0.000000000000000000, 1.000000000000000000 ) ) ;
#29546=ORIENTED_EDGE ( 'NONE', *, *, #10010, .F. ) ;
#29551=EDGE_LOOP ( 'NONE', ( #42422, #22167, #13906, #13979 ) ) ;
#29554=DIRECTION ( 'NONE',  ( -1.000000000000000000, -0.000000000000000000, -0.000000000000000000 ) ) ;
#29556=CARTESIAN_POINT ( 'NONE',  ( 0.000000000000000000, -44.61570720899106846, 14.73072383765551940 ) ) ;
#29568=DIRECTION ( 'NONE',  ( -1.000000000000000000, -0.000000000000000000, -0.000000000000000000 ) ) ;
#29575=CYLINDRICAL_SURFACE ( 'NONE', #35272, 20.00000000000000355 ) ;
#29586=EDGE_CURVE ( 'NONE', #4825, #12961, #24275, .T. ) ;
#29588=DIRECTION ( 'NONE',  ( -1.000000000000000000, 0.000000000000000000, 0.000000000000000000 ) ) ;
#29590=CARTESIAN_POINT ( 'NONE',  ( 0.000000000000000000, -3.840921266749489860, -47.34345070675173872 ) ) ;
#29593=EDGE_CURVE ( 'NONE', #21090, #5484, #11017, .T. ) ;
#29598=CARTESIAN_POINT ( 'NONE',  ( 18.00000000000000355, -50.95304419620816105, -10.38206564895716610 ) ) ;
#29600=FACE_OUTER_BOUND ( 'NONE', #13716, .T. ) ;
#29602=UNCERTAINTY_MEASURE_WITH_UNIT (LENGTH_MEASURE( 1.000000000000000082E-05 ), #26675, 'distance_accuracy_value', 'NONE');
#29611=DIRECTION ( 'NONE',  ( 0.000000000000000000, 0.000000000000000000, 1.000000000000000000 ) ) ;
#29612=ORIENTED_EDGE ( 'NONE', *, *, #25146, .F. ) ;
#29622=VECTOR ( 'NONE', #6988, 1000.000000000000000 ) ;
#29646=LINE ( 'NONE', #39648, #31957 ) ;
#29648=ORIENTED_EDGE ( 'NONE', *, *, #5293, .F. ) ;
#29653=ORIENTED_EDGE ( 'NONE', *, *, #3740, .T. ) ;
#29655=AXIS2_PLACEMENT_3D ( 'NONE', #8507, #42077, #41671 ) ;
#29658=ORIENTED_EDGE ( 'NONE', *, *, #43155, .F. ) ;
#29662=CYLINDRICAL_SURFACE ( 'NONE', #22391, 51.99999999999999289 ) ;
#29663=CARTESIAN_POINT ( 'NONE',  ( 18.00000000000000355, -5.667686777402029641, 46.64153600743603789 ) ) ;
#29664=EDGE_CURVE ( 'NONE', #36583, #40692, #35375, .T. ) ;
#29667=FACE_OUTER_BOUND ( 'NONE', #21047, .T. ) ;
#29668=ORIENTED_EDGE ( 'NONE', *, *, #21562, .T. ) ;
#29669=FACE_OUTER_BOUND ( 'NONE', #35897, .T. ) ;
#29670=AXIS2_PLACEMENT_3D ( 'NONE', #34998, #12536, #9238 ) ;
#29672=DIRECTION ( 'NONE',  ( -1.000000000000000000, 0.000000000000000000, 0.000000000000000000 ) ) ;
#29684=AXIS2_PLACEMENT_3D ( 'NONE', #17676, #10656, #18123 ) ;
#29701=ORIENTED_EDGE ( 'NONE', *, *, #7894, .F. ) ;
#29702=CARTESIAN_POINT ( 'NONE',  ( 18.00000000000000355, -11.90021268425522827, -45.45261810511227907 ) ) ;
#29713=AXIS2_PLACEMENT_3D ( 'NONE', #3388, #3162, #29611 ) ;
#29718=VECTOR ( 'NONE', #19295, 1000.000000000000000 ) ;
#29733=CARTESIAN_POINT ( 'NONE',  ( -132.0000507999999968, 1.347111479062088405E-15, 11.00000000000000000 ) ) ;
#29740=ORIENTED_EDGE ( 'NONE', *, *, #25288, .T. ) ;
#29745=AXIS2_PLACEMENT_3D ( 'NONE', #23941, #16967, #316 ) ;
#29750=LINE ( 'NONE', #29318, #36109 ) ;
#29751=VERTEX_POINT ( 'NONE', #24524 ) ;
#29756=VECTOR ( 'NONE', #30919, 1000.000000000000000 ) ;
#29763=AXIS2_PLACEMENT_3D ( 'NONE', #12451, #28394, #22497 ) ;
#29766=DIRECTION ( 'NONE',  ( 0.000000000000000000, 0.000000000000000000, 1.000000000000000000 ) ) ;
#29767=ORIENTED_EDGE ( 'NONE', *, *, #39782, .F. ) ;
#29778=DIRECTION ( 'NONE',  ( -1.000000000000000000, -0.000000000000000000, -0.000000000000000000 ) ) ;
#29781=ORIENTED_EDGE ( 'NONE', *, *, #3078, .F. ) ;
#29789=LINE ( 'NONE', #13209, #31695 ) ;
#29791=EDGE_CURVE ( 'NONE', #16, #31395, #1121, .T. ) ;
#29799=ADVANCED_FACE ( 'NONE', ( #27999 ), #5054, .T. ) ;
#29800=VECTOR ( 'NONE', #10723, 1000.000000000000000 ) ;
#29804=DIRECTION ( 'NONE',  ( -1.000000000000000000, 0.000000000000000000, 0.000000000000000000 ) ) ;
#29805=DIRECTION ( 'NONE',  ( -1.000000000000000000, 0.000000000000000000, 0.000000000000000000 ) ) ;
#29810=DIRECTION ( 'NONE',  ( 0.000000000000000000, 0.000000000000000000, 1.000000000000000000 ) ) ;
#29815=LINE ( 'NONE', #17164, #2397 ) ;
#29820=VECTOR ( 'NONE', #41657, 1000.000000000000000 ) ;
#29821=EDGE_CURVE ( 'NONE', #36216, #18546, #8200, .T. ) ;
#29823=CIRCLE ( 'NONE', #41665, 20.00000000000000355 ) ;
#29825=ORIENTED_EDGE ( 'NONE', *, *, #40986, .F. ) ;
#29832=ORIENTED_EDGE ( 'NONE', *, *, #17576, .F. ) ;
#29837=DIRECTION ( 'NONE',  ( 0.000000000000000000, -0.1253332335643113082, 0.9921147013144769877 ) ) ;
#29842=DIRECTION ( 'NONE',  ( 0.000000000000000000, 0.1253332335642974860, 0.9921147013144787641 ) ) ;
#29845=CARTESIAN_POINT ( 'NONE',  ( 0.000000000000000000, -13.85708833599999323, 45.43276465116659324 ) ) ;
#29850=ORIENTED_EDGE ( 'NONE', *, *, #22395, .T. ) ;
#29852=EDGE_CURVE ( 'NONE', #36282, #17321, #22532, .T. ) ;
#29854=AXIS2_PLACEMENT_3D ( 'NONE', #37014, #1221, #13920 ) ;
#29883=DIRECTION ( 'NONE',  ( 0.000000000000000000, 0.000000000000000000, -1.000000000000000000 ) ) ;
#29889=ORIENTED_EDGE ( 'NONE', *, *, #8813, .F. ) ;
#29896=DIRECTION ( 'NONE',  ( -1.000000000000000000, -0.000000000000000000, 0.000000000000000000 ) ) ;
#29903=EDGE_CURVE ( 'NONE', #21574, #21438, #4024, .T. ) ;
#29919=CARTESIAN_POINT ( 'NONE',  ( 0.000000000000000000, 0.000000000000000000, 0.000000000000000000 ) ) ;
#29923=LINE ( 'NONE', #6973, #25005 ) ;
#29925=DIRECTION ( 'NONE',  ( 0.000000000000000000, -0.7705132427757815927, -0.6374239897486989603 ) ) ;
#29937=CARTESIAN_POINT ( 'NONE',  ( -10.00000000000000000, 0.000000000000000000, 0.000000000000000000 ) ) ;
#29942=CARTESIAN_POINT ( 'NONE',  ( 18.00000000000000355, 0.000000000000000000, 0.000000000000000000 ) ) ;
#29945=DIRECTION ( 'NONE',  ( 0.000000000000000000, -0.7705132427757950264, 0.6374239897486826401 ) ) ;
#29947=EDGE_LOOP ( 'NONE', ( #10861, #41432, #18708, #40841 ) ) ;
#29958=ORIENTED_EDGE ( 'NONE', *, *, #7879, .T. ) ;
#29967=VERTEX_POINT ( 'NONE', #25375 ) ;
#29968=LINE ( 'NONE', #43024, #23608 ) ;
#29971=CARTESIAN_POINT ( 'NONE',  ( 0.000000000000000000, -46.90537658765328644, -2.727856614654796452 ) ) ;
#29985=EDGE_CURVE ( 'NONE', #28114, #28849, #9180, .T. ) ;
#29999=LINE ( 'NONE', #33254, #5640 ) ;
#30012=CARTESIAN_POINT ( 'NONE',  ( 9.000000000000001776, 25.61928775981044382, 45.25098998563486674 ) ) ;
#30020=DIRECTION ( 'NONE',  ( -1.000000000000000000, -0.000000000000000000, -0.000000000000000000 ) ) ;
#30028=EDGE_LOOP ( 'NONE', ( #23531, #38597, #36610, #34410 ) ) ;
#30033=DIRECTION ( 'NONE',  ( 0.000000000000000000, 0.000000000000000000, 1.000000000000000000 ) ) ;
#30037=CARTESIAN_POINT ( 'NONE',  ( 18.00000000000000355, 36.05989434073656952, -30.12041790338580682 ) ) ;
#30041=VERTEX_POINT ( 'NONE', #17053 ) ;
#30043=CARTESIAN_POINT ( 'NONE',  ( -10.00000000000000000, 0.000000000000000000, 0.000000000000000000 ) ) ;
#30045=LINE ( 'NONE', #36775, #7636 ) ;
#30055=DIRECTION ( 'NONE',  ( 0.000000000000000000, 0.000000000000000000, 1.000000000000000000 ) ) ;
#30080=CARTESIAN_POINT ( 'NONE',  ( 0.000000000000000000, -17.50309955389642269, 43.60271849949357659 ) ) ;
#30086=DIRECTION ( 'NONE',  ( 0.000000000000000000, 0.000000000000000000, 1.000000000000000000 ) ) ;
#30088=EDGE_CURVE ( 'NONE', #15352, #30905, #29923, .T. ) ;
#30090=ORIENTED_EDGE ( 'NONE', *, *, #926, .F. ) ;
#30098=DIRECTION ( 'NONE',  ( -1.000000000000000000, -0.000000000000000000, -0.000000000000000000 ) ) ;
#30101=CARTESIAN_POINT ( 'NONE',  ( 18.00000000000000355, -44.61570720899106846, 14.73072383765551940 ) ) ;
#30107=CARTESIAN_POINT ( 'NONE',  ( 0.000000000000000000, 12.30077720129096264, 50.52416135122086871 ) ) ;
#30116=AXIS2_PLACEMENT_3D ( 'NONE', #22928, #19637, #26163 ) ;
#30122=DIRECTION ( 'NONE',  ( -1.000000000000000000, -0.000000000000000000, 0.000000000000000000 ) ) ;
#30130=CARTESIAN_POINT ( 'NONE',  ( 18.00000000000000355, -49.65209126885773827, 15.44894276735532657 ) ) ;
#30132=EDGE_CURVE ( 'NONE', #40692, #5278, #7537, .T. ) ;
#30152=DIRECTION ( 'NONE',  ( -1.000000000000000000, 0.000000000000000000, 0.000000000000000000 ) ) ;
#30157=ORIENTED_EDGE ( 'NONE', *, *, #10535, .T. ) ;
#30161=DIRECTION ( 'NONE',  ( 0.000000000000000000, 0.000000000000000000, 1.000000000000000000 ) ) ;
#30162=EDGE_LOOP ( 'NONE', ( #22856, #974, #3540, #18241 ) ) ;
#30171=VERTEX_POINT ( 'NONE', #8874 ) ;
#30176=DIRECTION ( 'NONE',  ( -1.000000000000000000, 0.000000000000000000, -0.000000000000000000 ) ) ;
#30180=CYLINDRICAL_SURFACE ( 'NONE', #15056, 20.00000000000000711 ) ;
#30187=ORIENTED_EDGE ( 'NONE', *, *, #34982, .T. ) ;
#30191=EDGE_CURVE ( 'NONE', #2577, #6385, #470, .T. ) ;
#30212=DIRECTION ( 'NONE',  ( 0.000000000000000000, -0.3681245526846853022, 0.9297764858882484607 ) ) ;
#30215=DIRECTION ( 'NONE',  ( -1.000000000000000000, 0.000000000000000000, -0.000000000000000000 ) ) ;
#30217=EDGE_CURVE ( 'NONE', #28134, #33321, #27080, .T. ) ;
#30218=DIRECTION ( 'NONE',  ( 0.000000000000000000, 0.000000000000000000, 1.000000000000000000 ) ) ;
#30220=CIRCLE ( 'NONE', #16277, 47.49900000000000233 ) ;
#30227=DIRECTION ( 'NONE',  ( 0.000000000000000000, 0.000000000000000000, 1.000000000000000000 ) ) ;
#30231=EDGE_CURVE ( 'NONE', #16711, #5593, #17937, .T. ) ;
#30235=CARTESIAN_POINT ( 'NONE',  ( 18.00000000000000355, 0.000000000000000000, 0.000000000000000000 ) ) ;
#30240=ADVANCED_FACE ( 'NONE', ( #1066 ), #35263, .T. ) ;
#30248=LINE ( 'NONE', #34367, #34700 ) ;
#30257=CYLINDRICAL_SURFACE ( 'NONE', #28985, 51.99999999999999289 ) ;
#30262=AXIS2_PLACEMENT_3D ( 'NONE', #17741, #27979, #41454 ) ;
#30277=CARTESIAN_POINT ( 'NONE',  ( 18.00000000000000355, -30.93515269692088765, -36.04401931830283701 ) ) ;
#30286=EDGE_CURVE ( 'NONE', #7115, #4217, #25486, .T. ) ;
#30290=ORIENTED_EDGE ( 'NONE', *, *, #8473, .F. ) ;
#30293=ORIENTED_EDGE ( 'NONE', *, *, #4431, .T. ) ;
#30309=CIRCLE ( 'NONE', #24069, 47.49900000000000233 ) ;
#30319=CIRCLE ( 'NONE', #41443, 47.49899999999999523 ) ;
#30337=CARTESIAN_POINT ( 'NONE',  ( 0.000000000000000000, 27.43636312076376527, -38.14186064215121519 ) ) ;
#30339=CIRCLE ( 'NONE', #20583, 52.00000000000000000 ) ;
#30340=ORIENTED_EDGE ( 'NONE', *, *, #13562, .T. ) ;
#30348=ORIENTED_EDGE ( 'NONE', *, *, #13074, .T. ) ;
#30352=DIRECTION ( 'NONE',  ( -1.000000000000000000, -0.000000000000000000, -0.000000000000000000 ) ) ;
#30353=EDGE_CURVE ( 'NONE', #37184, #12223, #29073, .T. ) ;
#30355=CARTESIAN_POINT ( 'NONE',  ( 9.000000000000001776, -19.74581912682874929, 48.10512059033386834 ) ) ;
#30356=EDGE_LOOP ( 'NONE', ( #34999, #3374, #14655, #14095 ) ) ;
#30358=CARTESIAN_POINT ( 'NONE',  ( 0.000000000000000000, 24.72041153920788403, -40.55929306992662475 ) ) ;
#30362=CIRCLE ( 'NONE', #42199, 20.00000000000000711 ) ;
#30372=LINE ( 'NONE', #29733, #23115 ) ;
#30373=ORIENTED_EDGE ( 'NONE', *, *, #17576, .T. ) ;
#30374=CIRCLE ( 'NONE', #8065, 20.00000000000000355 ) ;
#30384=DIRECTION ( 'NONE',  ( -1.000000000000000000, -0.000000000000000000, 0.000000000000000000 ) ) ;
#30393=EDGE_CURVE ( 'NONE', #9420, #29484, #19343, .T. ) ;
#30401=ORIENTED_EDGE ( 'NONE', *, *, #29266, .T. ) ;
#30404=VECTOR ( 'NONE', #26776, 1000.000000000000000 ) ;
#30410=ORIENTED_EDGE ( 'NONE', *, *, #39039, .T. ) ;
#30417=EDGE_LOOP ( 'NONE', ( #39813, #12468, #14812, #21643 ) ) ;
#30420=LINE ( 'NONE', #494, #37433 ) ;
#30421=CARTESIAN_POINT ( 'NONE',  ( 0.000000000000000000, 43.55304910509446614, -28.41006711799937889 ) ) ;
#30426=CARTESIAN_POINT ( 'NONE',  ( 18.00000000000000355, 42.60732521687572927, 19.80331771201673519 ) ) ;
#30429=CIRCLE ( 'NONE', #22755, 47.49900000000000233 ) ;
#30434=CARTESIAN_POINT ( 'NONE',  ( 18.00000000000000355, 0.000000000000000000, 0.000000000000000000 ) ) ;
#30436=VERTEX_POINT ( 'NONE', #19577 ) ;
#30438=CYLINDRICAL_SURFACE ( 'NONE', #13004, 20.00000000000000355 ) ;
#30440=AXIS2_PLACEMENT_3D ( 'NONE', #37665, #16991, #10190 ) ;
#30445=ORIENTED_EDGE ( 'NONE', *, *, #26346, .F. ) ;
#30448=EDGE_CURVE ( 'NONE', #34314, #6747, #42443, .T. ) ;
#30452=ORIENTED_EDGE ( 'NONE', *, *, #26095, .F. ) ;
#30453=ORIENTED_EDGE ( 'NONE', *, *, #8055, .F. ) ;
#30455=CARTESIAN_POINT ( 'NONE',  ( 18.00000000000000355, 0.000000000000000000, 0.000000000000000000 ) ) ;
#30456=DIRECTION ( 'NONE',  ( -1.000000000000000000, 0.000000000000000000, 0.000000000000000000 ) ) ;
#30457=DIRECTION ( 'NONE',  ( -1.000000000000000000, -0.000000000000000000, -0.000000000000000000 ) ) ;
#30458=EDGE_LOOP ( 'NONE', ( #1554, #34523, #39854, #9851 ) ) ;
#30467=CARTESIAN_POINT ( 'NONE',  ( 18.00000000000000355, 11.90021268425617329, -45.45261810511203038 ) ) ;
#30487=DIRECTION ( 'NONE',  ( 0.000000000000000000, 0.000000000000000000, 1.000000000000000000 ) ) ;
#30488=ORIENTED_EDGE ( 'NONE', *, *, #32697, .F. ) ;
#30490=ORIENTED_EDGE ( 'NONE', *, *, #3562, .F. ) ;
#30492=FACE_OUTER_BOUND ( 'NONE', #42371, .T. ) ;
#30493=AXIS2_PLACEMENT_3D ( 'NONE', #22637, #12584, #12377 ) ;
#30496=CARTESIAN_POINT ( 'NONE',  ( 18.00000000000000355, 32.00046193115148441, 34.40241257139697950 ) ) ;
#30499=AXIS2_PLACEMENT_3D ( 'NONE', #31629, #25335, #24920 ) ;
#30501=FACE_OUTER_BOUND ( 'NONE', #37717, .T. ) ;
#30504=CARTESIAN_POINT ( 'NONE',  ( 9.000000000000001776, 31.08872492059957793, 41.68322423723110148 ) ) ;
#30506=EDGE_CURVE ( 'NONE', #18955, #41139, #11668, .T. ) ;
#30511=DIRECTION ( 'NONE',  ( -1.000000000000000000, 0.000000000000000000, 0.000000000000000000 ) ) ;
#30517=ORIENTED_EDGE ( 'NONE', *, *, #29461, .F. ) ;
#30522=CARTESIAN_POINT ( 'NONE',  ( 18.00000000000000355, -15.49408907645141653, -44.90087086784608061 ) ) ;
#30524=ORIENTED_EDGE ( 'NONE', *, *, #19041, .F. ) ;
#30536=VERTEX_POINT ( 'NONE', #17392 ) ;
#30539=DIRECTION ( 'NONE',  ( 0.000000000000000000, 0.000000000000000000, 1.000000000000000000 ) ) ;
#30547=ORIENTED_EDGE ( 'NONE', *, *, #31955, .F. ) ;
#30557=VECTOR ( 'NONE', #32901, 1000.000000000000000 ) ;
#30559=EDGE_CURVE ( 'NONE', #42037, #24522, #36731, .T. ) ;
#30560=DIRECTION ( 'NONE',  ( -1.000000000000000000, -0.000000000000000000, 0.000000000000000000 ) ) ;
#30578=CARTESIAN_POINT ( 'NONE',  ( 0.000000000000000000, 0.2227391519116599106, 46.98410307550730636 ) ) ;
#30585=VERTEX_POINT ( 'NONE', #742 ) ;
#30597=DIRECTION ( 'NONE',  ( -1.000000000000000000, 0.000000000000000000, 0.000000000000000000 ) ) ;
#30600=CYLINDRICAL_SURFACE ( 'NONE', #8056, 51.99999999999999289 ) ;
#30622=AXIS2_PLACEMENT_3D ( 'NONE', #31675, #14473, #24080 ) ;
#30637=VERTEX_POINT ( 'NONE', #2043 ) ;
#30641=LINE ( 'NONE', #10344, #32468 ) ;
#30645=VECTOR ( 'NONE', #20035, 1000.000000000000000 ) ;
#30650=DIRECTION ( 'NONE',  ( -1.000000000000000000, -0.000000000000000000, -0.000000000000000000 ) ) ;
#30652=DIRECTION ( 'NONE',  ( -1.000000000000000000, -0.000000000000000000, 0.000000000000000000 ) ) ;
#30654=VERTEX_POINT ( 'NONE', #32162 ) ;
#30657=CARTESIAN_POINT ( 'NONE',  ( 0.000000000000000000, 39.64889472655779201, -33.64468972902464117 ) ) ;
#30662=CARTESIAN_POINT ( 'NONE',  ( 0.000000000000000000, 46.19362259308845609, -8.585149169757988474 ) ) ;
#30678=ADVANCED_FACE ( 'NONE', ( #18053, #34570 ), #1399, .F. ) ;
#30683=CARTESIAN_POINT ( 'NONE',  ( 18.00000000000000355, -46.87740477351720614, 3.172455868805039270 ) ) ;
#30693=EDGE_CURVE ( 'NONE', #15576, #9420, #8198, .T. ) ;
#30704=CIRCLE ( 'NONE', #2117, 51.99999999999999289 ) ;
#30705=DIRECTION ( 'NONE',  ( -1.000000000000000000, -0.000000000000000000, 0.000000000000000000 ) ) ;
#30709=DIRECTION ( 'NONE',  ( -1.000000000000000000, -0.000000000000000000, -0.000000000000000000 ) ) ;
#30714=CARTESIAN_POINT ( 'NONE',  ( 18.00000000000000355, 0.000000000000000000, 0.000000000000000000 ) ) ;
#30718=ORIENTED_EDGE ( 'NONE', *, *, #28300, .F. ) ;
#30729=ORIENTED_EDGE ( 'NONE', *, *, #9591, .T. ) ;
#30730=DIRECTION ( 'NONE',  ( 0.000000000000000000, 0.5877852522924742473, -0.8090169943749465631 ) ) ;
#30736=AXIS2_PLACEMENT_3D ( 'NONE', #12216, #36165, #6279 ) ;
#30743=CIRCLE ( 'NONE', #41174, 20.00000000000000711 ) ;
#30749=CARTESIAN_POINT ( 'NONE',  ( 18.00000000000000355, -25.61928775981012762, -45.25098998563503727 ) ) ;
#30768=ORIENTED_EDGE ( 'NONE', *, *, #13677, .F. ) ;
#30773=ORIENTED_EDGE ( 'NONE', *, *, #38772, .F. ) ;
#30776=ORIENTED_EDGE ( 'NONE', *, *, #6214, .T. ) ;
#30785=CARTESIAN_POINT ( 'NONE',  ( 18.00000000000001421, 0.000000000000000000, 0.000000000000000000 ) ) ;
#30786=ORIENTED_EDGE ( 'NONE', *, *, #38400, .F. ) ;
#30797=LINE ( 'NONE', #1095, #32969 ) ;
#30801=FACE_OUTER_BOUND ( 'NONE', #29137, .T. ) ;
#30811=EDGE_CURVE ( 'NONE', #34548, #27883, #19740, .T. ) ;
#30812=DIRECTION ( 'NONE',  ( -1.000000000000000000, -0.000000000000000000, 0.000000000000000000 ) ) ;
#30814=AXIS2_PLACEMENT_3D ( 'NONE', #39029, #25563, #22717 ) ;
#30820=LINE ( 'NONE', #3954, #33975 ) ;
#30825=CARTESIAN_POINT ( 'NONE',  ( 18.00000000000000355, -35.11945359308083425, -38.34871548466050939 ) ) ;
#30834=ORIENTED_EDGE ( 'NONE', *, *, #1644, .T. ) ;
#30839=DIRECTION ( 'NONE',  ( 0.000000000000000000, -0.8443279255020201823, 0.5358267949789886631 ) ) ;
#30847=CYLINDRICAL_SURFACE ( 'NONE', #22904, 20.00000000000000355 ) ;
#30854=LINE ( 'NONE', #28471, #14220 ) ;
#30858=ORIENTED_EDGE ( 'NONE', *, *, #12608, .F. ) ;
#30865=ADVANCED_FACE ( 'NONE', ( #22384 ), #5959, .T. ) ;
#30866=CARTESIAN_POINT ( 'NONE',  ( 18.00000000000000355, 0.000000000000000000, 0.000000000000000000 ) ) ;
#30871=DIRECTION ( 'NONE',  ( -1.000000000000000000, -0.000000000000000000, -0.000000000000000000 ) ) ;
#30872=CARTESIAN_POINT ( 'NONE',  ( 18.00000000000000355, -26.17370628620627571, -39.63700417846190049 ) ) ;
#30879=CARTESIAN_POINT ( 'NONE',  ( 18.00000000000000355, 0.000000000000000000, 0.000000000000000000 ) ) ;
#30887=VERTEX_POINT ( 'NONE', #38915 ) ;
#30891=DIRECTION ( 'NONE',  ( 0.000000000000000000, 0.000000000000000000, 1.000000000000000000 ) ) ;
#30894=ORIENTED_EDGE ( 'NONE', *, *, #31113, .T. ) ;
#30905=VERTEX_POINT ( 'NONE', #32796 ) ;
#30919=DIRECTION ( 'NONE',  ( -1.000000000000000000, -0.000000000000000000, 0.000000000000000000 ) ) ;
#30923=CARTESIAN_POINT ( 'NONE',  ( 18.00000000000000355, 36.05989434073656952, -30.12041790338580682 ) ) ;
#30924=ORIENTED_EDGE ( 'NONE', *, *, #9501, .F. ) ;
#30929=ORIENTED_EDGE ( 'NONE', *, *, #21356, .T. ) ;
#30934=ORIENTED_EDGE ( 'NONE', *, *, #7647, .F. ) ;
#30937=ORIENTED_EDGE ( 'NONE', *, *, #38202, .T. ) ;
#30943=EDGE_CURVE ( 'NONE', #19993, #39452, #15619, .T. ) ;
#30950=VECTOR ( 'NONE', #1752, 1000.000000000000000 ) ;
#30968=CARTESIAN_POINT ( 'NONE',  ( 0.000000000000000000, 0.000000000000000000, 0.000000000000000000 ) ) ;
#30973=DIRECTION ( 'NONE',  ( -1.000000000000000000, -0.000000000000000000, 0.000000000000000000 ) ) ;
#30984=ORIENTED_EDGE ( 'NONE', *, *, #34721, .T. ) ;
#30987=AXIS2_PLACEMENT_3D ( 'NONE', #18323, #38330, #28557 ) ;
#30993=ORIENTED_EDGE ( 'NONE', *, *, #3159, .F. ) ;
#30997=ORIENTED_EDGE ( 'NONE', *, *, #35530, .F. ) ;
#31001=CARTESIAN_POINT ( 'NONE',  ( 18.00000000000000355, 11.90021268425617329, -45.45261810511203038 ) ) ;
#31006=AXIS2_PLACEMENT_3D ( 'NONE', #39140, #6625, #16712 ) ;
#31007=CARTESIAN_POINT ( 'NONE',  ( 18.00000000000000355, -42.41764978026621691, 20.20639853260276197 ) ) ;
#31012=CARTESIAN_POINT ( 'NONE',  ( 0.000000000000000000, 34.03046037009303149, -33.13733193845768454 ) ) ;
#31026=DIRECTION ( 'NONE',  ( -1.000000000000000000, -0.000000000000000000, -0.000000000000000000 ) ) ;
#31027=EDGE_CURVE ( 'NONE', #40171, #6447, #42723, .T. ) ;
#31032=DIRECTION ( 'NONE',  ( -1.000000000000000000, -0.000000000000000000, 0.000000000000000000 ) ) ;
#31040=ORIENTED_EDGE ( 'NONE', *, *, #5686, .F. ) ;
#31046=FACE_OUTER_BOUND ( 'NONE', #2677, .T. ) ;
#31050=EDGE_LOOP ( 'NONE', ( #14623, #23569, #7559, #33415 ) ) ;
#31053=ORIENTED_EDGE ( 'NONE', *, *, #18992, .F. ) ;
#31070=VERTEX_POINT ( 'NONE', #7245 ) ;
#31077=CIRCLE ( 'NONE', #7362, 47.49900000000000233 ) ;
#31078=CARTESIAN_POINT ( 'NONE',  ( 0.000000000000000000, 34.03046037009255542, 33.13733193845817482 ) ) ;
#31080=AXIS2_PLACEMENT_3D ( 'NONE', #25291, #21812, #35057 ) ;
#31085=CARTESIAN_POINT ( 'NONE',  ( 18.00000000000000355, 47.00885577955421013, -6.806061952191806874 ) ) ;
#31095=ORIENTED_EDGE ( 'NONE', *, *, #7212, .T. ) ;
#31103=DIRECTION ( 'NONE',  ( -1.000000000000000000, -0.000000000000000000, 0.000000000000000000 ) ) ;
#31105=CYLINDRICAL_SURFACE ( 'NONE', #39359, 20.00000000000000355 ) ;
#31113=EDGE_CURVE ( 'NONE', #34568, #14255, #14914, .T. ) ;
#31119=AXIS2_PLACEMENT_3D ( 'NONE', #13437, #23697, #7070 ) ;
#31147=AXIS2_PLACEMENT_3D ( 'NONE', #40712, #33540, #9976 ) ;
#31148=CARTESIAN_POINT ( 'NONE',  ( -10.00000000000000000, 0.000000000000000000, 0.000000000000000000 ) ) ;
#31153=VECTOR ( 'NONE', #31511, 1000.000000000000000 ) ;
#31157=VECTOR ( 'NONE', #7627, 1000.000000000000000 ) ;
#31159=CYLINDRICAL_SURFACE ( 'NONE', #34571, 47.49900000000000233 ) ;
#31169=VECTOR ( 'NONE', #20405, 1000.000000000000000 ) ;
#31171=LINE ( 'NONE', #37482, #9382 ) ;
#31184=ORIENTED_EDGE ( 'NONE', *, *, #8055, .T. ) ;
#31191=ORIENTED_EDGE ( 'NONE', *, *, #7534, .F. ) ;
#31200=ADVANCED_FACE ( 'NONE', ( #17717 ), #7635, .T. ) ;
#31214=CARTESIAN_POINT ( 'NONE',  ( 18.00000000000000355, -30.93515269692088765, -36.04401931830283701 ) ) ;
#31217=AXIS2_PLACEMENT_3D ( 'NONE', #37945, #8068, #34685 ) ;
#31229=DIRECTION ( 'NONE',  ( -1.000000000000000000, 0.000000000000000000, -0.000000000000000000 ) ) ;
#31235=EDGE_CURVE ( 'NONE', #34436, #40375, #10012, .T. ) ;
#31237=LINE ( 'NONE', #1324, #14954 ) ;
#31239=ORIENTED_EDGE ( 'NONE', *, *, #712, .F. ) ;
#31241=DIRECTION ( 'NONE',  ( 0.000000000000000000, -0.9980267284282708928, -0.06279051952932436509 ) ) ;
#31260=CARTESIAN_POINT ( 'NONE',  ( 18.00000000000000355, 0.000000000000000000, 0.000000000000000000 ) ) ;
#31264=EDGE_LOOP ( 'NONE', ( #40665, #14249, #13869, #25047 ) ) ;
#31266=VERTEX_POINT ( 'NONE', #14208 ) ;
#31273=VECTOR ( 'NONE', #33111, 1000.000000000000000 ) ;
#31279=CARTESIAN_POINT ( 'NONE',  ( 0.000000000000000000, 36.05989434073613609, 30.12041790338630776 ) ) ;
#31284=DIRECTION ( 'NONE',  ( 1.000000000000000000, 0.000000000000000000, 0.000000000000000000 ) ) ;
#31297=ORIENTED_EDGE ( 'NONE', *, *, #36826, .T. ) ;
#31299=FACE_OUTER_BOUND ( 'NONE', #30356, .T. ) ;
#31302=FACE_OUTER_BOUND ( 'NONE', #2575, .T. ) ;
#31316=ORIENTED_EDGE ( 'NONE', *, *, #27541, .F. ) ;
#31326=CARTESIAN_POINT ( 'NONE',  ( 18.00000000000000355, 0.000000000000000000, 0.000000000000000000 ) ) ;
#31345=ORIENTED_EDGE ( 'NONE', *, *, #24149, .F. ) ;
#31372=EDGE_CURVE ( 'NONE', #36216, #8904, #15511, .T. ) ;
#31376=EDGE_CURVE ( 'NONE', #8384, #2260, #28880, .T. ) ;
#31377=CARTESIAN_POINT ( 'NONE',  ( 0.000000000000000000, 47.49120266317495265, -0.8606222198177008176 ) ) ;
#31387=EDGE_LOOP ( 'NONE', ( #37455, #9912, #28000, #15718 ) ) ;
#31390=DIRECTION ( 'NONE',  ( -1.000000000000000000, 0.000000000000000000, 0.000000000000000000 ) ) ;
#31391=LINE ( 'NONE', #35291, #18553 ) ;
#31395=VERTEX_POINT ( 'NONE', #22286 ) ;
#31396=CARTESIAN_POINT ( 'NONE',  ( 0.000000000000000000, 0.000000000000000000, 0.000000000000000000 ) ) ;
#31408=CIRCLE ( 'NONE', #9778, 47.49900000000000944 ) ;
#31410=DIRECTION ( 'NONE',  ( 0.000000000000000000, 0.000000000000000000, 1.000000000000000000 ) ) ;
#31413=EDGE_CURVE ( 'NONE', #7587, #24871, #42078, .T. ) ;
#31415=VERTEX_POINT ( 'NONE', #36385 ) ;
#31421=CARTESIAN_POINT ( 'NONE',  ( 18.00000000000000355, 44.75336757549799671, -14.30704879393557150 ) ) ;
#31429=VERTEX_POINT ( 'NONE', #32908 ) ;
#31432=DIRECTION ( 'NONE',  ( 0.000000000000000000, -0.4817536741017223179, 0.8763066800438598092 ) ) ;
#31437=FACE_OUTER_BOUND ( 'NONE', #13200, .T. ) ;
#31446=DIRECTION ( 'NONE',  ( -1.000000000000000000, -0.000000000000000000, -0.000000000000000000 ) ) ;
#31453=CARTESIAN_POINT ( 'NONE',  ( 0.000000000000000000, 36.05989434073656952, -30.12041790338580682 ) ) ;
#31460=CARTESIAN_POINT ( 'NONE',  ( 18.00000000000000355, 13.56094713063571078, 50.20060470671745634 ) ) ;
#31467=AXIS2_PLACEMENT_3D ( 'NONE', #32729, #39476, #32519 ) ;
#31470=VERTEX_POINT ( 'NONE', #16350 ) ;
#31474=DIRECTION ( 'NONE',  ( 0.000000000000000000, 0.5877852522924685852, 0.8090169943749507819 ) ) ;
#31487=AXIS2_PLACEMENT_3D ( 'NONE', #36214, #6335, #19680 ) ;
#31502=DIRECTION ( 'NONE',  ( 0.000000000000000000, 0.000000000000000000, 1.000000000000000000 ) ) ;
#31511=DIRECTION ( 'NONE',  ( 1.000000000000000000, 0.000000000000000000, -0.000000000000000000 ) ) ;
#31512=DIRECTION ( 'NONE',  ( 0.000000000000000000, 0.000000000000000000, 1.000000000000000000 ) ) ;
#31522=EDGE_CURVE ( 'NONE', #13721, #1418, #43149, .T. ) ;
#31523=CARTESIAN_POINT ( 'NONE',  ( 9.000000000000001776, 12.30077720129095198, 50.52416135122086160 ) ) ;
#31531=DIRECTION ( 'NONE',  ( 0.000000000000000000, -0.8443279255020087470, -0.5358267949790065376 ) ) ;
#31541=AXIS2_PLACEMENT_3D ( 'NONE', #6060, #32250, #2328 ) ;
#31552=DIRECTION ( 'NONE',  ( 0.000000000000000000, 0.000000000000000000, 1.000000000000000000 ) ) ;
#31555=ORIENTED_EDGE ( 'NONE', *, *, #22433, .F. ) ;
#31557=CARTESIAN_POINT ( 'NONE',  ( 18.00000000000000355, 17.50309955389612426, 43.60271849949370448 ) ) ;
#31562=CIRCLE ( 'NONE', #17647, 20.00000000000000711 ) ;
#31573=DIRECTION ( 'NONE',  ( 0.000000000000000000, 0.000000000000000000, -1.000000000000000000 ) ) ;
#31574=ADVANCED_FACE ( 'NONE', ( #13734 ), #14372, .T. ) ;
#31576=CARTESIAN_POINT ( 'NONE',  ( 18.00000000000000355, 0.000000000000000000, 0.000000000000000000 ) ) ;
#31578=VERTEX_POINT ( 'NONE', #37476 ) ;
#31586=EDGE_LOOP ( 'NONE', ( #14287, #34744, #22760, #28894 ) ) ;
#31595=AXIS2_PLACEMENT_3D ( 'NONE', #3393, #106, #13474 ) ;
#31596=ADVANCED_FACE ( 'NONE', ( #10439 ), #7803, .T. ) ;
#31609=EDGE_CURVE ( 'NONE', #1751, #35293, #14945, .T. ) ;
#31610=VERTEX_POINT ( 'NONE', #17240 ) ;
#31627=CYLINDRICAL_SURFACE ( 'NONE', #12037, 47.49900000000000233 ) ;
#31629=CARTESIAN_POINT ( 'NONE',  ( 18.00000000000000355, 46.90537658765331486, 2.727856614654470491 ) ) ;
#31632=ORIENTED_EDGE ( 'NONE', *, *, #35960, .F. ) ;
#31634=AXIS2_PLACEMENT_3D ( 'NONE', #2481, #22619, #16057 ) ;
#31639=FACE_OUTER_BOUND ( 'NONE', #13088, .T. ) ;
#31641=VERTEX_POINT ( 'NONE', #7146 ) ;
#31654=CYLINDRICAL_SURFACE ( 'NONE', #41373, 51.99999999999999289 ) ;
#31662=PRODUCT_DEFINITION_FORMATION_WITH_SPECIFIED_SOURCE ( 'ANY', '', #19330, .NOT_KNOWN. ) ;
#31667=CARTESIAN_POINT ( 'NONE',  ( 18.00000000000000355, 42.03146605346817921, -22.12489237027272893 ) ) ;
#31671=EDGE_CURVE ( 'NONE', #10423, #2044, #7591, .T. ) ;
#31675=CARTESIAN_POINT ( 'NONE',  ( -10.00000000000000000, 0.000000000000000000, 0.000000000000000000 ) ) ;
#31676=DIRECTION ( 'NONE',  ( 0.000000000000000000, -0.9980267284282722251, 0.06279051952930256308 ) ) ;
#31679=ADVANCED_FACE ( 'NONE', ( #13948 ), #11103, .T. ) ;
#31680=CARTESIAN_POINT ( 'NONE',  ( 18.00000000000000355, 0.000000000000000000, 0.000000000000000000 ) ) ;
#31681=DIRECTION ( 'NONE',  ( -1.000000000000000000, 0.000000000000000000, -0.000000000000000000 ) ) ;
#31682=ORIENTED_EDGE ( 'NONE', *, *, #24608, .F. ) ;
#31689=ORIENTED_EDGE ( 'NONE', *, *, #15425, .F. ) ;
#31690=CYLINDRICAL_SURFACE ( 'NONE', #9134, 20.00000000000000711 ) ;
#31692=AXIS2_PLACEMENT_3D ( 'NONE', #27945, #22055, #17932 ) ;
#31695=VECTOR ( 'NONE', #23253, 1000.000000000000000 ) ;
#31696=CARTESIAN_POINT ( 'NONE',  ( 0.000000000000000000, 15.49408907645234201, -44.90087086784576087 ) ) ;
#31709=VERTEX_POINT ( 'NONE', #1021 ) ;
#31713=CARTESIAN_POINT ( 'NONE',  ( 0.000000000000000000, -30.93515269692137792, 36.04401931830242489 ) ) ;
#31718=ORIENTED_EDGE ( 'NONE', *, *, #34899, .F. ) ;
#31719=EDGE_CURVE ( 'NONE', #10605, #23617, #28913, .T. ) ;
#31735=CARTESIAN_POINT ( 'NONE',  ( 0.000000000000000000, -26.17370628620681927, 39.63700417846155233 ) ) ;
#31754=CARTESIAN_POINT ( 'NONE',  ( 0.000000000000000000, 46.77034588191335018, -22.72740077717179474 ) ) ;
#31755=AXIS2_PLACEMENT_3D ( 'NONE', #25430, #12326, #38269 ) ;
#31763=ORIENTED_EDGE ( 'NONE', *, *, #16812, .T. ) ;
#31764=SHAPE_REPRESENTATION_RELATIONSHIP ( 'NONE' , 'NONE' ,  #13509, #1547 ) ;
#31765=FACE_OUTER_BOUND ( 'NONE', #22264, .T. ) ;
#31776=CIRCLE ( 'NONE', #4593, 20.00000000000000355 ) ;
#31777=EDGE_CURVE ( 'NONE', #37135, #12470, #36530, .T. ) ;
#31785=AXIS2_PLACEMENT_3D ( 'NONE', #26100, #32838, #13014 ) ;
#31787=AXIS2_PLACEMENT_3D ( 'NONE', #13086, #38423, #39651 ) ;
#31799=CARTESIAN_POINT ( 'NONE',  ( 18.00000000000000355, -6.109652351742118626, 46.58570277113506819 ) ) ;
#31802=DIRECTION ( 'NONE',  ( 0.000000000000000000, 0.000000000000000000, 1.000000000000000000 ) ) ;
#31803=CARTESIAN_POINT ( 'NONE',  ( 0.000000000000000000, 46.21320724403663860, -10.97699764141904843 ) ) ;
#31810=CARTESIAN_POINT ( 'NONE',  ( 0.000000000000000000, 0.000000000000000000, 0.000000000000000000 ) ) ;
#31814=CIRCLE ( 'NONE', #38787, 20.00000000000001066 ) ;
#31824=DIRECTION ( 'NONE',  ( 0.000000000000000000, 0.3681245526846719240, 0.9297764858882537897 ) ) ;
#31833=ADVANCED_FACE ( 'NONE', ( #38757 ), #4750, .T. ) ;
#31853=ADVANCED_FACE ( 'NONE', ( #8452 ), #1897, .T. ) ;
#31854=ORIENTED_EDGE ( 'NONE', *, *, #5110, .F. ) ;
#31856=CARTESIAN_POINT ( 'NONE',  ( 18.00000000000000355, -46.21320724403656044, 10.97699764141937173 ) ) ;
#31866=CARTESIAN_POINT ( 'NONE',  ( 18.00000000000000355, 46.11014828289831513, 9.022736828081521665 ) ) ;
#31882=VERTEX_POINT ( 'NONE', #41610 ) ;
#31886=EDGE_CURVE ( 'NONE', #19539, #29967, #26110, .T. ) ;
#31887=ORIENTED_EDGE ( 'NONE', *, *, #4431, .F. ) ;
#31900=DIRECTION ( 'NONE',  ( -1.000000000000000000, 0.000000000000000000, -0.000000000000000000 ) ) ;
#31904=VERTEX_POINT ( 'NONE', #31377 ) ;
#31906=LINE ( 'NONE', #28639, #41688 ) ;
#31907=EDGE_CURVE ( 'NONE', #21438, #40692, #21603, .T. ) ;
#31914=DIRECTION ( 'NONE',  ( -1.000000000000000000, 0.000000000000000000, 0.000000000000000000 ) ) ;
#31917=CARTESIAN_POINT ( 'NONE',  ( 18.00000000000000355, 0.000000000000000000, 0.000000000000000000 ) ) ;
#31919=VERTEX_POINT ( 'NONE', #16301 ) ;
#31925=CARTESIAN_POINT ( 'NONE',  ( 18.00000000000000355, -40.47821179127736713, 32.64221760512744908 ) ) ;
#31943=ORIENTED_EDGE ( 'NONE', *, *, #5779, .F. ) ;
#31954=DIRECTION ( 'NONE',  ( -1.000000000000000000, -0.000000000000000000, -0.000000000000000000 ) ) ;
#31955=EDGE_CURVE ( 'NONE', #3154, #11369, #25442, .T. ) ;
#31957=VECTOR ( 'NONE', #13503, 1000.000000000000000 ) ;
#31966=EDGE_CURVE ( 'NONE', #3869, #37135, #7992, .T. ) ;
#31968=ORIENTED_EDGE ( 'NONE', *, *, #24054, .F. ) ;
#31972=ORIENTED_EDGE ( 'NONE', *, *, #6434, .F. ) ;
#31974=FACE_OUTER_BOUND ( 'NONE', #545, .T. ) ;
#31992=DIRECTION ( 'NONE',  ( 0.000000000000000000, 0.3681245526846785854, -0.9297764858882511252 ) ) ;
#31996=CYLINDRICAL_SURFACE ( 'NONE', #37625, 20.00000000000000711 ) ;
#31998=DIRECTION ( 'NONE',  ( -1.000000000000000000, -0.000000000000000000, -0.000000000000000000 ) ) ;
#31999=ORIENTED_EDGE ( 'NONE', *, *, #13677, .T. ) ;
#32011=DIRECTION ( 'NONE',  ( -1.000000000000000000, 0.000000000000000000, 0.000000000000000000 ) ) ;
#32016=CIRCLE ( 'NONE', #22981, 11.00000000000000000 ) ;
#32031=VERTEX_POINT ( 'NONE', #15886 ) ;
#32041=CIRCLE ( 'NONE', #41805, 51.99999999999999289 ) ;
#32042=ORIENTED_EDGE ( 'NONE', *, *, #39207, .T. ) ;
#32048=DIRECTION ( 'NONE',  ( 0.000000000000000000, 0.000000000000000000, 1.000000000000000000 ) ) ;
#32062=LINE ( 'NONE', #8497, #16602 ) ;
#32063=ORIENTED_EDGE ( 'NONE', *, *, #20409, .T. ) ;
#32071=CYLINDRICAL_SURFACE ( 'NONE', #20725, 47.49900000000000233 ) ;
#32075=CIRCLE ( 'NONE', #31692, 20.00000000000000355 ) ;
#32076=DIRECTION ( 'NONE',  ( 0.000000000000000000, 0.3681245526846786964, -0.9297764858882511252 ) ) ;
#32080=DIRECTION ( 'NONE',  ( -1.000000000000000000, 0.000000000000000000, -0.000000000000000000 ) ) ;
#32081=ORIENTED_EDGE ( 'NONE', *, *, #29985, .F. ) ;
#32106=ORIENTED_EDGE ( 'NONE', *, *, #19041, .T. ) ;
#32132=EDGE_LOOP ( 'NONE', ( #33536, #9467, #40603, #29958 ) ) ;
#32133=DIRECTION ( 'NONE',  ( 1.000000000000000000, 0.000000000000000000, 0.000000000000000000 ) ) ;
#32139=DIRECTION ( 'NONE',  ( -1.000000000000000000, -0.000000000000000000, 0.000000000000000000 ) ) ;
#32151=ORIENTED_EDGE ( 'NONE', *, *, #28284, .F. ) ;
#32161=ORIENTED_EDGE ( 'NONE', *, *, #3057, .F. ) ;
#32162=CARTESIAN_POINT ( 'NONE',  ( 0.000000000000000000, -19.74581912682808493, -48.10512059033413834 ) ) ;
#32166=CARTESIAN_POINT ( 'NONE',  ( 18.00000000000000355, -15.49408907645202937, 44.90087086784588166 ) ) ;
#32176=DIRECTION ( 'NONE',  ( 0.000000000000000000, 0.9510565162951521989, 0.3090169943749515036 ) ) ;
#32178=DIRECTION ( 'NONE',  ( -1.000000000000000000, -0.000000000000000000, 0.000000000000000000 ) ) ;
#32179=EDGE_LOOP ( 'NONE', ( #14151, #2834, #35636, #36183 ) ) ;
#32185=AXIS2_PLACEMENT_3D ( 'NONE', #18119, #29394, #39388 ) ;
#32186=ADVANCED_FACE ( 'NONE', ( #1574 ), #27802, .T. ) ;
#32192=EDGE_CURVE ( 'NONE', #14078, #10279, #36561, .T. ) ;
#32196=ORIENTED_EDGE ( 'NONE', *, *, #14033, .F. ) ;
#32197=CARTESIAN_POINT ( 'NONE',  ( -10.00000000000000000, 0.000000000000000000, 0.000000000000000000 ) ) ;
#32202=ORIENTED_EDGE ( 'NONE', *, *, #1791, .T. ) ;
#32215=ORIENTED_EDGE ( 'NONE', *, *, #31966, .T. ) ;
#32219=CIRCLE ( 'NONE', #25289, 52.00000000000000000 ) ;
#32226=CIRCLE ( 'NONE', #20421, 47.49900000000000233 ) ;
#32244=AXIS2_PLACEMENT_3D ( 'NONE', #9311, #15898, #42252 ) ;
#32246=CARTESIAN_POINT ( 'NONE',  ( 0.000000000000000000, 11.90021268425617329, -45.45261810511203038 ) ) ;
#32249=ADVANCED_FACE ( 'NONE', ( #12071 ), #42123, .T. ) ;
#32250=DIRECTION ( 'NONE',  ( 1.000000000000000000, 0.000000000000000000, 0.000000000000000000 ) ) ;
#32254=EDGE_CURVE ( 'NONE', #18421, #23373, #2404, .T. ) ;
#32255=CARTESIAN_POINT ( 'NONE',  ( 0.000000000000000000, 0.000000000000000000, 0.000000000000000000 ) ) ;
#32263=DIRECTION ( 'NONE',  ( -1.000000000000000000, 0.000000000000000000, 0.000000000000000000 ) ) ;
#32274=DIRECTION ( 'NONE',  ( -1.000000000000000000, 0.000000000000000000, -0.000000000000000000 ) ) ;
#32275=DIRECTION ( 'NONE',  ( -1.000000000000000000, -0.000000000000000000, 0.000000000000000000 ) ) ;
#32276=VERTEX_POINT ( 'NONE', #39272 ) ;
#32294=AXIS2_PLACEMENT_3D ( 'NONE', #31007, #39569, #24057 ) ;
#32303=DIRECTION ( 'NONE',  ( 1.000000000000000000, 0.000000000000000000, 0.000000000000000000 ) ) ;
#32308=CIRCLE ( 'NONE', #5151, 51.99999999999999289 ) ;
#32311=CARTESIAN_POINT ( 'NONE',  ( 0.000000000000000000, -0.2227391519113303131, -46.98410307550732057 ) ) ;
#32312=ORIENTED_EDGE ( 'NONE', *, *, #38400, .T. ) ;
#32328=CARTESIAN_POINT ( 'NONE',  ( 18.00000000000000355, -36.05989434073592292, -30.12041790338656710 ) ) ;
#32333=FACE_OUTER_BOUND ( 'NONE', #19056, .T. ) ;
#32335=EDGE_CURVE ( 'NONE', #1632, #6408, #40736, .T. ) ;
#32336=VERTEX_POINT ( 'NONE', #6139 ) ;
#32337=VECTOR ( 'NONE', #1753, 1000.000000000000000 ) ;
#32355=EDGE_CURVE ( 'NONE', #28896, #14673, #22129, .T. ) ;
#32370=AXIS2_PLACEMENT_3D ( 'NONE', #33466, #20413, #31502 ) ;
#32379=AXIS2_PLACEMENT_3D ( 'NONE', #33069, #25717, #22882 ) ;
#32395=CARTESIAN_POINT ( 'NONE',  ( 9.000000000000001776, -5.871425383721168956, -51.66745943012288222 ) ) ;
#32397=CYLINDRICAL_SURFACE ( 'NONE', #31634, 20.00000000000001066 ) ;
#32398=DIRECTION ( 'NONE',  ( -1.000000000000000000, -0.000000000000000000, 0.000000000000000000 ) ) ;
#32402=EDGE_CURVE ( 'NONE', #41964, #19993, #32963, .T. ) ;
#32403=ORIENTED_EDGE ( 'NONE', *, *, #9886, .F. ) ;
#32406=CARTESIAN_POINT ( 'NONE',  ( 0.000000000000000000, -5.871425383721900815, 51.66745943012280406 ) ) ;
#32412=VERTEX_POINT ( 'NONE', #42988 ) ;
#32424=DIRECTION ( 'NONE',  ( 0.000000000000000000, -0.7705132427757949154, 0.6374239897486827511 ) ) ;
#32432=DIRECTION ( 'NONE',  ( -1.000000000000000000, -0.000000000000000000, 0.000000000000000000 ) ) ;
#32451=AXIS2_PLACEMENT_3D ( 'NONE', #21735, #34988, #18456 ) ;
#32453=AXIS2_PLACEMENT_3D ( 'NONE', #33772, #5122, #11262 ) ;
#32468=VECTOR ( 'NONE', #23682, 1000.000000000000000 ) ;
#32470=ORIENTED_EDGE ( 'NONE', *, *, #16704, .T. ) ;
#32471=VECTOR ( 'NONE', #27254, 1000.000000000000000 ) ;
#32474=DIRECTION ( 'NONE',  ( -1.000000000000000000, -0.000000000000000000, 0.000000000000000000 ) ) ;
#32475=ORIENTED_EDGE ( 'NONE', *, *, #32623, .F. ) ;
#32487=AXIS2_PLACEMENT_3D ( 'NONE', #24042, #24272, #4350 ) ;
#32488=ORIENTED_EDGE ( 'NONE', *, *, #40509, .T. ) ;
#32491=CARTESIAN_POINT ( 'NONE',  ( 18.00000000000001421, 0.000000000000000000, 0.000000000000000000 ) ) ;
#32493=CARTESIAN_POINT ( 'NONE',  ( 0.000000000000000000, -46.77034588191318676, 22.72740077717213936 ) ) ;
#32495=ORIENTED_EDGE ( 'NONE', *, *, #3344, .T. ) ;
#32499=DIRECTION ( 'NONE',  ( 0.000000000000000000, 0.000000000000000000, -1.000000000000000000 ) ) ;
#32505=AXIS2_PLACEMENT_3D ( 'NONE', #21168, #34418, #21395 ) ;
#32510=ORIENTED_EDGE ( 'NONE', *, *, #21743, .T. ) ;
#32517=CARTESIAN_POINT ( 'NONE',  ( 9.000000000000001776, -25.61928775981074935, 45.25098998563468200 ) ) ;
#32519=DIRECTION ( 'NONE',  ( 0.000000000000000000, 0.4817536741017162671, -0.8763066800438630288 ) ) ;
#32521=ORIENTED_EDGE ( 'NONE', *, *, #2383, .F. ) ;
#32526=AXIS2_PLACEMENT_3D ( 'NONE', #31148, #38522, #8642 ) ;
#32532=ORIENTED_EDGE ( 'NONE', *, *, #27297, .F. ) ;
#32535=ORIENTED_EDGE ( 'NONE', *, *, #15661, .T. ) ;
#32544=EDGE_CURVE ( 'NONE', #33622, #8604, #5958, .T. ) ;
#32553=DIRECTION ( 'NONE',  ( -1.000000000000000000, -0.000000000000000000, 0.000000000000000000 ) ) ;
#32569=ORIENTED_EDGE ( 'NONE', *, *, #36697, .F. ) ;
#32570=( NAMED_UNIT ( * ) SI_UNIT ( $, .STERADIAN. ) SOLID_ANGLE_UNIT ( ) );
#32573=AXIS2_PLACEMENT_3D ( 'NONE', #34505, #17991, #8332 ) ;
#32585=VERTEX_POINT ( 'NONE', #7859 ) ;
#32606=DIRECTION ( 'NONE',  ( -1.000000000000000000, -0.000000000000000000, 0.000000000000000000 ) ) ;
#32612=DIRECTION ( 'NONE',  ( -1.000000000000000000, -0.000000000000000000, 0.000000000000000000 ) ) ;
#32623=EDGE_CURVE ( 'NONE', #4717, #22785, #37289, .T. ) ;
#32625=CIRCLE ( 'NONE', #7518, 20.00000000000000711 ) ;
#32633=CIRCLE ( 'NONE', #13856, 20.00000000000000711 ) ;
#32635=AXIS2_PLACEMENT_3D ( 'NONE', #9667, #19728, #39307 ) ;
#32639=VERTEX_POINT ( 'NONE', #21446 ) ;
#32650=ORIENTED_EDGE ( 'NONE', *, *, #12261, .T. ) ;
#32658=CIRCLE ( 'NONE', #8279, 20.00000000000000711 ) ;
#32659=CARTESIAN_POINT ( 'NONE',  ( 9.000000000000001776, 44.25018368420742831, 27.31155879685195842 ) ) ;
#32660=DIRECTION ( 'NONE',  ( 0.000000000000000000, 0.000000000000000000, 1.000000000000000000 ) ) ;
#32684=CIRCLE ( 'NONE', #20177, 20.00000000000000355 ) ;
#32692=DIRECTION ( 'NONE',  ( 0.000000000000000000, 0.000000000000000000, -1.000000000000000000 ) ) ;
#32697=EDGE_CURVE ( 'NONE', #42073, #23910, #13652, .T. ) ;
#32699=CARTESIAN_POINT ( 'NONE',  ( 0.000000000000000000, 0.000000000000000000, 0.000000000000000000 ) ) ;
#32703=EDGE_CURVE ( 'NONE', #28999, #41125, #40764, .T. ) ;
#32705=DIRECTION ( 'NONE',  ( 0.000000000000000000, 0.000000000000000000, 1.000000000000000000 ) ) ;
#32710=CARTESIAN_POINT ( 'NONE',  ( 0.000000000000000000, 47.32430374665963058, -21.55018039121477713 ) ) ;
#32711=ADVANCED_FACE ( 'NONE', ( #28813 ), #28607, .T. ) ;
#32713=DIRECTION ( 'NONE',  ( 0.000000000000000000, 0.000000000000000000, 1.000000000000000000 ) ) ;
#32714=CARTESIAN_POINT ( 'NONE',  ( -10.00000000000000000, 0.000000000000000000, 0.000000000000000000 ) ) ;
#32727=DIRECTION ( 'NONE',  ( -1.000000000000000000, -0.000000000000000000, -0.000000000000000000 ) ) ;
#32729=CARTESIAN_POINT ( 'NONE',  ( 18.00000000000000355, 0.000000000000000000, 0.000000000000000000 ) ) ;
#32743=ORIENTED_EDGE ( 'NONE', *, *, #31777, .F. ) ;
#32766=CIRCLE ( 'NONE', #33456, 47.49900000000000233 ) ;
#32770=ADVANCED_FACE ( 'NONE', ( #31639 ), #2160, .T. ) ;
#32772=CARTESIAN_POINT ( 'NONE',  ( 0.000000000000000000, 0.000000000000000000, 0.000000000000000000 ) ) ;
#32790=FACE_OUTER_BOUND ( 'NONE', #4647, .T. ) ;
#32793=CYLINDRICAL_SURFACE ( 'NONE', #6153, 51.99999999999999289 ) ;
#32796=CARTESIAN_POINT ( 'NONE',  ( 0.000000000000000000, -46.21320724403641123, -10.97699764142002010 ) ) ;
#32797=ORIENTED_EDGE ( 'NONE', *, *, #7869, .F. ) ;
#32803=ORIENTED_EDGE ( 'NONE', *, *, #39165, .T. ) ;
#32816=VERTEX_POINT ( 'NONE', #22291 ) ;
#32824=VECTOR ( 'NONE', #38930, 1000.000000000000000 ) ;
#32826=VECTOR ( 'NONE', #41106, 1000.000000000000000 ) ;
#32830=CARTESIAN_POINT ( 'NONE',  ( 18.00000000000000355, -32.32520163883607722, 34.09746168776025854 ) ) ;
#32838=DIRECTION ( 'NONE',  ( -1.000000000000000000, 0.000000000000000000, -0.000000000000000000 ) ) ;
#32840=DIRECTION ( 'NONE',  ( 0.000000000000000000, 0.000000000000000000, 1.000000000000000000 ) ) ;
#32844=EDGE_CURVE ( 'NONE', #14699, #35634, #9791, .T. ) ;
#32855=DIRECTION ( 'NONE',  ( 0.000000000000000000, 0.000000000000000000, 1.000000000000000000 ) ) ;
#32867=FACE_OUTER_BOUND ( 'NONE', #34, .T. ) ;
#32868=EDGE_LOOP ( 'NONE', ( #26213, #26930, #27255, #21801 ) ) ;
#32886=VECTOR ( 'NONE', #16820, 1000.000000000000000 ) ;
#32899=DIRECTION ( 'NONE',  ( 0.000000000000000000, 0.000000000000000000, 1.000000000000000000 ) ) ;
#32901=DIRECTION ( 'NONE',  ( -1.000000000000000000, 0.000000000000000000, 0.000000000000000000 ) ) ;
#32908=CARTESIAN_POINT ( 'NONE',  ( 18.00000000000000355, -47.00885577955416039, 6.806061952192135500 ) ) ;
#32911=DIRECTION ( 'NONE',  ( 0.000000000000000000, 0.000000000000000000, 1.000000000000000000 ) ) ;
#32920=CIRCLE ( 'NONE', #32244, 20.00000000000000711 ) ;
#32927=PRODUCT_CONTEXT ( 'NONE', #5251, 'mechanical' ) ;
#32937=ADVANCED_FACE ( 'NONE', ( #29667 ), #33564, .T. ) ;
#32941=AXIS2_PLACEMENT_3D ( 'NONE', #6681, #40685, #16544 ) ;
#32952=CIRCLE ( 'NONE', #21153, 47.49900000000001654 ) ;
#32953=ORIENTED_EDGE ( 'NONE', *, *, #42963, .T. ) ;
#32959=ADVANCED_FACE ( 'NONE', ( #39873 ), #19441, .T. ) ;
#32962=CYLINDRICAL_SURFACE ( 'NONE', #9413, 51.99999999999999289 ) ;
#32963=LINE ( 'NONE', #30355, #12251 ) ;
#32969=VECTOR ( 'NONE', #14451, 1000.000000000000000 ) ;
#32972=VECTOR ( 'NONE', #8108, 1000.000000000000000 ) ;
#32974=VERTEX_POINT ( 'NONE', #19648 ) ;
#32976=CARTESIAN_POINT ( 'NONE',  ( 0.000000000000000000, -35.11945359308136716, 38.34871548466002622 ) ) ;
#32991=DIRECTION ( 'NONE',  ( -1.000000000000000000, 0.000000000000000000, -0.000000000000000000 ) ) ;
#32992=ORIENTED_EDGE ( 'NONE', *, *, #17308, .F. ) ;
#32993=DIRECTION ( 'NONE',  ( 0.000000000000000000, 0.000000000000000000, 1.000000000000000000 ) ) ;
#33016=EDGE_CURVE ( 'NONE', #17987, #11580, #42200, .T. ) ;
#33020=CARTESIAN_POINT ( 'NONE',  ( 0.000000000000000000, -29.60891106212762125, -37.14118181634796656 ) ) ;
#33022=ORIENTED_EDGE ( 'NONE', *, *, #23504, .T. ) ;
#33024=VECTOR ( 'NONE', #15940, 1000.000000000000000 ) ;
#33025=ORIENTED_EDGE ( 'NONE', *, *, #20230, .F. ) ;
#33041=CARTESIAN_POINT ( 'NONE',  ( 18.00000000000000355, 0.000000000000000000, 0.000000000000000000 ) ) ;
#33043=CARTESIAN_POINT ( 'NONE',  ( 18.00000000000000355, -38.92705108641711576, -27.21837053747839263 ) ) ;
#33046=ORIENTED_EDGE ( 'NONE', *, *, #21055, .F. ) ;
#33051=VERTEX_POINT ( 'NONE', #27460 ) ;
#33057=AXIS2_PLACEMENT_3D ( 'NONE', #42380, #12099, #25420 ) ;
#33065=DIRECTION ( 'NONE',  ( -1.000000000000000000, -0.000000000000000000, -0.000000000000000000 ) ) ;
#33069=CARTESIAN_POINT ( 'NONE',  ( 0.000000000000000000, 46.11014828289844303, -9.022736828080878624 ) ) ;
#33079=ORIENTED_EDGE ( 'NONE', *, *, #9372, .F. ) ;
#33081=DIRECTION ( 'NONE',  ( 0.000000000000000000, 0.000000000000000000, 1.000000000000000000 ) ) ;
#33090=ORIENTED_EDGE ( 'NONE', *, *, #956, .F. ) ;
#33092=AXIS2_PLACEMENT_3D ( 'NONE', #9975, #19837, #23323 ) ;
#33101=ORIENTED_EDGE ( 'NONE', *, *, #31376, .F. ) ;
#33109=CYLINDRICAL_SURFACE ( 'NONE', #36970, 51.99999999999999289 ) ;
#33111=DIRECTION ( 'NONE',  ( -1.000000000000000000, -0.000000000000000000, 0.000000000000000000 ) ) ;
#33112=AXIS2_PLACEMENT_3D ( 'NONE', #36029, #6155, #19500 ) ;
#33118=EDGE_CURVE ( 'NONE', #31429, #32974, #28368, .T. ) ;
#33136=ADVANCED_FACE ( 'NONE', ( #37691 ), #7810, .T. ) ;
#33137=AXIS2_PLACEMENT_3D ( 'NONE', #26905, #19736, #33647 ) ;
#33139=DIRECTION ( 'NONE',  ( 1.000000000000000000, 0.000000000000000000, 0.000000000000000000 ) ) ;
#33143=DIRECTION ( 'NONE',  ( -1.000000000000000000, 0.000000000000000000, -0.000000000000000000 ) ) ;
#33162=CARTESIAN_POINT ( 'NONE',  ( 18.00000000000000355, 0.000000000000000000, 0.000000000000000000 ) ) ;
#33174=ADVANCED_FACE ( 'NONE', ( #12183 ), #25506, .T. ) ;
#33181=CARTESIAN_POINT ( 'NONE',  ( 18.00000000000000355, 41.20225022064669673, -23.63323037071358357 ) ) ;
#33182=CIRCLE ( 'NONE', #17919, 20.00000000000000355 ) ;
#33186=ORIENTED_EDGE ( 'NONE', *, *, #25334, .T. ) ;
#33191=CARTESIAN_POINT ( 'NONE',  ( 0.000000000000000000, 0.000000000000000000, 0.000000000000000000 ) ) ;
#33195=DIRECTION ( 'NONE',  ( 0.000000000000000000, 0.000000000000000000, 1.000000000000000000 ) ) ;
#33212=CARTESIAN_POINT ( 'NONE',  ( -10.00000000000000000, 0.000000000000000000, 0.000000000000000000 ) ) ;
#33215=EDGE_CURVE ( 'NONE', #14276, #38773, #26255, .T. ) ;
#33222=CARTESIAN_POINT ( 'NONE',  ( 18.00000000000000355, 0.000000000000000000, 0.000000000000000000 ) ) ;
#33235=AXIS2_PLACEMENT_3D ( 'NONE', #19860, #42710, #36833 ) ;
#33238=EDGE_LOOP ( 'NONE', ( #26045, #17889, #786, #25302 ) ) ;
#33242=DIRECTION ( 'NONE',  ( -1.000000000000000000, -0.000000000000000000, 0.000000000000000000 ) ) ;
#33254=CARTESIAN_POINT ( 'NONE',  ( 18.00000000000000355, 30.93515269692114344, 36.04401931830261674 ) ) ;
#33258=DIRECTION ( 'NONE',  ( 0.000000000000000000, 0.000000000000000000, 1.000000000000000000 ) ) ;
#33262=DIRECTION ( 'NONE',  ( 0.000000000000000000, 0.000000000000000000, 1.000000000000000000 ) ) ;
#33276=ORIENTED_EDGE ( 'NONE', *, *, #34982, .F. ) ;
#33279=CARTESIAN_POINT ( 'NONE',  ( 9.000000000000001776, 40.47821179127714686, 32.64221760512772619 ) ) ;
#33287=AXIS2_PLACEMENT_3D ( 'NONE', #37713, #27939, #837 ) ;
#33305=VERTEX_POINT ( 'NONE', #36132 ) ;
#33311=AXIS2_PLACEMENT_3D ( 'NONE', #31680, #1124, #31474 ) ;
#33312=CARTESIAN_POINT ( 'NONE',  ( -10.00000000000000000, 0.000000000000000000, 0.000000000000000000 ) ) ;
#33316=CARTESIAN_POINT ( 'NONE',  ( 18.00000000000000355, -47.00885577955406802, -6.806061952192774989 ) ) ;
#33317=VERTEX_POINT ( 'NONE', #26127 ) ;
#33321=VERTEX_POINT ( 'NONE', #6251 ) ;
#33322=DIRECTION ( 'NONE',  ( 0.000000000000000000, 0.000000000000000000, 1.000000000000000000 ) ) ;
#33332=DIRECTION ( 'NONE',  ( -1.000000000000000000, 0.000000000000000000, 0.000000000000000000 ) ) ;
#33340=ADVANCED_FACE ( 'NONE', ( #32867 ), #9947, .T. ) ;
#33344=ADVANCED_FACE ( 'NONE', ( #20039 ), #40031, .F. ) ;
#33354=CARTESIAN_POINT ( 'NONE',  ( 18.00000000000000355, -46.19362259308839214, 8.585149169758333088 ) ) ;
#33355=CYLINDRICAL_SURFACE ( 'NONE', #33235, 20.00000000000000355 ) ;
#33358=ORIENTED_EDGE ( 'NONE', *, *, #8265, .T. ) ;
#33361=LINE ( 'NONE', #819, #32886 ) ;
#33362=DIRECTION ( 'NONE',  ( 0.000000000000000000, -0.9510565162951565288, 0.3090169943749382919 ) ) ;
#33375=DIRECTION ( 'NONE',  ( 0.000000000000000000, -0.9822872507286903865, 0.1873813145857150808 ) ) ;
#33378=ORIENTED_EDGE ( 'NONE', *, *, #28640, .F. ) ;
#33382=ORIENTED_EDGE ( 'NONE', *, *, #23463, .F. ) ;
#33391=DIRECTION ( 'NONE',  ( 1.000000000000000000, -0.000000000000000000, -0.000000000000000000 ) ) ;
#33402=CIRCLE ( 'NONE', #3424, 47.49900000000000944 ) ;
#33415=ORIENTED_EDGE ( 'NONE', *, *, #361, .T. ) ;
#33429=DIRECTION ( 'NONE',  ( -1.000000000000000000, 0.000000000000000000, -0.000000000000000000 ) ) ;
#33432=DIRECTION ( 'NONE',  ( 0.000000000000000000, 0.000000000000000000, 1.000000000000000000 ) ) ;
#33445=CARTESIAN_POINT ( 'NONE',  ( 18.00000000000000355, 0.000000000000000000, 0.000000000000000000 ) ) ;
#33456=AXIS2_PLACEMENT_3D ( 'NONE', #25764, #5656, #19218 ) ;
#33457=EDGE_CURVE ( 'NONE', #16830, #12278, #13256, .T. ) ;
#33459=DIRECTION ( 'NONE',  ( -1.000000000000000000, -0.000000000000000000, 0.000000000000000000 ) ) ;
#33462=ORIENTED_EDGE ( 'NONE', *, *, #4641, .T. ) ;
#33464=ORIENTED_EDGE ( 'NONE', *, *, #23628, .T. ) ;
#33466=CARTESIAN_POINT ( 'NONE',  ( 18.00000000000000355, 0.000000000000000000, 0.000000000000000000 ) ) ;
#33469=EDGE_CURVE ( 'NONE', #2698, #16003, #10197, .T. ) ;
#33473=CIRCLE ( 'NONE', #2801, 47.49900000000000233 ) ;
#33485=CIRCLE ( 'NONE', #16836, 47.49900000000000233 ) ;
#33486=ADVANCED_FACE ( 'NONE', ( #20457 ), #7313, .T. ) ;
#33487=CIRCLE ( 'NONE', #23686, 20.00000000000000000 ) ;
#33502=ORIENTED_EDGE ( 'NONE', *, *, #19618, .T. ) ;
#33504=LINE ( 'NONE', #23932, #39110 ) ;
#33509=ADVANCED_FACE ( 'NONE', ( #36992 ), #13682, .T. ) ;
#33514=DIRECTION ( 'NONE',  ( -1.000000000000000000, 0.000000000000000000, 0.000000000000000000 ) ) ;
#33515=VERTEX_POINT ( 'NONE', #40680 ) ;
#33516=VECTOR ( 'NONE', #27628, 1000.000000000000000 ) ;
#33518=CARTESIAN_POINT ( 'NONE',  ( 18.00000000000000355, 29.60891106212788415, 37.14118181634774629 ) ) ;
#33532=FACE_OUTER_BOUND ( 'NONE', #7444, .T. ) ;
#33536=ORIENTED_EDGE ( 'NONE', *, *, #1853, .F. ) ;
#33540=DIRECTION ( 'NONE',  ( -1.000000000000000000, 0.000000000000000000, 0.000000000000000000 ) ) ;
#33548=VECTOR ( 'NONE', #23725, 1000.000000000000000 ) ;
#33559=DIRECTION ( 'NONE',  ( 0.000000000000000000, 0.5877852522924686962, 0.8090169943749506709 ) ) ;
#33564=CYLINDRICAL_SURFACE ( 'NONE', #14369, 20.00000000000000711 ) ;
#33577=AXIS2_PLACEMENT_3D ( 'NONE', #13827, #40819, #24519 ) ;
#33578=EDGE_CURVE ( 'NONE', #11001, #32412, #16526, .T. ) ;
#33581=CIRCLE ( 'NONE', #4322, 47.49899999999999523 ) ;
#33585=DIRECTION ( 'NONE',  ( -1.000000000000000000, -0.000000000000000000, -0.000000000000000000 ) ) ;
#33611=ORIENTED_EDGE ( 'NONE', *, *, #9253, .F. ) ;
#33622=VERTEX_POINT ( 'NONE', #5126 ) ;
#33623=DIRECTION ( 'NONE',  ( -1.000000000000000000, 0.000000000000000000, 0.000000000000000000 ) ) ;
#33627=EDGE_CURVE ( 'NONE', #37085, #4630, #8736, .T. ) ;
#33632=ORIENTED_EDGE ( 'NONE', *, *, #24927, .T. ) ;
#33634=DIRECTION ( 'NONE',  ( 0.000000000000000000, 0.000000000000000000, 1.000000000000000000 ) ) ;
#33646=DIRECTION ( 'NONE',  ( 0.000000000000000000, 0.000000000000000000, -1.000000000000000000 ) ) ;
#33647=DIRECTION ( 'NONE',  ( 0.000000000000000000, 0.000000000000000000, 1.000000000000000000 ) ) ;
#33648=ORIENTED_EDGE ( 'NONE', *, *, #25037, .F. ) ;
#33652=ORIENTED_EDGE ( 'NONE', *, *, #40, .F. ) ;
#33656=VERTEX_POINT ( 'NONE', #41778 ) ;
#33662=CIRCLE ( 'NONE', #31595, 52.00000000000000000 ) ;
#33665=CARTESIAN_POINT ( 'NONE',  ( 18.00000000000000355, -5.667686777402029641, 46.64153600743603789 ) ) ;
#33671=EDGE_CURVE ( 'NONE', #8463, #31266, #38005, .T. ) ;
#33674=ORIENTED_EDGE ( 'NONE', *, *, #27471, .F. ) ;
#33675=CARTESIAN_POINT ( 'NONE',  ( 0.000000000000000000, -27.43636312076348815, 38.14186064215142835 ) ) ;
#33685=DIRECTION ( 'NONE',  ( 1.000000000000000000, -0.000000000000000000, -0.000000000000000000 ) ) ;
#33695=ADVANCED_FACE ( 'NONE', ( #4918 ), #25451, .T. ) ;
#33721=ORIENTED_EDGE ( 'NONE', *, *, #10671, .F. ) ;
#33732=CARTESIAN_POINT ( 'NONE',  ( 0.000000000000000000, -27.79676263918163315, -37.88001506494799031 ) ) ;
#33735=VECTOR ( 'NONE', #10437, 1000.000000000000000 ) ;
#33736=ORIENTED_EDGE ( 'NONE', *, *, #12622, .F. ) ;
#33746=CARTESIAN_POINT ( 'NONE',  ( 0.000000000000000000, -31.08872492059927595, -41.68322423723131465 ) ) ;
#33761=ORIENTED_EDGE ( 'NONE', *, *, #30559, .T. ) ;
#33764=ORIENTED_EDGE ( 'NONE', *, *, #18108, .T. ) ;
#33771=DIRECTION ( 'NONE',  ( -1.000000000000000000, 0.000000000000000000, 0.000000000000000000 ) ) ;
#33772=CARTESIAN_POINT ( 'NONE',  ( 18.00000000000000355, -46.87740477351715640, -3.172455868805708956 ) ) ;
#33837=ORIENTED_EDGE ( 'NONE', *, *, #5779, .T. ) ;
#33846=CARTESIAN_POINT ( 'NONE',  ( 18.00000000000000355, 0.000000000000000000, 0.000000000000000000 ) ) ;
#33847=ORIENTED_EDGE ( 'NONE', *, *, #31907, .T. ) ;
#33856=CARTESIAN_POINT ( 'NONE',  ( 9.000000000000001776, 51.19683565102456413, -9.104066087302932431 ) ) ;
#33859=DIRECTION ( 'NONE',  ( -1.000000000000000000, 0.000000000000000000, -0.000000000000000000 ) ) ;
#33864=ORIENTED_EDGE ( 'NONE', *, *, #27769, .F. ) ;
#33869=DIRECTION ( 'NONE',  ( 0.000000000000000000, 0.7705132427757861446, 0.6374239897486935202 ) ) ;
#33877=EDGE_CURVE ( 'NONE', #41807, #26478, #40102, .T. ) ;
#33879=ORIENTED_EDGE ( 'NONE', *, *, #38876, .T. ) ;
#33881=ORIENTED_EDGE ( 'NONE', *, *, #21611, .F. ) ;
#33888=DIRECTION ( 'NONE',  ( -1.000000000000000000, 0.000000000000000000, 0.000000000000000000 ) ) ;
#33890=VERTEX_POINT ( 'NONE', #23247 ) ;
#33892=DIRECTION ( 'NONE',  ( -1.000000000000000000, 0.000000000000000000, 0.000000000000000000 ) ) ;
#33903=DIRECTION ( 'NONE',  ( 0.000000000000000000, 0.000000000000000000, 1.000000000000000000 ) ) ;
#33904=ORIENTED_EDGE ( 'NONE', *, *, #1550, .T. ) ;
#33905=AXIS2_PLACEMENT_3D ( 'NONE', #27694, #40958, #14168 ) ;
#33911=DIRECTION ( 'NONE',  ( -1.000000000000000000, 0.000000000000000000, -0.000000000000000000 ) ) ;
#33929=ADVANCED_FACE ( 'NONE', ( #36942 ), #14273, .T. ) ;
#33933=EDGE_CURVE ( 'NONE', #8384, #4825, #34109, .T. ) ;
#33951=EDGE_CURVE ( 'NONE', #41712, #21090, #6670, .T. ) ;
#33956=EDGE_CURVE ( 'NONE', #17013, #909, #31077, .T. ) ;
#33958=VERTEX_POINT ( 'NONE', #919 ) ;
#33959=DIRECTION ( 'NONE',  ( -1.000000000000000000, -0.000000000000000000, -0.000000000000000000 ) ) ;
#33968=AXIS2_PLACEMENT_3D ( 'NONE', #4164, #672, #41248 ) ;
#33970=LINE ( 'NONE', #23964, #26297 ) ;
#33971=ORIENTED_EDGE ( 'NONE', *, *, #32335, .F. ) ;
#33972=AXIS2_PLACEMENT_3D ( 'NONE', #18948, #5377, #22220 ) ;
#33973=LINE ( 'NONE', #30504, #16537 ) ;
#33975=VECTOR ( 'NONE', #30176, 1000.000000000000000 ) ;
#33980=CARTESIAN_POINT ( 'NONE',  ( 0.000000000000000000, 51.19683565102457834, -9.104066087302939536 ) ) ;
#33997=AXIS2_PLACEMENT_3D ( 'NONE', #12691, #42541, #8540 ) ;
#34010=EDGE_CURVE ( 'NONE', #24871, #14972, #17882, .T. ) ;
#34031=EDGE_CURVE ( 'NONE', #15847, #18339, #38038, .T. ) ;
#34036=AXIS2_PLACEMENT_3D ( 'NONE', #29114, #9868, #23221 ) ;
#34037=EDGE_LOOP ( 'NONE', ( #35689, #11519, #8902, #8271 ) ) ;
#34039=DIRECTION ( 'NONE',  ( -1.000000000000000000, 0.000000000000000000, -0.000000000000000000 ) ) ;
#34041=ORIENTED_EDGE ( 'NONE', *, *, #41457, .F. ) ;
#34043=ORIENTED_EDGE ( 'NONE', *, *, #41227, .F. ) ;
#34044=CARTESIAN_POINT ( 'NONE',  ( 18.00000000000000355, 46.11014828289831513, 9.022736828081521665 ) ) ;
#34048=VERTEX_POINT ( 'NONE', #30421 ) ;
#34053=CARTESIAN_POINT ( 'NONE',  ( 9.000000000000001776, -0.6505223195686603566, 51.99593080916757515 ) ) ;
#34060=EDGE_CURVE ( 'NONE', #16003, #10495, #30641, .T. ) ;
#34065=CARTESIAN_POINT ( 'NONE',  ( 0.000000000000000000, 46.11014828289831513, 9.022736828081521665 ) ) ;
#34067=ORIENTED_EDGE ( 'NONE', *, *, #662, .T. ) ;
#34071=EDGE_LOOP ( 'NONE', ( #16922, #2574, #13156, #18660 ) ) ;
#34072=DIRECTION ( 'NONE',  ( 0.000000000000000000, 0.7705132427757904745, -0.6374239897486881912 ) ) ;
#34078=DIRECTION ( 'NONE',  ( -1.000000000000000000, 0.000000000000000000, 0.000000000000000000 ) ) ;
#34079=ORIENTED_EDGE ( 'NONE', *, *, #13074, .F. ) ;
#34081=ORIENTED_EDGE ( 'NONE', *, *, #29004, .F. ) ;
#34086=CIRCLE ( 'NONE', #23658, 20.00000000000000355 ) ;
#34095=ORIENTED_EDGE ( 'NONE', *, *, #39601, .T. ) ;
#34097=ORIENTED_EDGE ( 'NONE', *, *, #21796, .F. ) ;
#34100=CARTESIAN_POINT ( 'NONE',  ( 18.00000000000000355, -43.55304910509425298, 28.41006711799970219 ) ) ;
#34109=LINE ( 'NONE', #17785, #363 ) ;
#34113=EDGE_CURVE ( 'NONE', #23617, #14608, #18437, .T. ) ;
#34124=ORIENTED_EDGE ( 'NONE', *, *, #5330, .T. ) ;
#34128=EDGE_LOOP ( 'NONE', ( #16349, #38375, #30157, #25144 ) ) ;
#34130=ORIENTED_EDGE ( 'NONE', *, *, #36701, .T. ) ;
#34132=CARTESIAN_POINT ( 'NONE',  ( 0.000000000000000000, 0.000000000000000000, 0.000000000000000000 ) ) ;
#34137=ORIENTED_EDGE ( 'NONE', *, *, #4407, .T. ) ;
#34139=DIRECTION ( 'NONE',  ( 0.000000000000000000, 0.000000000000000000, 1.000000000000000000 ) ) ;
#34141=ORIENTED_EDGE ( 'NONE', *, *, #3322, .T. ) ;
#34146=DIRECTION ( 'NONE',  ( -1.000000000000000000, -0.000000000000000000, 0.000000000000000000 ) ) ;
#34148=ORIENTED_EDGE ( 'NONE', *, *, #35560, .T. ) ;
#34164=CIRCLE ( 'NONE', #23062, 20.00000000000001066 ) ;
#34166=FACE_OUTER_BOUND ( 'NONE', #23427, .T. ) ;
#34181=DIRECTION ( 'NONE',  ( 0.000000000000000000, -0.6845471059286950544, 0.7289686274214053352 ) ) ;
#34184=DIRECTION ( 'NONE',  ( 0.000000000000000000, 0.000000000000000000, 1.000000000000000000 ) ) ;
#34189=DIRECTION ( 'NONE',  ( -1.000000000000000000, 0.000000000000000000, 0.000000000000000000 ) ) ;
#34197=ORIENTED_EDGE ( 'NONE', *, *, #4165, .T. ) ;
#34203=VERTEX_POINT ( 'NONE', #22141 ) ;
#34212=CARTESIAN_POINT ( 'NONE',  ( 18.00000000000000355, -47.32430374665946715, 21.55018039121508977 ) ) ;
#34215=AXIS2_PLACEMENT_3D ( 'NONE', #30101, #29896, #381 ) ;
#34223=EDGE_CURVE ( 'NONE', #19720, #35293, #38443, .T. ) ;
#34233=DIRECTION ( 'NONE',  ( -1.000000000000000000, 0.000000000000000000, 0.000000000000000000 ) ) ;
#34247=CARTESIAN_POINT ( 'NONE',  ( 18.00000000000000355, 27.43636312076321104, 38.14186064215159888 ) ) ;
#34248=CARTESIAN_POINT ( 'NONE',  ( 18.00000000000000355, -27.79676263918163315, -37.88001506494799031 ) ) ;
#34251=ORIENTED_EDGE ( 'NONE', *, *, #41715, .T. ) ;
#34270=EDGE_CURVE ( 'NONE', #42728, #5490, #13714, .T. ) ;
#34297=EDGE_CURVE ( 'NONE', #5537, #19539, #14399, .T. ) ;
#34312=EDGE_LOOP ( 'NONE', ( #32470, #11537, #7197, #22646 ) ) ;
#34314=VERTEX_POINT ( 'NONE', #40320 ) ;
#34319=FACE_OUTER_BOUND ( 'NONE', #2086, .T. ) ;
#34321=EDGE_CURVE ( 'NONE', #26486, #10423, #30429, .T. ) ;
#34328=DIRECTION ( 'NONE',  ( -1.000000000000000000, 0.000000000000000000, 0.000000000000000000 ) ) ;
#34341=EDGE_LOOP ( 'NONE', ( #21627, #7481, #8274, #15599 ) ) ;
#34342=CARTESIAN_POINT ( 'NONE',  ( 0.000000000000000000, -51.19683565102437939, -9.104066087303987587 ) ) ;
#34345=DIRECTION ( 'NONE',  ( -1.000000000000000000, -0.000000000000000000, 0.000000000000000000 ) ) ;
#34347=EDGE_CURVE ( 'NONE', #2287, #3059, #29036, .T. ) ;
#34349=ORIENTED_EDGE ( 'NONE', *, *, #19880, .T. ) ;
#34363=CARTESIAN_POINT ( 'NONE',  ( 18.00000000000000355, 27.79676263918187118, 37.88001506494779846 ) ) ;
#34367=CARTESIAN_POINT ( 'NONE',  ( 18.00000000000000355, -29.60891106212812574, 37.14118181634756155 ) ) ;
#34377=ORIENTED_EDGE ( 'NONE', *, *, #29985, .T. ) ;
#34399=AXIS2_PLACEMENT_3D ( 'NONE', #4571, #18163, #24038 ) ;
#34408=DIRECTION ( 'NONE',  ( -1.000000000000000000, -0.000000000000000000, 0.000000000000000000 ) ) ;
#34410=ORIENTED_EDGE ( 'NONE', *, *, #41033, .F. ) ;
#34415=CARTESIAN_POINT ( 'NONE',  ( 18.00000000000000355, -20.99948489194451540, 42.60488980472774045 ) ) ;
#34418=DIRECTION ( 'NONE',  ( -1.000000000000000000, 0.000000000000000000, 0.000000000000000000 ) ) ;
#34428=FACE_OUTER_BOUND ( 'NONE', #25598, .T. ) ;
#34429=FACE_OUTER_BOUND ( 'NONE', #35471, .T. ) ;
#34430=AXIS2_PLACEMENT_3D ( 'NONE', #12226, #12447, #31432 ) ;
#34432=AXIS2_PLACEMENT_3D ( 'NONE', #35539, #14869, #5659 ) ;
#34436=VERTEX_POINT ( 'NONE', #6481 ) ;
#34440=AXIS2_PLACEMENT_3D ( 'NONE', #21369, #37670, #11088 ) ;
#34452=DIRECTION ( 'NONE',  ( 0.000000000000000000, 0.000000000000000000, 1.000000000000000000 ) ) ;
#34465=AXIS2_PLACEMENT_3D ( 'NONE', #13172, #17696, #39734 ) ;
#34471=DIRECTION ( 'NONE',  ( 0.000000000000000000, 0.7705132427757859226, 0.6374239897486936313 ) ) ;
#34474=LINE ( 'NONE', #4581, #1553 ) ;
#34475=LINE ( 'NONE', #4584, #39859 ) ;
#34477=ORIENTED_EDGE ( 'NONE', *, *, #8051, .T. ) ;
#34479=CIRCLE ( 'NONE', #3772, 47.49899999999998812 ) ;
#34489=AXIS2_PLACEMENT_3D ( 'NONE', #31326, #35012, #5914 ) ;
#34498=CARTESIAN_POINT ( 'NONE',  ( 18.00000000000000355, 46.90537658765334328, -2.727856614653797251 ) ) ;
#34505=CARTESIAN_POINT ( 'NONE',  ( 18.00000000000000355, -22.43957647427129842, -41.27978878573651400 ) ) ;
#34510=CARTESIAN_POINT ( 'NONE',  ( 18.00000000000000355, -36.05989434073635636, 30.12041790338605551 ) ) ;
#34513=CIRCLE ( 'NONE', #33112, 47.49900000000000944 ) ;
#34519=CARTESIAN_POINT ( 'NONE',  ( 18.00000000000000355, -46.87740477351715640, -3.172455868805708956 ) ) ;
#34523=ORIENTED_EDGE ( 'NONE', *, *, #34031, .T. ) ;
#34526=ORIENTED_EDGE ( 'NONE', *, *, #8734, .T. ) ;
#34533=DIRECTION ( 'NONE',  ( 1.000000000000000000, -0.000000000000000000, 0.000000000000000000 ) ) ;
#34535=VERTEX_POINT ( 'NONE', #25947 ) ;
#34548=VERTEX_POINT ( 'NONE', #42276 ) ;
#34550=DIRECTION ( 'NONE',  ( 0.000000000000000000, 0.000000000000000000, 1.000000000000000000 ) ) ;
#34559=ORIENTED_EDGE ( 'NONE', *, *, #8813, .T. ) ;
#34568=VERTEX_POINT ( 'NONE', #22273 ) ;
#34570=FACE_OUTER_BOUND ( 'NONE', #37584, .T. ) ;
#34571=AXIS2_PLACEMENT_3D ( 'NONE', #1247, #37887, #9082 ) ;
#34575=ORIENTED_EDGE ( 'NONE', *, *, #891, .F. ) ;
#34586=ORIENTED_EDGE ( 'NONE', *, *, #18992, .T. ) ;
#34591=CARTESIAN_POINT ( 'NONE',  ( 18.00000000000000355, -27.43636312076348815, 38.14186064215142835 ) ) ;
#34608=AXIS2_PLACEMENT_3D ( 'NONE', #29360, #32398, #33903 ) ;
#34614=CARTESIAN_POINT ( 'NONE',  ( 18.00000000000000355, -51.93417535146743802, 2.615612846549011383 ) ) ;
#34634=ORIENTED_EDGE ( 'NONE', *, *, #133, .T. ) ;
#34644=ORIENTED_EDGE ( 'NONE', *, *, #19876, .T. ) ;
#34647=EDGE_LOOP ( 'NONE', ( #21637, #36571, #446, #9463 ) ) ;
#34651=ORIENTED_EDGE ( 'NONE', *, *, #10125, .T. ) ;
#34652=DIRECTION ( 'NONE',  ( 1.000000000000000000, 0.000000000000000000, 0.000000000000000000 ) ) ;
#34662=AXIS2_PLACEMENT_3D ( 'NONE', #8181, #35432, #8387 ) ;
#34685=DIRECTION ( 'NONE',  ( 0.000000000000000000, 0.000000000000000000, -1.000000000000000000 ) ) ;
#34688=CIRCLE ( 'NONE', #29138, 20.00000000000000711 ) ;
#34694=ORIENTED_EDGE ( 'NONE', *, *, #5686, .T. ) ;
#34700=VECTOR ( 'NONE', #27633, 1000.000000000000000 ) ;
#34701=FACE_OUTER_BOUND ( 'NONE', #902, .T. ) ;
#34702=ORIENTED_EDGE ( 'NONE', *, *, #2848, .F. ) ;
#34717=LINE ( 'NONE', #7880, #367 ) ;
#34721=EDGE_CURVE ( 'NONE', #36878, #9086, #14433, .T. ) ;
#34728=AXIS2_PLACEMENT_3D ( 'NONE', #40997, #38746, #4559 ) ;
#34736=ORIENTED_EDGE ( 'NONE', *, *, #2206, .T. ) ;
#34739=ORIENTED_EDGE ( 'NONE', *, *, #22986, .F. ) ;
#34742=EDGE_CURVE ( 'NONE', #3059, #40767, #10940, .T. ) ;
#34744=ORIENTED_EDGE ( 'NONE', *, *, #20368, .T. ) ;
#34766=ORIENTED_EDGE ( 'NONE', *, *, #20312, .T. ) ;
#34778=CARTESIAN_POINT ( 'NONE',  ( 18.00000000000000355, 0.000000000000000000, 0.000000000000000000 ) ) ;
#34783=VERTEX_POINT ( 'NONE', #4950 ) ;
#34789=CARTESIAN_POINT ( 'NONE',  ( 18.00000000000000355, -44.25018368420723647, -27.31155879685227106 ) ) ;
#34797=ORIENTED_EDGE ( 'NONE', *, *, #12257, .T. ) ;
#34802=FACE_OUTER_BOUND ( 'NONE', #37946, .T. ) ;
#34806=AXIS2_PLACEMENT_3D ( 'NONE', #24645, #14165, #27246 ) ;
#34807=CIRCLE ( 'NONE', #17437, 51.99999999999999289 ) ;
#34810=DIRECTION ( 'NONE',  ( 0.000000000000000000, 0.4817536741017100499, 0.8763066800438665815 ) ) ;
#34812=CARTESIAN_POINT ( 'NONE',  ( 18.00000000000000355, 47.49120266317495265, -0.8606222198177008176 ) ) ;
#34819=CARTESIAN_POINT ( 'NONE',  ( 18.00000000000000355, 0.000000000000000000, 0.000000000000000000 ) ) ;
#34821=ADVANCED_FACE ( 'NONE', ( #28323 ), #11511, .T. ) ;
#34823=DIRECTION ( 'NONE',  ( 0.000000000000000000, 0.000000000000000000, 1.000000000000000000 ) ) ;
#34824=EDGE_CURVE ( 'NONE', #24285, #39306, #18522, .T. ) ;
#34825=CARTESIAN_POINT ( 'NONE',  ( 18.00000000000000355, -19.44205635905570873, 43.33776004284602124 ) ) ;
#34836=ORIENTED_EDGE ( 'NONE', *, *, #32623, .T. ) ;
#34839=CARTESIAN_POINT ( 'NONE',  ( 0.000000000000000000, 49.25004636492411692, -16.68630974939707556 ) ) ;
#34841=CARTESIAN_POINT ( 'NONE',  ( 18.00000000000000355, 30.93515269692163017, -36.04401931830219752 ) ) ;
#34845=EDGE_CURVE ( 'NONE', #16742, #42167, #24193, .T. ) ;
#34847=EDGE_CURVE ( 'NONE', #39905, #40629, #37878, .T. ) ;
#34850=DIRECTION ( 'NONE',  ( 0.000000000000000000, 0.000000000000000000, 1.000000000000000000 ) ) ;
#34853=CARTESIAN_POINT ( 'NONE',  ( 9.000000000000001776, 51.85248208264517444, 3.914090171286374265 ) ) ;
#34862=ORIENTED_EDGE ( 'NONE', *, *, #29586, .F. ) ;
#34866=AXIS2_PLACEMENT_3D ( 'NONE', #964, #14975, #7960 ) ;
#34867=CIRCLE ( 'NONE', #16077, 7.500000000000000000 ) ;
#34885=ORIENTED_EDGE ( 'NONE', *, *, #18108, .F. ) ;
#34888=CARTESIAN_POINT ( 'NONE',  ( 18.00000000000000355, 35.11945359308163006, -38.34871548465977753 ) ) ;
#34892=AXIS2_PLACEMENT_3D ( 'NONE', #22651, #39384, #16090 ) ;
#34899=EDGE_CURVE ( 'NONE', #30887, #5278, #38104, .T. ) ;
#34903=ORIENTED_EDGE ( 'NONE', *, *, #28712, .T. ) ;
#34907=VECTOR ( 'NONE', #5460, 1000.000000000000000 ) ;
#34915=EDGE_CURVE ( 'NONE', #16293, #34548, #40168, .T. ) ;
#34917=CARTESIAN_POINT ( 'NONE',  ( 0.000000000000000000, -47.22458491092815791, -5.098390039074710778 ) ) ;
#34934=DIRECTION ( 'NONE',  ( 0.000000000000000000, 0.000000000000000000, 1.000000000000000000 ) ) ;
#34982=EDGE_CURVE ( 'NONE', #36319, #6919, #29065, .T. ) ;
#34988=DIRECTION ( 'NONE',  ( -1.000000000000000000, -0.000000000000000000, -0.000000000000000000 ) ) ;
#34989=AXIS2_PLACEMENT_3D ( 'NONE', #42701, #16344, #13087 ) ;
#34993=ORIENTED_EDGE ( 'NONE', *, *, #40623, .T. ) ;
#34997=DIRECTION ( 'NONE',  ( -1.000000000000000000, -0.000000000000000000, 0.000000000000000000 ) ) ;
#34998=CARTESIAN_POINT ( 'NONE',  ( 18.00000000000000355, 0.000000000000000000, 0.000000000000000000 ) ) ;
#34999=ORIENTED_EDGE ( 'NONE', *, *, #15661, .F. ) ;
#35012=DIRECTION ( 'NONE',  ( -1.000000000000000000, 0.000000000000000000, -0.000000000000000000 ) ) ;
#35013=ORIENTED_EDGE ( 'NONE', *, *, #11477, .F. ) ;
#35015=FACE_OUTER_BOUND ( 'NONE', #4561, .T. ) ;
#35026=CARTESIAN_POINT ( 'NONE',  ( 18.00000000000000355, 0.000000000000000000, 0.000000000000000000 ) ) ;
#35038=DIRECTION ( 'NONE',  ( 0.000000000000000000, 0.000000000000000000, 1.000000000000000000 ) ) ;
#35043=CARTESIAN_POINT ( 'NONE',  ( 0.000000000000000000, 46.87740477351718482, -3.172455868805370560 ) ) ;
#35044=DIRECTION ( 'NONE',  ( -1.000000000000000000, 0.000000000000000000, -0.000000000000000000 ) ) ;
#35048=CARTESIAN_POINT ( 'NONE',  ( 0.000000000000000000, 0.000000000000000000, 0.000000000000000000 ) ) ;
#35050=DIRECTION ( 'NONE',  ( -1.000000000000000000, -0.000000000000000000, -0.000000000000000000 ) ) ;
#35051=CIRCLE ( 'NONE', #39887, 20.00000000000000355 ) ;
#35055=ADVANCED_FACE ( 'NONE', ( #38741 ), #12159, .T. ) ;
#35057=DIRECTION ( 'NONE',  ( 0.000000000000000000, 0.000000000000000000, -1.000000000000000000 ) ) ;
#35060=ORIENTED_EDGE ( 'NONE', *, *, #792, .T. ) ;
#35064=EDGE_CURVE ( 'NONE', #42813, #18280, #17255, .T. ) ;
#35071=ORIENTED_EDGE ( 'NONE', *, *, #20552, .T. ) ;
#35082=EDGE_CURVE ( 'NONE', #20186, #23198, #18677, .T. ) ;
#35083=EDGE_CURVE ( 'NONE', #17013, #34048, #1880, .T. ) ;
#35084=ORIENTED_EDGE ( 'NONE', *, *, #32844, .T. ) ;
#35098=CYLINDRICAL_SURFACE ( 'NONE', #36941, 20.00000000000000355 ) ;
#35101=CARTESIAN_POINT ( 'NONE',  ( 18.00000000000000355, -46.87740477351715640, -3.172455868805708956 ) ) ;
#35102=VERTEX_POINT ( 'NONE', #6871 ) ;
#35106=VERTEX_POINT ( 'NONE', #3138 ) ;
#35135=VERTEX_POINT ( 'NONE', #40654 ) ;
#35142=CARTESIAN_POINT ( 'NONE',  ( -10.00000000000000000, 0.000000000000000000, 0.000000000000000000 ) ) ;
#35144=AXIS2_PLACEMENT_3D ( 'NONE', #15668, #42024, #22016 ) ;
#35150=CARTESIAN_POINT ( 'NONE',  ( 18.00000000000000355, 38.92705108641732892, 27.21837053747810842 ) ) ;
#35157=ORIENTED_EDGE ( 'NONE', *, *, #4245, .F. ) ;
#35159=ORIENTED_EDGE ( 'NONE', *, *, #31907, .F. ) ;
#35192=ORIENTED_EDGE ( 'NONE', *, *, #29821, .T. ) ;
#35206=AXIS2_PLACEMENT_3D ( 'NONE', #1204, #37427, #40259 ) ;
#35213=DIRECTION ( 'NONE',  ( -0.000000000000000000, 0.000000000000000000, 1.000000000000000000 ) ) ;
#35258=CARTESIAN_POINT ( 'NONE',  ( 18.00000000000000355, 3.840921266750508156, -47.34345070675165346 ) ) ;
#35260=DIRECTION ( 'NONE',  ( 0.000000000000000000, -0.5877852522924802425, 0.8090169943749421222 ) ) ;
#35263=CYLINDRICAL_SURFACE ( 'NONE', #42272, 47.49900000000000233 ) ;
#35264=DIRECTION ( 'NONE',  ( -1.000000000000000000, 0.000000000000000000, 0.000000000000000000 ) ) ;
#35265=ORIENTED_EDGE ( 'NONE', *, *, #20759, .T. ) ;
#35271=EDGE_CURVE ( 'NONE', #3223, #24128, #19365, .T. ) ;
#35272=AXIS2_PLACEMENT_3D ( 'NONE', #8856, #38510, #35664 ) ;
#35275=ORIENTED_EDGE ( 'NONE', *, *, #4766, .F. ) ;
#35282=EDGE_CURVE ( 'NONE', #26486, #36379, #14299, .T. ) ;
#35288=AXIS2_PLACEMENT_3D ( 'NONE', #41371, #8010, #11520 ) ;
#35291=CARTESIAN_POINT ( 'NONE',  ( 18.00000000000000355, 35.20873326984080620, 31.88259874184042886 ) ) ;
#35293=VERTEX_POINT ( 'NONE', #1832 ) ;
#35294=CARTESIAN_POINT ( 'NONE',  ( -10.00000000000000000, 0.000000000000000000, 0.000000000000000000 ) ) ;
#35297=EDGE_CURVE ( 'NONE', #10495, #11938, #39482, .T. ) ;
#35312=CARTESIAN_POINT ( 'NONE',  ( -10.00000000000000000, 0.000000000000000000, 0.000000000000000000 ) ) ;
#35313=VECTOR ( 'NONE', #40933, 1000.000000000000000 ) ;
#35319=ORIENTED_EDGE ( 'NONE', *, *, #24444, .T. ) ;
#35325=CARTESIAN_POINT ( 'NONE',  ( 0.000000000000000000, -32.32520163883607722, 34.09746168776025854 ) ) ;
#35326=ORIENTED_EDGE ( 'NONE', *, *, #36948, .T. ) ;
#35330=CARTESIAN_POINT ( 'NONE',  ( 18.00000000000000355, 43.83938735307292944, -18.28286404005752175 ) ) ;
#35332=ADVANCED_FACE ( 'NONE', ( #41756 ), #7734, .T. ) ;
#35341=EDGE_LOOP ( 'NONE', ( #16635, #2398, #2089, #39577 ) ) ;
#35347=CARTESIAN_POINT ( 'NONE',  ( -132.0000507999999968, 0.000000000000000000, 0.000000000000000000 ) ) ;
#35355=AXIS2_PLACEMENT_3D ( 'NONE', #6845, #10343, #23681 ) ;
#35361=EDGE_CURVE ( 'NONE', #31070, #2459, #7519, .T. ) ;
#35366=VECTOR ( 'NONE', #7189, 1000.000000000000000 ) ;
#35374=ORIENTED_EDGE ( 'NONE', *, *, #11897, .F. ) ;
#35375=CIRCLE ( 'NONE', #6811, 20.00000000000001066 ) ;
#35376=DIRECTION ( 'NONE',  ( 0.000000000000000000, 0.000000000000000000, -1.000000000000000000 ) ) ;
#35383=EDGE_CURVE ( 'NONE', #30536, #42073, #18258, .T. ) ;
#35387=EDGE_CURVE ( 'NONE', #26141, #26339, #11686, .T. ) ;
#35403=CIRCLE ( 'NONE', #13158, 51.99999999999999289 ) ;
#35407=CARTESIAN_POINT ( 'NONE',  ( 0.000000000000000000, 32.00046193115198179, -34.40241257139653186 ) ) ;
#35412=ORIENTED_EDGE ( 'NONE', *, *, #24000, .F. ) ;
#35418=CARTESIAN_POINT ( 'NONE',  ( 18.00000000000000355, 37.91532898920922889, 28.61088654061651937 ) ) ;
#35427=DIRECTION ( 'NONE',  ( 0.000000000000000000, 0.000000000000000000, 1.000000000000000000 ) ) ;
#35428=DIRECTION ( 'NONE',  ( 0.000000000000000000, 0.000000000000000000, -1.000000000000000000 ) ) ;
#35429=ORIENTED_EDGE ( 'NONE', *, *, #15000, .T. ) ;
#35432=DIRECTION ( 'NONE',  ( -1.000000000000000000, 0.000000000000000000, 0.000000000000000000 ) ) ;
#35470=DIRECTION ( 'NONE',  ( -1.000000000000000000, 0.000000000000000000, -0.000000000000000000 ) ) ;
#35471=EDGE_LOOP ( 'NONE', ( #30410, #29889, #643, #42227 ) ) ;
#35484=CARTESIAN_POINT ( 'NONE',  ( 9.000000000000001776, 31.08872492060014636, -41.68322423723067516 ) ) ;
#35494=ORIENTED_EDGE ( 'NONE', *, *, #24456, .T. ) ;
#35498=DIRECTION ( 'NONE',  ( 0.000000000000000000, 0.000000000000000000, -1.000000000000000000 ) ) ;
#35499=DIRECTION ( 'NONE',  ( -1.000000000000000000, -0.000000000000000000, -0.000000000000000000 ) ) ;
#35500=ADVANCED_FACE ( 'NONE', ( #32790 ), #2871, .T. ) ;
#35506=DIRECTION ( 'NONE',  ( 1.000000000000000000, -0.000000000000000000, -0.000000000000000000 ) ) ;
#35514=CYLINDRICAL_SURFACE ( 'NONE', #2930, 47.49900000000000233 ) ;
#35519=DIRECTION ( 'NONE',  ( 0.000000000000000000, 0.000000000000000000, -1.000000000000000000 ) ) ;
#35521=VERTEX_POINT ( 'NONE', #18699 ) ;
#35523=FACE_OUTER_BOUND ( 'NONE', #26747, .T. ) ;
#35524=ORIENTED_EDGE ( 'NONE', *, *, #21536, .T. ) ;
#35530=EDGE_CURVE ( 'NONE', #28999, #20186, #38688, .T. ) ;
#35536=AXIS2_PLACEMENT_3D ( 'NONE', #9248, #23030, #42605 ) ;
#35539=CARTESIAN_POINT ( 'NONE',  ( 0.000000000000000000, 17.08890430202750110, 43.76671000081951490 ) ) ;
#35545=EDGE_CURVE ( 'NONE', #4843, #41828, #40233, .T. ) ;
#35558=AXIS2_PLACEMENT_3D ( 'NONE', #39397, #9539, #22891 ) ;
#35560=EDGE_CURVE ( 'NONE', #32031, #32639, #7487, .T. ) ;
#35561=AXIS2_PLACEMENT_3D ( 'NONE', #35895, #4243, #26750 ) ;
#35563=DIRECTION ( 'NONE',  ( 0.000000000000000000, 0.000000000000000000, 1.000000000000000000 ) ) ;
#35575=DIRECTION ( 'NONE',  ( -1.000000000000000000, -0.000000000000000000, 0.000000000000000000 ) ) ;
#35586=CARTESIAN_POINT ( 'NONE',  ( 18.00000000000000355, -46.19362259308827845, -8.585149169758995669 ) ) ;
#35593=EDGE_CURVE ( 'NONE', #39812, #36216, #8220, .T. ) ;
#35604=CARTESIAN_POINT ( 'NONE',  ( 18.00000000000000355, -38.92705108641711576, -27.21837053747839263 ) ) ;
#35612=( NAMED_UNIT ( * ) PLANE_ANGLE_UNIT ( ) SI_UNIT ( $, .RADIAN. ) );
#35615=EDGE_CURVE ( 'NONE', #6740, #32276, #24991, .T. ) ;
#35616=EDGE_CURVE ( 'NONE', #20160, #38193, #17320, .T. ) ;
#35627=DIRECTION ( 'NONE',  ( -1.000000000000000000, 0.000000000000000000, 0.000000000000000000 ) ) ;
#35628=VECTOR ( 'NONE', #8180, 1000.000000000000000 ) ;
#35629=CARTESIAN_POINT ( 'NONE',  ( 18.00000000000000355, -11.46872990052412788, 45.56340405422441364 ) ) ;
#35634=VERTEX_POINT ( 'NONE', #36918 ) ;
#35636=ORIENTED_EDGE ( 'NONE', *, *, #5551, .F. ) ;
#35639=FACE_OUTER_BOUND ( 'NONE', #30162, .T. ) ;
#35645=DIRECTION ( 'NONE',  ( -1.000000000000000000, 0.000000000000000000, -0.000000000000000000 ) ) ;
#35646=CARTESIAN_POINT ( 'NONE',  ( 0.000000000000000000, 0.000000000000000000, 0.000000000000000000 ) ) ;
#35657=DIRECTION ( 'NONE',  ( 0.000000000000000000, 0.000000000000000000, -1.000000000000000000 ) ) ;
#35659=AXIS2_PLACEMENT_3D ( 'NONE', #34247, #34039, #20777 ) ;
#35662=ORIENTED_EDGE ( 'NONE', *, *, #27769, .T. ) ;
#35664=DIRECTION ( 'NONE',  ( 0.000000000000000000, 0.000000000000000000, 1.000000000000000000 ) ) ;
#35677=ORIENTED_EDGE ( 'NONE', *, *, #35883, .T. ) ;
#35683=CYLINDRICAL_SURFACE ( 'NONE', #25748, 20.00000000000000355 ) ;
#35689=ORIENTED_EDGE ( 'NONE', *, *, #24444, .F. ) ;
#35694=LINE ( 'NONE', #32659, #20796 ) ;
#35696=EDGE_LOOP ( 'NONE', ( #35319, #23242, #16903, #3349 ) ) ;
#35710=VECTOR ( 'NONE', #19795, 1000.000000000000000 ) ;
#35725=ORIENTED_EDGE ( 'NONE', *, *, #24466, .F. ) ;
#35727=FACE_OUTER_BOUND ( 'NONE', #2203, .T. ) ;
#35731=ORIENTED_EDGE ( 'NONE', *, *, #17099, .T. ) ;
#35734=DIRECTION ( 'NONE',  ( -1.000000000000000000, -0.000000000000000000, 0.000000000000000000 ) ) ;
#35739=DIRECTION ( 'NONE',  ( -1.000000000000000000, -0.000000000000000000, 0.000000000000000000 ) ) ;
#35743=AXIS2_PLACEMENT_3D ( 'NONE', #11118, #24446, #7819 ) ;
#35757=EDGE_CURVE ( 'NONE', #3682, #39427, #42354, .T. ) ;
#35759=DIRECTION ( 'NONE',  ( 0.000000000000000000, 0.000000000000000000, 1.000000000000000000 ) ) ;
#35760=FACE_OUTER_BOUND ( 'NONE', #11312, .T. ) ;
#35769=EDGE_LOOP ( 'NONE', ( #37574, #30924, #40670, #35071 ) ) ;
#35773=ORIENTED_EDGE ( 'NONE', *, *, #30811, .F. ) ;
#35776=AXIS2_PLACEMENT_3D ( 'NONE', #6597, #39751, #23233 ) ;
#35777=ORIENTED_EDGE ( 'NONE', *, *, #4486, .T. ) ;
#35782=DIRECTION ( 'NONE',  ( -1.000000000000000000, 0.000000000000000000, 0.000000000000000000 ) ) ;
#35797=EDGE_LOOP ( 'NONE', ( #23014, #38910, #26101, #14710 ) ) ;
#35800=ORIENTED_EDGE ( 'NONE', *, *, #24608, .T. ) ;
#35802=DIRECTION ( 'NONE',  ( 0.000000000000000000, -0.9510565162951500895, -0.3090169943749582204 ) ) ;
#35809=ORIENTED_EDGE ( 'NONE', *, *, #39822, .F. ) ;
#35812=LINE ( 'NONE', #9012, #29718 ) ;
#35821=CIRCLE ( 'NONE', #7278, 47.49900000000000233 ) ;
#35822=EDGE_LOOP ( 'NONE', ( #22287, #25370, #3509, #38530 ) ) ;
#35826=DIRECTION ( 'NONE',  ( 0.000000000000000000, 0.000000000000000000, -1.000000000000000000 ) ) ;
#35827=ADVANCED_FACE ( 'NONE', ( #14693 ), #11627, .T. ) ;
#35829=CARTESIAN_POINT ( 'NONE',  ( 18.00000000000000355, 32.32520163883631170, -34.09746168776002406 ) ) ;
#35837=CARTESIAN_POINT ( 'NONE',  ( 18.00000000000000355, -50.95304419620831737, 10.38206564895643957 ) ) ;
#35841=CARTESIAN_POINT ( 'NONE',  ( 18.00000000000000355, 35.11945359308110426, 38.34871548466026070 ) ) ;
#35849=EDGE_CURVE ( 'NONE', #2932, #16830, #37481, .T. ) ;
#35857=ORIENTED_EDGE ( 'NONE', *, *, #7235, .F. ) ;
#35858=FILL_AREA_STYLE_COLOUR ( '', #5087 ) ;
#35867=ADVANCED_FACE ( 'NONE', ( #22745 ), #8759, .T. ) ;
#35880=ORIENTED_EDGE ( 'NONE', *, *, #37002, .F. ) ;
#35882=CIRCLE ( 'NONE', #6615, 20.00000000000000711 ) ;
#35883=EDGE_CURVE ( 'NONE', #28679, #35634, #22212, .T. ) ;
#35884=AXIS2_PLACEMENT_3D ( 'NONE', #16495, #10356, #26720 ) ;
#35885=DIRECTION ( 'NONE',  ( 0.000000000000000000, -0.5877852522924802425, 0.8090169943749422332 ) ) ;
#35886=DIRECTION ( 'NONE',  ( 0.000000000000000000, -0.1253332335642905193, -0.9921147013144796523 ) ) ;
#35889=CARTESIAN_POINT ( 'NONE',  ( 9.000000000000001776, 5.871425383722282731, -51.66745943012276143 ) ) ;
#35891=DIRECTION ( 'NONE',  ( 0.000000000000000000, 0.000000000000000000, 1.000000000000000000 ) ) ;
#35895=CARTESIAN_POINT ( 'NONE',  ( 18.00000000000000355, 0.000000000000000000, 0.000000000000000000 ) ) ;
#35896=DIRECTION ( 'NONE',  ( -1.000000000000000000, -0.000000000000000000, 0.000000000000000000 ) ) ;
#35897=EDGE_LOOP ( 'NONE', ( #22716, #19595, #3267, #37636 ) ) ;
#35910=AXIS2_PLACEMENT_3D ( 'NONE', #30785, #14003, #27301 ) ;
#35913=CIRCLE ( 'NONE', #26880, 20.00000000000000355 ) ;
#35915=AXIS2_PLACEMENT_3D ( 'NONE', #24554, #923, #11012 ) ;
#35922=ORIENTED_EDGE ( 'NONE', *, *, #24149, .T. ) ;
#35932=DIRECTION ( 'NONE',  ( 0.000000000000000000, 0.000000000000000000, 1.000000000000000000 ) ) ;
#35933=ORIENTED_EDGE ( 'NONE', *, *, #27668, .F. ) ;
#35939=AXIS2_PLACEMENT_3D ( 'NONE', #17679, #6143, #10449 ) ;
#35941=AXIS2_PLACEMENT_3D ( 'NONE', #16598, #16357, #32705 ) ;
#35945=DIRECTION ( 'NONE',  ( -1.000000000000000000, 0.000000000000000000, 0.000000000000000000 ) ) ;
#35953=CIRCLE ( 'NONE', #35288, 51.99999999999999289 ) ;
#35957=DIRECTION ( 'NONE',  ( -1.000000000000000000, 0.000000000000000000, 0.000000000000000000 ) ) ;
#35960=EDGE_CURVE ( 'NONE', #21443, #4850, #32625, .T. ) ;
#35964=CARTESIAN_POINT ( 'NONE',  ( 18.00000000000000355, -37.91532898920899441, -28.61088654061679648 ) ) ;
#35985=VECTOR ( 'NONE', #7150, 1000.000000000000000 ) ;
#35990=EDGE_CURVE ( 'NONE', #9735, #24321, #16622, .T. ) ;
#36000=ORIENTED_EDGE ( 'NONE', *, *, #7845, .F. ) ;
#36005=ORIENTED_EDGE ( 'NONE', *, *, #9278, .F. ) ;
#36006=AXIS2_PLACEMENT_3D ( 'NONE', #5260, #18627, #34934 ) ;
#36012=CARTESIAN_POINT ( 'NONE',  ( 18.00000000000000355, 44.25018368420781201, -27.31155879685132959 ) ) ;
#36017=CIRCLE ( 'NONE', #12979, 20.00000000000000355 ) ;
#36019=LINE ( 'NONE', #37264, #13681 ) ;
#36029=CARTESIAN_POINT ( 'NONE',  ( 18.00000000000000355, 0.000000000000000000, 0.000000000000000000 ) ) ;
#36031=DIRECTION ( 'NONE',  ( -1.000000000000000000, -0.000000000000000000, 0.000000000000000000 ) ) ;
#36034=DIRECTION ( 'NONE',  ( -1.000000000000000000, -0.000000000000000000, -0.000000000000000000 ) ) ;
#36041=AXIS2_PLACEMENT_3D ( 'NONE', #30455, #4017, #34139 ) ;
#36054=EDGE_CURVE ( 'NONE', #34436, #23020, #31906, .T. ) ;
#36065=ORIENTED_EDGE ( 'NONE', *, *, #7276, .T. ) ;
#36067=ORIENTED_EDGE ( 'NONE', *, *, #34347, .T. ) ;
#36069=AXIS2_PLACEMENT_3D ( 'NONE', #37131, #19956, #33869 ) ;
#36070=AXIS2_PLACEMENT_3D ( 'NONE', #35142, #22314, #35563 ) ;
#36075=ORIENTED_EDGE ( 'NONE', *, *, #22986, .T. ) ;
#36078=CIRCLE ( 'NONE', #538, 47.49900000000000233 ) ;
#36079=DIRECTION ( 'NONE',  ( -1.000000000000000000, -0.000000000000000000, 0.000000000000000000 ) ) ;
#36082=ORIENTED_EDGE ( 'NONE', *, *, #20368, .F. ) ;
#36090=DIRECTION ( 'NONE',  ( -1.000000000000000000, 0.000000000000000000, -0.000000000000000000 ) ) ;
#36097=CARTESIAN_POINT ( 'NONE',  ( 9.000000000000001776, -49.25004636492400323, 16.68630974939742018 ) ) ;
#36105=ORIENTED_EDGE ( 'NONE', *, *, #35083, .F. ) ;
#36106=FACE_OUTER_BOUND ( 'NONE', #30028, .T. ) ;
#36107=EDGE_LOOP ( 'NONE', ( #13910, #19941, #19054, #36737 ) ) ;
#36109=VECTOR ( 'NONE', #5947, 1000.000000000000000 ) ;
#36112=DIRECTION ( 'NONE',  ( 0.000000000000000000, 0.000000000000000000, 1.000000000000000000 ) ) ;
#36116=DIRECTION ( 'NONE',  ( 0.000000000000000000, 0.9980267284282713369, 0.06279051952931692659 ) ) ;
#36122=DIRECTION ( 'NONE',  ( -1.000000000000000000, -0.000000000000000000, -0.000000000000000000 ) ) ;
#36126=CARTESIAN_POINT ( 'NONE',  ( 18.00000000000000355, 30.03615769709791650, -42.44795908868957923 ) ) ;
#36132=CARTESIAN_POINT ( 'NONE',  ( 18.00000000000000355, 51.93417535146740960, 2.615612846549358217 ) ) ;
#36152=CARTESIAN_POINT ( 'NONE',  ( 0.000000000000000000, 0.000000000000000000, 0.000000000000000000 ) ) ;
#36156=CIRCLE ( 'NONE', #38256, 20.00000000000000711 ) ;
#36157=EDGE_CURVE ( 'NONE', #40496, #27281, #3026, .T. ) ;
#36165=DIRECTION ( 'NONE',  ( -1.000000000000000000, 0.000000000000000000, -0.000000000000000000 ) ) ;
#36168=LINE ( 'NONE', #19847, #31273 ) ;
#36175=DIRECTION ( 'NONE',  ( 0.000000000000000000, -0.8443279255020087470, -0.5358267949790064266 ) ) ;
#36180=DIRECTION ( 'NONE',  ( -1.000000000000000000, 0.000000000000000000, 0.000000000000000000 ) ) ;
#36182=LINE ( 'NONE', #2996, #7743 ) ;
#36183=ORIENTED_EDGE ( 'NONE', *, *, #3884, .F. ) ;
#36187=EDGE_CURVE ( 'NONE', #25951, #40496, #32658, .T. ) ;
#36193=CIRCLE ( 'NONE', #27067, 20.00000000000000000 ) ;
#36207=ORIENTED_EDGE ( 'NONE', *, *, #32703, .T. ) ;
#36210=AXIS2_PLACEMENT_3D ( 'NONE', #26467, #17482, #15 ) ;
#36214=CARTESIAN_POINT ( 'NONE',  ( 0.000000000000000000, 0.000000000000000000, 0.000000000000000000 ) ) ;
#36215=DIRECTION ( 'NONE',  ( -1.000000000000000000, 0.000000000000000000, -0.000000000000000000 ) ) ;
#36216=VERTEX_POINT ( 'NONE', #21434 ) ;
#36229=CARTESIAN_POINT ( 'NONE',  ( 18.00000000000000355, 9.744342220503391161, 46.48873837489801275 ) ) ;
#36233=VECTOR ( 'NONE', #13472, 1000.000000000000000 ) ;
#36237=AXIS2_PLACEMENT_3D ( 'NONE', #15664, #11307, #34850 ) ;
#36251=EDGE_CURVE ( 'NONE', #25329, #16, #6174, .T. ) ;
#36254=CARTESIAN_POINT ( 'NONE',  ( 18.00000000000000355, -22.82995208772716467, 41.06517797613655318 ) ) ;
#36272=ORIENTED_EDGE ( 'NONE', *, *, #10735, .F. ) ;
#36282=VERTEX_POINT ( 'NONE', #14645 ) ;
#36287=FACE_OUTER_BOUND ( 'NONE', #20170, .T. ) ;
#36291=ORIENTED_EDGE ( 'NONE', *, *, #37350, .F. ) ;
#36296=DIRECTION ( 'NONE',  ( 1.000000000000000000, 0.000000000000000000, 0.000000000000000000 ) ) ;
#36297=CARTESIAN_POINT ( 'NONE',  ( 0.000000000000000000, 30.03615769709734451, 42.44795908868999135 ) ) ;
#36319=VERTEX_POINT ( 'NONE', #14858 ) ;
#36331=ORIENTED_EDGE ( 'NONE', *, *, #28347, .T. ) ;
#36334=CARTESIAN_POINT ( 'NONE',  ( 0.000000000000000000, -6.109652351741465814, -46.58570277113515345 ) ) ;
#36336=DIRECTION ( 'NONE',  ( -1.000000000000000000, 0.000000000000000000, 0.000000000000000000 ) ) ;
#36353=CARTESIAN_POINT ( 'NONE',  ( 18.00000000000000355, -11.90021268425586953, 45.45261810511210143 ) ) ;
#36357=CYLINDRICAL_SURFACE ( 'NONE', #41494, 20.00000000000000355 ) ;
#36358=ORIENTED_EDGE ( 'NONE', *, *, #7350, .F. ) ;
#36362=ADVANCED_FACE ( 'NONE', ( #13991 ), #7418, .T. ) ;
#36367=CARTESIAN_POINT ( 'NONE',  ( 18.00000000000000355, 12.30077720129167318, -50.52416135122068397 ) ) ;
#36377=CARTESIAN_POINT ( 'NONE',  ( 18.00000000000000355, -45.78515115856033901, -12.64416602183713856 ) ) ;
#36378=AXIS2_PLACEMENT_3D ( 'NONE', #27756, #7649, #41882 ) ;
#36379=VERTEX_POINT ( 'NONE', #38378 ) ;
#36382=CARTESIAN_POINT ( 'NONE',  ( 18.00000000000000355, 0.000000000000000000, 0.000000000000000000 ) ) ;
#36385=CARTESIAN_POINT ( 'NONE',  ( 0.000000000000000000, -0.6505223195679212811, -51.99593080916758936 ) ) ;
#36391=ORIENTED_EDGE ( 'NONE', *, *, #43102, .F. ) ;
#36433=CARTESIAN_POINT ( 'NONE',  ( 0.000000000000000000, -20.99948489194393275, -42.60488980472802467 ) ) ;
#36452=CARTESIAN_POINT ( 'NONE',  ( 9.000000000000001776, -7.162210897275388177, -51.50439529848834042 ) ) ;
#36460=ORIENTED_EDGE ( 'NONE', *, *, #1853, .T. ) ;
#36462=DIRECTION ( 'NONE',  ( -1.000000000000000000, -0.000000000000000000, -0.000000000000000000 ) ) ;
#36468=CARTESIAN_POINT ( 'NONE',  ( 18.00000000000000355, 0.000000000000000000, 0.000000000000000000 ) ) ;
#36471=DIRECTION ( 'NONE',  ( -1.000000000000000000, 0.000000000000000000, -0.000000000000000000 ) ) ;
#36472=VERTEX_POINT ( 'NONE', #18367 ) ;
#36473=DIRECTION ( 'NONE',  ( -1.000000000000000000, 0.000000000000000000, 0.000000000000000000 ) ) ;
#36494=CARTESIAN_POINT ( 'NONE',  ( 9.000000000000001776, -46.77034588191288123, -22.72740077717278595 ) ) ;
#36495=DIRECTION ( 'NONE',  ( 0.000000000000000000, -0.3681245526846654847, -0.9297764858882564543 ) ) ;
#36496=EDGE_CURVE ( 'NONE', #27343, #14260, #36156, .T. ) ;
#36505=CARTESIAN_POINT ( 'NONE',  ( 18.00000000000000355, -41.20225022064653331, 23.63323037071389621 ) ) ;
#36510=VECTOR ( 'NONE', #3817, 1000.000000000000000 ) ;
#36513=AXIS2_PLACEMENT_3D ( 'NONE', #4283, #18307, #10862 ) ;
#36517=DIRECTION ( 'NONE',  ( 0.000000000000000000, 0.3681245526846719240, 0.9297764858882537897 ) ) ;
#36523=CARTESIAN_POINT ( 'NONE',  ( 18.00000000000000355, 0.000000000000000000, 0.000000000000000000 ) ) ;
#36530=CIRCLE ( 'NONE', #14976, 52.00000000000000000 ) ;
#36533=AXIS2_PLACEMENT_3D ( 'NONE', #30968, #1284, #20766 ) ;
#36537=DIRECTION ( 'NONE',  ( 0.000000000000000000, 0.000000000000000000, 1.000000000000000000 ) ) ;
#36550=ORIENTED_EDGE ( 'NONE', *, *, #19494, .T. ) ;
#36554=FACE_OUTER_BOUND ( 'NONE', #26854, .T. ) ;
#36557=FACE_OUTER_BOUND ( 'NONE', #32132, .T. ) ;
#36561=CIRCLE ( 'NONE', #8709, 47.49900000000000233 ) ;
#36562=EDGE_CURVE ( 'NONE', #14260, #15934, #23282, .T. ) ;
#36569=VECTOR ( 'NONE', #14614, 1000.000000000000000 ) ;
#36571=ORIENTED_EDGE ( 'NONE', *, *, #35593, .T. ) ;
#36578=ORIENTED_EDGE ( 'NONE', *, *, #17656, .F. ) ;
#36581=DIRECTION ( 'NONE',  ( 0.000000000000000000, -0.9980267284282722251, 0.06279051952930256308 ) ) ;
#36583=VERTEX_POINT ( 'NONE', #10378 ) ;
#36585=ORIENTED_EDGE ( 'NONE', *, *, #20312, .F. ) ;
#36587=ADVANCED_FACE ( 'NONE', ( #7300 ), #3373, .T. ) ;
#36589=CARTESIAN_POINT ( 'NONE',  ( 18.00000000000000355, -41.20225022064620646, -23.63323037071445043 ) ) ;
#36593=CARTESIAN_POINT ( 'NONE',  ( 0.000000000000000000, 24.47917365150008706, -45.87777302070908547 ) ) ;
#36594=EDGE_CURVE ( 'NONE', #7115, #501, #4815, .T. ) ;
#36610=ORIENTED_EDGE ( 'NONE', *, *, #11590, .F. ) ;
#36615=DIRECTION ( 'NONE',  ( 0.000000000000000000, 0.000000000000000000, 1.000000000000000000 ) ) ;
#36616=CARTESIAN_POINT ( 'NONE',  ( 18.00000000000000355, 0.000000000000000000, 0.000000000000000000 ) ) ;
#36630=DIRECTION ( 'NONE',  ( -1.000000000000000000, 0.000000000000000000, 0.000000000000000000 ) ) ;
#36634=ORIENTED_EDGE ( 'NONE', *, *, #3683, .F. ) ;
#36640=DIRECTION ( 'NONE',  ( 0.000000000000000000, 0.000000000000000000, 1.000000000000000000 ) ) ;
#36646=EDGE_LOOP ( 'NONE', ( #28477, #40252, #36708, #32312 ) ) ;
#36652=ORIENTED_EDGE ( 'NONE', *, *, #38876, .F. ) ;
#36665=DIRECTION ( 'NONE',  ( -1.000000000000000000, -0.000000000000000000, -0.000000000000000000 ) ) ;
#36669=EDGE_CURVE ( 'NONE', #32336, #40198, #34086, .T. ) ;
#36685=AXIS2_PLACEMENT_3D ( 'NONE', #10860, #6918, #37237 ) ;
#36686=DIRECTION ( 'NONE',  ( 0.000000000000000000, 0.9980267284282712259, 0.06279051952931682945 ) ) ;
#36688=ORIENTED_EDGE ( 'NONE', *, *, #20310, .F. ) ;
#36697=EDGE_CURVE ( 'NONE', #1103, #640, #27129, .T. ) ;
#36699=CARTESIAN_POINT ( 'NONE',  ( 0.000000000000000000, -27.43636312076294814, -38.14186064215179073 ) ) ;
#36701=EDGE_CURVE ( 'NONE', #4217, #4058, #8303, .T. ) ;
#36703=EDGE_LOOP ( 'NONE', ( #9011, #33736, #3702, #22430 ) ) ;
#36708=ORIENTED_EDGE ( 'NONE', *, *, #31235, .T. ) ;
#36710=ORIENTED_EDGE ( 'NONE', *, *, #41082, .F. ) ;
#36714=DIRECTION ( 'NONE',  ( -1.000000000000000000, 0.000000000000000000, 0.000000000000000000 ) ) ;
#36716=ORIENTED_EDGE ( 'NONE', *, *, #10010, .T. ) ;
#36717=CARTESIAN_POINT ( 'NONE',  ( 18.00000000000000355, -0.6505223195679212811, -51.99593080916758936 ) ) ;
#36728=CIRCLE ( 'NONE', #24234, 20.00000000000000355 ) ;
#36731=CIRCLE ( 'NONE', #36041, 51.99999999999999289 ) ;
#36737=ORIENTED_EDGE ( 'NONE', *, *, #38344, .T. ) ;
#36743=CARTESIAN_POINT ( 'NONE',  ( 18.00000000000000355, -44.61570720899084819, -14.73072383765613047 ) ) ;
#36747=VERTEX_POINT ( 'NONE', #11693 ) ;
#36766=FACE_OUTER_BOUND ( 'NONE', #11275, .T. ) ;
#36769=CARTESIAN_POINT ( 'NONE',  ( 18.00000000000000355, -37.91532898920940653, 28.61088654061626357 ) ) ;
#36771=ORIENTED_EDGE ( 'NONE', *, *, #8955, .T. ) ;
#36775=CARTESIAN_POINT ( 'NONE',  ( 9.000000000000001776, 51.93417535146740960, -2.615612846549368431 ) ) ;
#36780=DIRECTION ( 'NONE',  ( -1.000000000000000000, -0.000000000000000000, 0.000000000000000000 ) ) ;
#36783=DIRECTION ( 'NONE',  ( 1.000000000000000000, 0.000000000000000000, 0.000000000000000000 ) ) ;
#36794=DIRECTION ( 'NONE',  ( -1.000000000000000000, -0.000000000000000000, 0.000000000000000000 ) ) ;
#36804=DIRECTION ( 'NONE',  ( 0.000000000000000000, -0.5877852522924802425, 0.8090169943749422332 ) ) ;
#36805=EDGE_LOOP ( 'NONE', ( #1119, #24745, #3486, #14950 ) ) ;
#36818=VERTEX_POINT ( 'NONE', #12117 ) ;
#36821=LINE ( 'NONE', #6930, #15551 ) ;
#36825=CIRCLE ( 'NONE', #11797, 20.00000000000000355 ) ;
#36826=EDGE_CURVE ( 'NONE', #35293, #25440, #38287, .T. ) ;
#36833=DIRECTION ( 'NONE',  ( 0.000000000000000000, 0.000000000000000000, 1.000000000000000000 ) ) ;
#36864=VERTEX_POINT ( 'NONE', #32166 ) ;
#36873=ORIENTED_EDGE ( 'NONE', *, *, #3740, .F. ) ;
#36878=VERTEX_POINT ( 'NONE', #35837 ) ;
#36885=AXIS2_PLACEMENT_3D ( 'NONE', #20773, #628, #34452 ) ;
#36887=CARTESIAN_POINT ( 'NONE',  ( 18.00000000000000355, 25.61928775981106554, -45.25098998563449726 ) ) ;
#36901=CARTESIAN_POINT ( 'NONE',  ( 0.000000000000000000, 0.000000000000000000, 0.000000000000000000 ) ) ;
#36916=CARTESIAN_POINT ( 'NONE',  ( 0.000000000000000000, 44.61570720899096898, -14.73072383765582671 ) ) ;
#36917=EDGE_LOOP ( 'NONE', ( #13557, #23204 ) ) ;
#36918=CARTESIAN_POINT ( 'NONE',  ( 0.000000000000000000, 46.77034588191303754, 22.72740077717245910 ) ) ;
#36921=CYLINDRICAL_SURFACE ( 'NONE', #16564, 20.00000000000000355 ) ;
#36922=ORIENTED_EDGE ( 'NONE', *, *, #15042, .T. ) ;
#36926=DIRECTION ( 'NONE',  ( -1.000000000000000000, -0.000000000000000000, -0.000000000000000000 ) ) ;
#36941=AXIS2_PLACEMENT_3D ( 'NONE', #28149, #7838, #21196 ) ;
#36942=FACE_OUTER_BOUND ( 'NONE', #8173, .T. ) ;
#36948=EDGE_CURVE ( 'NONE', #26032, #41807, #11848, .T. ) ;
#36967=CIRCLE ( 'NONE', #6322, 20.00000000000001066 ) ;
#36970=AXIS2_PLACEMENT_3D ( 'NONE', #2766, #2338, #2565 ) ;
#36972=ORIENTED_EDGE ( 'NONE', *, *, #41992, .T. ) ;
#36992=FACE_OUTER_BOUND ( 'NONE', #22258, .T. ) ;
#36998=DIRECTION ( 'NONE',  ( 0.000000000000000000, 0.7705132427757903635, -0.6374239897486881912 ) ) ;
#37000=AXIS2_PLACEMENT_3D ( 'NONE', #31917, #1997, #5913 ) ;
#37002=EDGE_CURVE ( 'NONE', #34548, #39812, #34807, .T. ) ;
#37004=ORIENTED_EDGE ( 'NONE', *, *, #22702, .F. ) ;
#37014=CARTESIAN_POINT ( 'NONE',  ( 0.000000000000000000, -27.79676263918213763, 37.88001506494759241 ) ) ;
#37021=CARTESIAN_POINT ( 'NONE',  ( 9.000000000000001776, 51.93417535146740960, 2.615612846549358217 ) ) ;
#37043=ORIENTED_EDGE ( 'NONE', *, *, #20695, .T. ) ;
#37047=CARTESIAN_POINT ( 'NONE',  ( 18.00000000000000355, 0.000000000000000000, 0.000000000000000000 ) ) ;
#37054=FACE_OUTER_BOUND ( 'NONE', #28566, .T. ) ;
#37060=EDGE_CURVE ( 'NONE', #3682, #9021, #21697, .T. ) ;
#37062=CIRCLE ( 'NONE', #41945, 20.00000000000000355 ) ;
#37064=AXIS2_PLACEMENT_3D ( 'NONE', #19273, #12920, #41925 ) ;
#37065=VECTOR ( 'NONE', #37124, 1000.000000000000000 ) ;
#37076=DIRECTION ( 'NONE',  ( -1.000000000000000000, 0.000000000000000000, -0.000000000000000000 ) ) ;
#37085=VERTEX_POINT ( 'NONE', #11412 ) ;
#37093=CARTESIAN_POINT ( 'NONE',  ( 18.00000000000000355, 36.06787431788731624, -37.45808914225448660 ) ) ;
#37098=EDGE_LOOP ( 'NONE', ( #23289, #35933, #24325, #14416 ) ) ;
#37101=DIRECTION ( 'NONE',  ( -1.000000000000000000, 0.000000000000000000, -0.000000000000000000 ) ) ;
#37104=EDGE_CURVE ( 'NONE', #24364, #34048, #43134, .T. ) ;
#37109=DIRECTION ( 'NONE',  ( -1.000000000000000000, -0.000000000000000000, 0.000000000000000000 ) ) ;
#37111=ORIENTED_EDGE ( 'NONE', *, *, #9173, .T. ) ;
#37113=DIRECTION ( 'NONE',  ( -1.000000000000000000, 0.000000000000000000, 0.000000000000000000 ) ) ;
#37124=DIRECTION ( 'NONE',  ( 1.000000000000000000, -0.000000000000000000, 0.000000000000000000 ) ) ;
#37127=ORIENTED_EDGE ( 'NONE', *, *, #13539, .F. ) ;
#37131=CARTESIAN_POINT ( 'NONE',  ( 0.000000000000000000, 0.000000000000000000, 0.000000000000000000 ) ) ;
#37135=VERTEX_POINT ( 'NONE', #38225 ) ;
#37146=ORIENTED_EDGE ( 'NONE', *, *, #25524, .F. ) ;
#37161=CARTESIAN_POINT ( 'NONE',  ( 18.00000000000000355, 46.90537658765334328, -2.727856614653797251 ) ) ;
#37179=DIRECTION ( 'NONE',  ( 0.000000000000000000, -0.1253332335642905471, -0.9921147013144795412 ) ) ;
#37184=VERTEX_POINT ( 'NONE', #11637 ) ;
#37198=ORIENTED_EDGE ( 'NONE', *, *, #27345, .F. ) ;
#37202=AXIS2_PLACEMENT_3D ( 'NONE', #522, #37395, #68 ) ;
#37204=AXIS2_PLACEMENT_3D ( 'NONE', #42310, #19877, #42520 ) ;
#37207=CARTESIAN_POINT ( 'NONE',  ( 0.000000000000000000, 6.109652351742432153, -46.58570277113501845 ) ) ;
#37215=ORIENTED_EDGE ( 'NONE', *, *, #28737, .F. ) ;
#37219=ADVANCED_FACE ( 'NONE', ( #9398 ), #42547, .T. ) ;
#37227=CARTESIAN_POINT ( 'NONE',  ( 18.00000000000000355, 19.44205635905542096, 43.33776004284615624 ) ) ;
#37229=VECTOR ( 'NONE', #12231, 1000.000000000000000 ) ;
#37230=ORIENTED_EDGE ( 'NONE', *, *, #21172, .F. ) ;
#37237=DIRECTION ( 'NONE',  ( 0.000000000000000000, -0.9510565162951500895, -0.3090169943749581649 ) ) ;
#37239=CARTESIAN_POINT ( 'NONE',  ( 18.00000000000000355, 35.20873326984126805, -31.88259874183992792 ) ) ;
#37240=VERTEX_POINT ( 'NONE', #26004 ) ;
#37241=CYLINDRICAL_SURFACE ( 'NONE', #3504, 7.500000000000000000 ) ;
#37256=VERTEX_POINT ( 'NONE', #8982 ) ;
#37264=CARTESIAN_POINT ( 'NONE',  ( 9.000000000000001776, -24.47917365149914559, -45.87777302070959706 ) ) ;
#37274=AXIS2_PLACEMENT_3D ( 'NONE', #41808, #22862, #35886 ) ;
#37276=VERTEX_POINT ( 'NONE', #38642 ) ;
#37280=CARTESIAN_POINT ( 'NONE',  ( 0.000000000000000000, 0.000000000000000000, 0.000000000000000000 ) ) ;
#37283=AXIS2_PLACEMENT_3D ( 'NONE', #17186, #17626, #30891 ) ;
#37288=DIRECTION ( 'NONE',  ( 1.000000000000000000, -0.000000000000000000, -0.000000000000000000 ) ) ;
#37289=CIRCLE ( 'NONE', #9454, 20.00000000000001066 ) ;
#37298=AXIS2_PLACEMENT_3D ( 'NONE', #6682, #20045, #33081 ) ;
#37307=ADVANCED_FACE ( 'NONE', ( #5279 ), #28852, .T. ) ;
#37309=ORIENTED_EDGE ( 'NONE', *, *, #16441, .T. ) ;
#37329=CARTESIAN_POINT ( 'NONE',  ( 18.00000000000000355, 42.03146605346785947, 22.12489237027331512 ) ) ;
#37340=LINE ( 'NONE', #33043, #20656 ) ;
#37341=FACE_OUTER_BOUND ( 'NONE', #8498, .T. ) ;
#37342=ORIENTED_EDGE ( 'NONE', *, *, #35530, .T. ) ;
#37345=CARTESIAN_POINT ( 'NONE',  ( 18.00000000000000355, -45.78515115856033901, -12.64416602183713856 ) ) ;
#37349=DIRECTION ( 'NONE',  ( -1.000000000000000000, 0.000000000000000000, 0.000000000000000000 ) ) ;
#37350=EDGE_CURVE ( 'NONE', #20569, #40464, #19263, .T. ) ;
#37376=DIRECTION ( 'NONE',  ( -1.000000000000000000, 0.000000000000000000, -0.000000000000000000 ) ) ;
#37379=DIRECTION ( 'NONE',  ( 0.000000000000000000, 0.000000000000000000, 1.000000000000000000 ) ) ;
#37389=AXIS2_PLACEMENT_3D ( 'NONE', #29470, #12889, #19037 ) ;
#37395=DIRECTION ( 'NONE',  ( 1.000000000000000000, 0.000000000000000000, 0.000000000000000000 ) ) ;
#37397=LINE ( 'NONE', #21309, #11742 ) ;
#37414=CIRCLE ( 'NONE', #11699, 52.00000000000000000 ) ;
#37418=ORIENTED_EDGE ( 'NONE', *, *, #38772, .T. ) ;
#37423=AXIS2_PLACEMENT_3D ( 'NONE', #23279, #13451, #36116 ) ;
#37426=CIRCLE ( 'NONE', #14483, 20.00000000000000711 ) ;
#37427=DIRECTION ( 'NONE',  ( -1.000000000000000000, -0.000000000000000000, -0.000000000000000000 ) ) ;
#37429=CARTESIAN_POINT ( 'NONE',  ( 18.00000000000000355, 0.000000000000000000, 0.000000000000000000 ) ) ;
#37433=VECTOR ( 'NONE', #27152, 1000.000000000000000 ) ;
#37441=EDGE_CURVE ( 'NONE', #13305, #15791, #32041, .T. ) ;
#37443=DIRECTION ( 'NONE',  ( -1.000000000000000000, -0.000000000000000000, -0.000000000000000000 ) ) ;
#37450=CIRCLE ( 'NONE', #18022, 51.99999999999999289 ) ;
#37455=ORIENTED_EDGE ( 'NONE', *, *, #15965, .T. ) ;
#37456=AXIS2_PLACEMENT_3D ( 'NONE', #25019, #2035, #5324 ) ;
#37461=VERTEX_POINT ( 'NONE', #10044 ) ;
#37471=CARTESIAN_POINT ( 'NONE',  ( 0.000000000000000000, 0.000000000000000000, 0.000000000000000000 ) ) ;
#37476=CARTESIAN_POINT ( 'NONE',  ( 18.00000000000000355, 34.03046037009255542, 33.13733193845817482 ) ) ;
#37477=ORIENTED_EDGE ( 'NONE', *, *, #29006, .F. ) ;
#37481=CIRCLE ( 'NONE', #19429, 20.00000000000000711 ) ;
#37482=CARTESIAN_POINT ( 'NONE',  ( 18.00000000000000355, 45.78515115856060191, -12.64416602183617577 ) ) ;
#37485=VECTOR ( 'NONE', #28262, 1000.000000000000000 ) ;
#37492=CYLINDRICAL_SURFACE ( 'NONE', #39166, 51.99999999999999289 ) ;
#37520=DIRECTION ( 'NONE',  ( -1.000000000000000000, 0.000000000000000000, -0.000000000000000000 ) ) ;
#37521=CIRCLE ( 'NONE', #16634, 47.49900000000000233 ) ;
#37534=DIRECTION ( 'NONE',  ( 1.000000000000000000, 0.000000000000000000, 0.000000000000000000 ) ) ;
#37537=CARTESIAN_POINT ( 'NONE',  ( 18.00000000000000355, -44.75336757549769118, -14.30704879393654316 ) ) ;
#37547=DIRECTION ( 'NONE',  ( -1.000000000000000000, -0.000000000000000000, -0.000000000000000000 ) ) ;
#37549=DIRECTION ( 'NONE',  ( 0.000000000000000000, 0.9822872507286892763, -0.1873813145857214368 ) ) ;
#37553=EDGE_CURVE ( 'NONE', #9021, #10641, #4878, .T. ) ;
#37554=DIRECTION ( 'NONE',  ( 0.000000000000000000, 0.000000000000000000, 1.000000000000000000 ) ) ;
#37574=ORIENTED_EDGE ( 'NONE', *, *, #29147, .F. ) ;
#37576=EDGE_LOOP ( 'NONE', ( #29832, #15854, #30934, #29048 ) ) ;
#37582=CARTESIAN_POINT ( 'NONE',  ( 18.00000000000000355, 19.74581912682842244, 48.10512059033398913 ) ) ;
#37584=EDGE_LOOP ( 'NONE', ( #2468, #24137, #19217, #5121, #41855, #42471, #42257, #28275, #42466, #23710, #40876, #7083, #7744, #17279, #17709, #5552, #28036, #10657, #27762, #12701, #3121, #6722, #32475, #4783, #33090, #41601, #30547, #6300, #39835, #3587, #23996, #42786, #42661, #8073, #3843, #2330, #41005, #14919, #1014, #10789, #32161, #34885, #36358, #23949, #42916, #14565, #525, #42668, #21972, #16970, #14697, #35809, #34739, #11643, #1560, #17188, #28699, #17410, #1882, #35157, #37669, #17454, #818, #33648, #39781, #33101, #12362, #33721, #12738, #18463, #33276, #42215, #24408, #701, #9239, #30524, #36873, #13388, #24372, #31943, #24163, #4196, #4212, #8662, #33971, #25236, #15519, #8643, #900, #10467, #42191, #26703, #24188, #28705, #34043, #2220, #6096, #29486, #4276, #37777, #35880, #22357, #3952, #36082, #14093, #23598, #8077, #16908, #34081, #5759, #39807, #15731, #12047, #18024, #34097, #4405, #27465, #19534, #42744, #41395, #13895, #16906, #17347, #10724, #41722, #4873, #21592, #12035, #34041, #32151, #31854, #39726, #6361, #33674, #10426, #20410, #9798, #4838, #38838, #22993, #15868, #32403, #3680, #15715, #30090, #38108, #41906, #3899, #41220, #25836, #12296, #31972, #29701, #18593, #23624, #6933, #34079, #41445, #33652, #17588, #14643, #28758, #16498, #43147, #11636, #20628, #6377, #40103, #6350, #11404, #29658, #36000, #11028, #9524, #2069, #5957, #31345, #4550, #15481, #30453, #41370, #11280, #5528, #3706, #20329, #11376, #12113, #18143, #24945, #28350, #21755, #18798, #16513, #25858, #28710, #8684, #9762, #40356, #7251, #2611, #30768, #27722, #26814 ) ) ;
#37590=DIRECTION ( 'NONE',  ( -1.000000000000000000, -0.000000000000000000, 0.000000000000000000 ) ) ;
#37591=CARTESIAN_POINT ( 'NONE',  ( 18.00000000000000355, 44.47301969247467923, -16.68249143361863318 ) ) ;
#37592=EDGE_LOOP ( 'NONE', ( #8787, #30729, #38034, #24077 ) ) ;
#37609=EDGE_LOOP ( 'NONE', ( #29079, #34862, #19011, #3379 ) ) ;
#37612=DIRECTION ( 'NONE',  ( -1.000000000000000000, 0.000000000000000000, 0.000000000000000000 ) ) ;
#37625=AXIS2_PLACEMENT_3D ( 'NONE', #11285, #37660, #35038 ) ;
#37627=AXIS2_PLACEMENT_3D ( 'NONE', #33354, #19859, #33559 ) ;
#37629=CIRCLE ( 'NONE', #4203, 20.00000000000000711 ) ;
#37635=DIRECTION ( 'NONE',  ( -1.000000000000000000, 0.000000000000000000, 0.000000000000000000 ) ) ;
#37636=ORIENTED_EDGE ( 'NONE', *, *, #38408, .T. ) ;
#37640=CYLINDRICAL_SURFACE ( 'NONE', #19750, 20.00000000000000355 ) ;
#37642=AXIS2_PLACEMENT_3D ( 'NONE', #5031, #39032, #21875 ) ;
#37644=DIRECTION ( 'NONE',  ( -1.000000000000000000, 0.000000000000000000, 0.000000000000000000 ) ) ;
#37645=ORIENTED_EDGE ( 'NONE', *, *, #32402, .F. ) ;
#37652=AXIS2_PLACEMENT_3D ( 'NONE', #6663, #33065, #32855 ) ;
#37655=AXIS2_PLACEMENT_3D ( 'NONE', #22709, #35957, #25555 ) ;
#37656=CARTESIAN_POINT ( 'NONE',  ( 0.000000000000000000, 40.47821179127761582, -32.64221760512715775 ) ) ;
#37659=VECTOR ( 'NONE', #34189, 1000.000000000000000 ) ;
#37660=DIRECTION ( 'NONE',  ( -1.000000000000000000, -0.000000000000000000, 0.000000000000000000 ) ) ;
#37663=DIRECTION ( 'NONE',  ( -1.000000000000000000, 0.000000000000000000, 0.000000000000000000 ) ) ;
#37665=CARTESIAN_POINT ( 'NONE',  ( 0.000000000000000000, -17.50309955389580452, -43.60271849949383949 ) ) ;
#37669=ORIENTED_EDGE ( 'NONE', *, *, #23798, .F. ) ;
#37670=DIRECTION ( 'NONE',  ( -1.000000000000000000, 0.000000000000000000, 0.000000000000000000 ) ) ;
#37689=CARTESIAN_POINT ( 'NONE',  ( 0.000000000000000000, 37.91532898920961969, -28.61088654061597936 ) ) ;
#37690=AXIS2_PLACEMENT_3D ( 'NONE', #741, #20660, #13235 ) ;
#37691=FACE_OUTER_BOUND ( 'NONE', #1238, .T. ) ;
#37710=AXIS2_PLACEMENT_3D ( 'NONE', #22762, #42126, #16202 ) ;
#37711=DIRECTION ( 'NONE',  ( -1.000000000000000000, -0.000000000000000000, 0.000000000000000000 ) ) ;
#37713=CARTESIAN_POINT ( 'NONE',  ( 0.000000000000000000, 0.000000000000000000, 0.000000000000000000 ) ) ;
#37717=EDGE_LOOP ( 'NONE', ( #27616, #24467, #32521, #16977 ) ) ;
#37724=DIRECTION ( 'NONE',  ( 0.000000000000000000, 0.000000000000000000, 1.000000000000000000 ) ) ;
#37725=AXIS2_PLACEMENT_3D ( 'NONE', #38925, #36079, #19333 ) ;
#37729=EDGE_LOOP ( 'NONE', ( #5976, #15172, #3434, #19911 ) ) ;
#37764=EDGE_CURVE ( 'NONE', #27281, #37276, #32766, .T. ) ;
#37766=CARTESIAN_POINT ( 'NONE',  ( 0.000000000000000000, 0.000000000000000000, 0.000000000000000000 ) ) ;
#37767=EDGE_CURVE ( 'NONE', #8604, #33622, #34867, .T. ) ;
#37769=FACE_OUTER_BOUND ( 'NONE', #27804, .T. ) ;
#37776=VECTOR ( 'NONE', #17100, 1000.000000000000000 ) ;
#37777=ORIENTED_EDGE ( 'NONE', *, *, #35593, .F. ) ;
#37791=EDGE_CURVE ( 'NONE', #25035, #235, #8395, .T. ) ;
#37806=ORIENTED_EDGE ( 'NONE', *, *, #16249, .T. ) ;
#37811=CIRCLE ( 'NONE', #23901, 20.00000000000000711 ) ;
#37829=ORIENTED_EDGE ( 'NONE', *, *, #16329, .F. ) ;
#37838=EDGE_CURVE ( 'NONE', #12073, #16328, #13989, .T. ) ;
#37839=CARTESIAN_POINT ( 'NONE',  ( 18.00000000000000355, 0.000000000000000000, 0.000000000000000000 ) ) ;
#37847=ORIENTED_EDGE ( 'NONE', *, *, #33215, .T. ) ;
#37855=EDGE_CURVE ( 'NONE', #22661, #19113, #38349, .T. ) ;
#37856=CIRCLE ( 'NONE', #22584, 20.00000000000000355 ) ;
#37858=FACE_OUTER_BOUND ( 'NONE', #17788, .T. ) ;
#37859=VERTEX_POINT ( 'NONE', #35330 ) ;
#37861=CARTESIAN_POINT ( 'NONE',  ( 9.000000000000001776, -36.06787431788703913, 37.45808914225474950 ) ) ;
#37866=CYLINDRICAL_SURFACE ( 'NONE', #8907, 51.99999999999999289 ) ;
#37878=LINE ( 'NONE', #41589, #9520 ) ;
#37885=CARTESIAN_POINT ( 'NONE',  ( 18.00000000000000355, 0.000000000000000000, 0.000000000000000000 ) ) ;
#37887=DIRECTION ( 'NONE',  ( -1.000000000000000000, -0.000000000000000000, 0.000000000000000000 ) ) ;
#37903=ORIENTED_EDGE ( 'NONE', *, *, #8169, .T. ) ;
#37907=EDGE_CURVE ( 'NONE', #39944, #4717, #30704, .T. ) ;
#37912=EDGE_CURVE ( 'NONE', #10533, #3682, #26525, .T. ) ;
#37915=CARTESIAN_POINT ( 'NONE',  ( 0.000000000000000000, 24.47917365149946889, 45.87777302070943364 ) ) ;
#37932=LINE ( 'NONE', #4789, #18191 ) ;
#37935=DIRECTION ( 'NONE',  ( -1.000000000000000000, 0.000000000000000000, 0.000000000000000000 ) ) ;
#37937=ORIENTED_EDGE ( 'NONE', *, *, #17308, .T. ) ;
#37945=CARTESIAN_POINT ( 'NONE',  ( 0.000000000000000000, -44.75336757549789013, 14.30704879393590012 ) ) ;
#37946=EDGE_LOOP ( 'NONE', ( #7993, #14797, #1403, #25072 ) ) ;
#37947=EDGE_CURVE ( 'NONE', #40464, #24642, #4937, .T. ) ;
#37950=CIRCLE ( 'NONE', #17093, 20.00000000000000355 ) ;
#37957=VERTEX_POINT ( 'NONE', #10218 ) ;
#37958=LINE ( 'NONE', #4356, #12032 ) ;
#37965=VERTEX_POINT ( 'NONE', #23776 ) ;
#37975=FACE_OUTER_BOUND ( 'NONE', #6652, .T. ) ;
#37985=DIRECTION ( 'NONE',  ( 0.000000000000000000, -0.4817536741017035551, -0.8763066800438700232 ) ) ;
#37987=AXIS2_PLACEMENT_3D ( 'NONE', #35629, #11899, #5745 ) ;
#37988=ORIENTED_EDGE ( 'NONE', *, *, #23463, .T. ) ;
#38005=CIRCLE ( 'NONE', #27569, 20.00000000000000711 ) ;
#38010=CARTESIAN_POINT ( 'NONE',  ( -10.00000000000000000, 0.000000000000000000, 0.000000000000000000 ) ) ;
#38012=ORIENTED_EDGE ( 'NONE', *, *, #9986, .F. ) ;
#38015=EDGE_CURVE ( 'NONE', #11580, #1632, #33487, .T. ) ;
#38016=LINE ( 'NONE', #28020, #2878 ) ;
#38034=ORIENTED_EDGE ( 'NONE', *, *, #40403, .T. ) ;
#38035=DIRECTION ( 'NONE',  ( 0.000000000000000000, 0.000000000000000000, 1.000000000000000000 ) ) ;
#38037=ADVANCED_FACE ( 'NONE', ( #42709 ), #29662, .T. ) ;
#38038=CIRCLE ( 'NONE', #4582, 51.99999999999999289 ) ;
#38039=CARTESIAN_POINT ( 'NONE',  ( 18.00000000000000355, 0.000000000000000000, 0.000000000000000000 ) ) ;
#38041=EDGE_CURVE ( 'NONE', #6092, #42889, #7808, .T. ) ;
#38045=AXIS2_PLACEMENT_3D ( 'NONE', #16063, #29368, #22849 ) ;
#38054=VECTOR ( 'NONE', #6353, 1000.000000000000000 ) ;
#38065=LINE ( 'NONE', #27847, #11181 ) ;
#38070=DIRECTION ( 'NONE',  ( 0.000000000000000000, 0.000000000000000000, 1.000000000000000000 ) ) ;
#38088=CIRCLE ( 'NONE', #29763, 20.00000000000000711 ) ;
#38089=CIRCLE ( 'NONE', #11756, 20.00000000000000711 ) ;
#38095=ADVANCED_FACE ( 'NONE', ( #1464 ), #7371, .T. ) ;
#38098=EDGE_CURVE ( 'NONE', #6854, #28114, #19506, .T. ) ;
#38102=CARTESIAN_POINT ( 'NONE',  ( 18.00000000000000355, -6.109652351741465814, -46.58570277113515345 ) ) ;
#38104=CIRCLE ( 'NONE', #8155, 20.00000000000000711 ) ;
#38107=CYLINDRICAL_SURFACE ( 'NONE', #36513, 47.49900000000000233 ) ;
#38108=ORIENTED_EDGE ( 'NONE', *, *, #21563, .F. ) ;
#38120=DIRECTION ( 'NONE',  ( -1.000000000000000000, 0.000000000000000000, -0.000000000000000000 ) ) ;
#38123=CARTESIAN_POINT ( 'NONE',  ( 0.000000000000000000, 0.000000000000000000, 0.000000000000000000 ) ) ;
#38142=AXIS2_PLACEMENT_3D ( 'NONE', #33212, #36462, #10307 ) ;
#38160=CYLINDRICAL_SURFACE ( 'NONE', #11452, 20.00000000000000711 ) ;
#38161=CARTESIAN_POINT ( 'NONE',  ( 18.00000000000000355, 13.85708833599968770, 45.43276465116669982 ) ) ;
#38168=VECTOR ( 'NONE', #4230, 1000.000000000000000 ) ;
#38172=DIRECTION ( 'NONE',  ( 1.000000000000000000, 0.000000000000000000, 0.000000000000000000 ) ) ;
#38184=CARTESIAN_POINT ( 'NONE',  ( 18.00000000000000355, 0.000000000000000000, 0.000000000000000000 ) ) ;
#38193=VERTEX_POINT ( 'NONE', #40520 ) ;
#38196=AXIS2_PLACEMENT_3D ( 'NONE', #8334, #14043, #27338 ) ;
#38202=EDGE_CURVE ( 'NONE', #41125, #24437, #23991, .T. ) ;
#38224=ORIENTED_EDGE ( 'NONE', *, *, #12910, .T. ) ;
#38225=CARTESIAN_POINT ( 'NONE',  ( 0.000000000000000000, 50.95304419620825342, 10.38206564895679129 ) ) ;
#38230=DIRECTION ( 'NONE',  ( 0.000000000000000000, 0.000000000000000000, 1.000000000000000000 ) ) ;
#38232=CARTESIAN_POINT ( 'NONE',  ( 18.00000000000000355, 3.840921266749842022, 47.34345070675171030 ) ) ;
#38256=AXIS2_PLACEMENT_3D ( 'NONE', #6019, #8705, #4020 ) ;
#38269=DIRECTION ( 'NONE',  ( 0.000000000000000000, 0.000000000000000000, 1.000000000000000000 ) ) ;
#38272=CARTESIAN_POINT ( 'NONE',  ( 0.000000000000000000, 0.000000000000000000, 0.000000000000000000 ) ) ;
#38275=CARTESIAN_POINT ( 'NONE',  ( 0.000000000000000000, 0.000000000000000000, 0.000000000000000000 ) ) ;
#38282=ORIENTED_EDGE ( 'NONE', *, *, #21796, .T. ) ;
#38287=CIRCLE ( 'NONE', #19511, 20.00000000000000711 ) ;
#38292=DIRECTION ( 'NONE',  ( -1.000000000000000000, 0.000000000000000000, 0.000000000000000000 ) ) ;
#38312=EDGE_LOOP ( 'NONE', ( #729, #6965, #36716, #36065 ) ) ;
#38323=CARTESIAN_POINT ( 'NONE',  ( 0.000000000000000000, 0.000000000000000000, 0.000000000000000000 ) ) ;
#38325=FACE_OUTER_BOUND ( 'NONE', #25993, .T. ) ;
#38330=DIRECTION ( 'NONE',  ( 1.000000000000000000, 0.000000000000000000, 0.000000000000000000 ) ) ;
#38337=EDGE_CURVE ( 'NONE', #4630, #21903, #6234, .T. ) ;
#38344=EDGE_CURVE ( 'NONE', #39961, #28966, #13238, .T. ) ;
#38345=ORIENTED_EDGE ( 'NONE', *, *, #20270, .T. ) ;
#38349=CIRCLE ( 'NONE', #20993, 52.00000000000000000 ) ;
#38351=ORIENTED_EDGE ( 'NONE', *, *, #25929, .F. ) ;
#38354=EDGE_CURVE ( 'NONE', #16239, #25141, #30045, .T. ) ;
#38362=DIRECTION ( 'NONE',  ( 0.000000000000000000, 0.000000000000000000, 1.000000000000000000 ) ) ;
#38375=ORIENTED_EDGE ( 'NONE', *, *, #7944, .F. ) ;
#38377=DIRECTION ( 'NONE',  ( 0.000000000000000000, 0.000000000000000000, 1.000000000000000000 ) ) ;
#38378=CARTESIAN_POINT ( 'NONE',  ( 0.000000000000000000, -13.85708833599937861, -45.43276465116677798 ) ) ;
#38382=ORIENTED_EDGE ( 'NONE', *, *, #296, .T. ) ;
#38385=CIRCLE ( 'NONE', #22423, 20.00000000000000711 ) ;
#38386=CARTESIAN_POINT ( 'NONE',  ( 0.000000000000000000, 0.000000000000000000, 0.000000000000000000 ) ) ;
#38395=DIRECTION ( 'NONE',  ( -1.000000000000000000, 0.000000000000000000, 0.000000000000000000 ) ) ;
#38400=EDGE_CURVE ( 'NONE', #40375, #25565, #6669, .T. ) ;
#38402=CARTESIAN_POINT ( 'NONE',  ( 18.00000000000000355, 0.000000000000000000, 0.000000000000000000 ) ) ;
#38406=CARTESIAN_POINT ( 'NONE',  ( 0.000000000000000000, -0.6505223195686533622, 51.99593080916758936 ) ) ;
#38407=AXIS2_PLACEMENT_3D ( 'NONE', #17067, #30352, #428 ) ;
#38408=EDGE_CURVE ( 'NONE', #36747, #19747, #1374, .T. ) ;
#38415=LINE ( 'NONE', #41903, #1559 ) ;
#38416=ORIENTED_EDGE ( 'NONE', *, *, #25060, .T. ) ;
#38419=CARTESIAN_POINT ( 'NONE',  ( 18.00000000000000355, 36.05989434073613609, 30.12041790338630776 ) ) ;
#38423=DIRECTION ( 'NONE',  ( -1.000000000000000000, -0.000000000000000000, -0.000000000000000000 ) ) ;
#38436=ORIENTED_EDGE ( 'NONE', *, *, #9501, .T. ) ;
#38443=LINE ( 'NONE', #24764, #18606 ) ;
#38445=ORIENTED_EDGE ( 'NONE', *, *, #32335, .T. ) ;
#38455=AXIS2_PLACEMENT_3D ( 'NONE', #40743, #14173, #36615 ) ;
#38457=ORIENTED_EDGE ( 'NONE', *, *, #26397, .T. ) ;
#38471=DIRECTION ( 'NONE',  ( 0.000000000000000000, 0.000000000000000000, 1.000000000000000000 ) ) ;
#38485=EDGE_CURVE ( 'NONE', #12223, #17739, #2231, .T. ) ;
#38487=DIRECTION ( 'NONE',  ( 0.000000000000000000, 0.000000000000000000, 1.000000000000000000 ) ) ;
#38498=( NAMED_UNIT ( * ) SI_UNIT ( $, .STERADIAN. ) SOLID_ANGLE_UNIT ( ) );
#38507=DIRECTION ( 'NONE',  ( -1.000000000000000000, -0.000000000000000000, 0.000000000000000000 ) ) ;
#38508=ORIENTED_EDGE ( 'NONE', *, *, #39009, .F. ) ;
#38510=DIRECTION ( 'NONE',  ( -1.000000000000000000, -0.000000000000000000, 0.000000000000000000 ) ) ;
#38514=AXIS2_PLACEMENT_3D ( 'NONE', #35026, #17842, #21340 ) ;
#38517=ORIENTED_EDGE ( 'NONE', *, *, #569, .F. ) ;
#38518=LINE ( 'NONE', #11507, #17235 ) ;
#38522=DIRECTION ( 'NONE',  ( -1.000000000000000000, -0.000000000000000000, -0.000000000000000000 ) ) ;
#38527=DIRECTION ( 'NONE',  ( 0.000000000000000000, 0.1253332335643046469, -0.9921147013144777649 ) ) ;
#38530=ORIENTED_EDGE ( 'NONE', *, *, #28210, .T. ) ;
#38535=CARTESIAN_POINT ( 'NONE',  ( 0.000000000000000000, 49.65209126885762458, 15.44894276735567651 ) ) ;
#38546=LINE ( 'NONE', #28565, #41524 ) ;
#38547=ORIENTED_EDGE ( 'NONE', *, *, #18056, .T. ) ;
#38549=CIRCLE ( 'NONE', #19779, 47.49900000000000944 ) ;
#38551=DIRECTION ( 'NONE',  ( -1.000000000000000000, 0.000000000000000000, 0.000000000000000000 ) ) ;
#38563=ORIENTED_EDGE ( 'NONE', *, *, #15425, .T. ) ;
#38568=DIRECTION ( 'NONE',  ( 0.000000000000000000, 0.000000000000000000, 1.000000000000000000 ) ) ;
#38574=ORIENTED_EDGE ( 'NONE', *, *, #19048, .T. ) ;
#38575=CYLINDRICAL_SURFACE ( 'NONE', #15631, 20.00000000000000711 ) ;
#38578=VERTEX_POINT ( 'NONE', #15181 ) ;
#38580=DIRECTION ( 'NONE',  ( 0.000000000000000000, 0.3681245526846720906, 0.9297764858882537897 ) ) ;
#38591=DIRECTION ( 'NONE',  ( 0.000000000000000000, 0.000000000000000000, 1.000000000000000000 ) ) ;
#38597=ORIENTED_EDGE ( 'NONE', *, *, #27984, .T. ) ;
#38603=ORIENTED_EDGE ( 'NONE', *, *, #21166, .T. ) ;
#38616=VECTOR ( 'NONE', #40584, 1000.000000000000000 ) ;
#38623=VECTOR ( 'NONE', #4965, 1000.000000000000000 ) ;
#38634=AXIS2_PLACEMENT_3D ( 'NONE', #10286, #36665, #33195 ) ;
#38642=CARTESIAN_POINT ( 'NONE',  ( 0.000000000000000000, 47.00885577955421013, -6.806061952191806874 ) ) ;
#38661=CARTESIAN_POINT ( 'NONE',  ( 0.000000000000000000, -42.60732521687558005, -19.80331771201703006 ) ) ;
#38666=AXIS2_PLACEMENT_3D ( 'NONE', #42253, #12407, #5617 ) ;
#38673=VERTEX_POINT ( 'NONE', #4331 ) ;
#38685=DIRECTION ( 'NONE',  ( 0.000000000000000000, 0.000000000000000000, -1.000000000000000000 ) ) ;
#38686=AXIS2_PLACEMENT_3D ( 'NONE', #8405, #38710, #8202 ) ;
#38688=LINE ( 'NONE', #2039, #16595 ) ;
#38699=VERTEX_POINT ( 'NONE', #7406 ) ;
#38703=ORIENTED_EDGE ( 'NONE', *, *, #14566, .T. ) ;
#38710=DIRECTION ( 'NONE',  ( -1.000000000000000000, -0.000000000000000000, -0.000000000000000000 ) ) ;
#38711=VERTEX_POINT ( 'NONE', #26259 ) ;
#38728=CARTESIAN_POINT ( 'NONE',  ( 18.00000000000000355, 0.000000000000000000, 0.000000000000000000 ) ) ;
#38739=EDGE_LOOP ( 'NONE', ( #40517, #22426, #21491, #35494 ) ) ;
#38740=CARTESIAN_POINT ( 'NONE',  ( 18.00000000000000355, 26.17370628620655637, 39.63700417846172286 ) ) ;
#38741=FACE_OUTER_BOUND ( 'NONE', #9393, .T. ) ;
#38746=DIRECTION ( 'NONE',  ( 1.000000000000000000, 0.000000000000000000, 0.000000000000000000 ) ) ;
#38748=LINE ( 'NONE', #1887, #38937 ) ;
#38757=FACE_OUTER_BOUND ( 'NONE', #26673, .T. ) ;
#38764=ORIENTED_EDGE ( 'NONE', *, *, #34060, .T. ) ;
#38772=EDGE_CURVE ( 'NONE', #26339, #26382, #39016, .T. ) ;
#38773=VERTEX_POINT ( 'NONE', #26681 ) ;
#38778=DIRECTION ( 'NONE',  ( -1.000000000000000000, 0.000000000000000000, 0.000000000000000000 ) ) ;
#38787=AXIS2_PLACEMENT_3D ( 'NONE', #20370, #30384, #27119 ) ;
#38795=CARTESIAN_POINT ( 'NONE',  ( 18.00000000000000355, -42.41764978026593269, -20.20639853260334107 ) ) ;
#38806=ORIENTED_EDGE ( 'NONE', *, *, #10761, .T. ) ;
#38826=VECTOR ( 'NONE', #23272, 1000.000000000000000 ) ;
#38831=CARTESIAN_POINT ( 'NONE',  ( 18.00000000000000355, -20.99948489194451540, 42.60488980472774045 ) ) ;
#38833=CARTESIAN_POINT ( 'NONE',  ( 0.000000000000000000, -51.93417535146738828, -2.615612846549715709 ) ) ;
#38835=EDGE_LOOP ( 'NONE', ( #16549, #26882, #6715, #35265 ) ) ;
#38838=ORIENTED_EDGE ( 'NONE', *, *, #1791, .F. ) ;
#38845=CIRCLE ( 'NONE', #15904, 51.99999999999999289 ) ;
#38856=CARTESIAN_POINT ( 'NONE',  ( 0.000000000000000000, 5.667686777401707232, 46.64153600743607342 ) ) ;
#38857=ORIENTED_EDGE ( 'NONE', *, *, #12721, .T. ) ;
#38861=DIRECTION ( 'NONE',  ( -1.000000000000000000, -0.000000000000000000, -0.000000000000000000 ) ) ;
#38862=CIRCLE ( 'NONE', #5430, 47.49900000000000233 ) ;
#38876=EDGE_CURVE ( 'NONE', #26478, #26596, #12580, .T. ) ;
#38888=FACE_OUTER_BOUND ( 'NONE', #12129, .T. ) ;
#38890=AXIS2_PLACEMENT_3D ( 'NONE', #12483, #6121, #2390 ) ;
#38897=CARTESIAN_POINT ( 'NONE',  ( 0.000000000000000000, -2.123073309835498801, 47.45152853935333326 ) ) ;
#38901=ORIENTED_EDGE ( 'NONE', *, *, #24419, .T. ) ;
#38910=ORIENTED_EDGE ( 'NONE', *, *, #19605, .F. ) ;
#38912=EDGE_CURVE ( 'NONE', #12154, #25951, #15498, .T. ) ;
#38915=CARTESIAN_POINT ( 'NONE',  ( 0.000000000000000000, 47.49120266317495265, 0.8606222198176843863 ) ) ;
#38921=CYLINDRICAL_SURFACE ( 'NONE', #35536, 47.49900000000000233 ) ;
#38925=CARTESIAN_POINT ( 'NONE',  ( 18.00000000000000355, -36.05989434073592292, -30.12041790338656710 ) ) ;
#38930=DIRECTION ( 'NONE',  ( -1.000000000000000000, 0.000000000000000000, 0.000000000000000000 ) ) ;
#38933=DIRECTION ( 'NONE',  ( -1.000000000000000000, -0.000000000000000000, 0.000000000000000000 ) ) ;
#38937=VECTOR ( 'NONE', #32011, 1000.000000000000000 ) ;
#38951=VERTEX_POINT ( 'NONE', #22052 ) ;
#38959=DIRECTION ( 'NONE',  ( 0.000000000000000000, 0.000000000000000000, 1.000000000000000000 ) ) ;
#38964=AXIS2_PLACEMENT_3D ( 'NONE', #20021, #6877, #39167 ) ;
#38966=DIRECTION ( 'NONE',  ( -1.000000000000000000, 0.000000000000000000, 0.000000000000000000 ) ) ;
#38978=EDGE_CURVE ( 'NONE', #34048, #39608, #37932, .T. ) ;
#39008=CYLINDRICAL_SURFACE ( 'NONE', #43073, 47.49900000000000233 ) ;
#39009=EDGE_CURVE ( 'NONE', #4850, #22654, #11905, .T. ) ;
#39016=CIRCLE ( 'NONE', #36210, 20.00000000000000355 ) ;
#39017=ORIENTED_EDGE ( 'NONE', *, *, #16253, .T. ) ;
#39020=CARTESIAN_POINT ( 'NONE',  ( 18.00000000000000355, 0.000000000000000000, 0.000000000000000000 ) ) ;
#39029=CARTESIAN_POINT ( 'NONE',  ( 18.00000000000000355, 0.000000000000000000, 0.000000000000000000 ) ) ;
#39030=ORIENTED_EDGE ( 'NONE', *, *, #37553, .F. ) ;
#39031=CARTESIAN_POINT ( 'NONE',  ( 18.00000000000000355, 0.000000000000000000, 0.000000000000000000 ) ) ;
#39032=DIRECTION ( 'NONE',  ( -1.000000000000000000, -0.000000000000000000, 0.000000000000000000 ) ) ;
#39037=FACE_OUTER_BOUND ( 'NONE', #36107, .T. ) ;
#39039=EDGE_CURVE ( 'NONE', #18280, #22812, #5396, .T. ) ;
#39044=AXIS2_PLACEMENT_3D ( 'NONE', #22879, #36122, #42874 ) ;
#39058=CARTESIAN_POINT ( 'NONE',  ( 18.00000000000000355, 44.47301969247467923, -16.68249143361863318 ) ) ;
#39061=ORIENTED_EDGE ( 'NONE', *, *, #40509, .F. ) ;
#39067=ORIENTED_EDGE ( 'NONE', *, *, #40417, .T. ) ;
#39068=CARTESIAN_POINT ( 'NONE',  ( 18.00000000000000355, -27.43636312076294814, -38.14186064215179073 ) ) ;
#39077=CIRCLE ( 'NONE', #41891, 51.99999999999999289 ) ;
#39083=CARTESIAN_POINT ( 'NONE',  ( -132.0000507999999968, 0.000000000000000000, 0.000000000000000000 ) ) ;
#39090=DIRECTION ( 'NONE',  ( -1.000000000000000000, 0.000000000000000000, -0.000000000000000000 ) ) ;
#39100=DIRECTION ( 'NONE',  ( 0.000000000000000000, 0.000000000000000000, 1.000000000000000000 ) ) ;
#39108=VECTOR ( 'NONE', #17566, 1000.000000000000000 ) ;
#39110=VECTOR ( 'NONE', #27404, 1000.000000000000000 ) ;
#39112=ADVANCED_FACE ( 'NONE', ( #28756 ), #2297, .T. ) ;
#39116=CIRCLE ( 'NONE', #1498, 20.00000000000000711 ) ;
#39117=CARTESIAN_POINT ( 'NONE',  ( 0.000000000000000000, -22.82995208772716467, 41.06517797613655318 ) ) ;
#39125=EDGE_LOOP ( 'NONE', ( #43005, #2121, #38282, #12402 ) ) ;
#39140=CARTESIAN_POINT ( 'NONE',  ( -10.00000000000000000, 0.000000000000000000, 0.000000000000000000 ) ) ;
#39141=AXIS2_PLACEMENT_3D ( 'NONE', #1116, #31026, #10308 ) ;
#39159=EDGE_CURVE ( 'NONE', #11580, #255, #9523, .T. ) ;
#39161=DIRECTION ( 'NONE',  ( 1.000000000000000000, 0.000000000000000000, 0.000000000000000000 ) ) ;
#39165=EDGE_CURVE ( 'NONE', #9752, #33321, #9785, .T. ) ;
#39166=AXIS2_PLACEMENT_3D ( 'NONE', #20959, #13961, #30539 ) ;
#39167=DIRECTION ( 'NONE',  ( 0.000000000000000000, -0.9980267284282723361, 0.06279051952930261860 ) ) ;
#39175=EDGE_LOOP ( 'NONE', ( #17059, #41788, #1898, #33904 ) ) ;
#39186=VERTEX_POINT ( 'NONE', #28965 ) ;
#39192=EDGE_CURVE ( 'NONE', #26141, #42150, #10506, .T. ) ;
#39193=LINE ( 'NONE', #22465, #10747 ) ;
#39196=ORIENTED_EDGE ( 'NONE', *, *, #2383, .T. ) ;
#39207=EDGE_CURVE ( 'NONE', #39608, #15819, #4933, .T. ) ;
#39231=ORIENTED_EDGE ( 'NONE', *, *, #23504, .F. ) ;
#39239=ADVANCED_FACE ( 'NONE', ( #29600 ), #20028, .T. ) ;
#39241=CIRCLE ( 'NONE', #41338, 47.49900000000000233 ) ;
#39247=CARTESIAN_POINT ( 'NONE',  ( 9.000000000000001776, 12.30077720129167851, -50.52416135122069107 ) ) ;
#39248=CARTESIAN_POINT ( 'NONE',  ( 18.00000000000000355, 47.22458491092820765, 5.098390039074388369 ) ) ;
#39249=DIRECTION ( 'NONE',  ( -1.000000000000000000, 0.000000000000000000, 0.000000000000000000 ) ) ;
#39262=EDGE_CURVE ( 'NONE', #21384, #291, #41831, .T. ) ;
#39264=AXIS2_PLACEMENT_3D ( 'NONE', #16726, #4003, #43074 ) ;
#39270=CARTESIAN_POINT ( 'NONE',  ( 18.00000000000000355, 24.72041153920788403, -40.55929306992662475 ) ) ;
#39272=CARTESIAN_POINT ( 'NONE',  ( 0.000000000000000000, -29.60891106212812574, 37.14118181634756155 ) ) ;
#39273=ORIENTED_EDGE ( 'NONE', *, *, #2446, .F. ) ;
#39279=CARTESIAN_POINT ( 'NONE',  ( 0.000000000000000000, -15.49408907645141653, -44.90087086784608061 ) ) ;
#39280=DIRECTION ( 'NONE',  ( 0.000000000000000000, 0.000000000000000000, 1.000000000000000000 ) ) ;
#39286=ADVANCED_FACE ( 'NONE', ( #2519 ), #42453, .T. ) ;
#39292=DIRECTION ( 'NONE',  ( 0.000000000000000000, 0.000000000000000000, 1.000000000000000000 ) ) ;
#39298=VECTOR ( 'NONE', #12312, 1000.000000000000000 ) ;
#39306=VERTEX_POINT ( 'NONE', #5808 ) ;
#39307=DIRECTION ( 'NONE',  ( 0.000000000000000000, -0.6845471059286950544, 0.7289686274214053352 ) ) ;
#39310=DIRECTION ( 'NONE',  ( -1.000000000000000000, 0.000000000000000000, -0.000000000000000000 ) ) ;
#39316=CARTESIAN_POINT ( 'NONE',  ( 0.000000000000000000, 0.000000000000000000, 0.000000000000000000 ) ) ;
#39327=AXIS2_PLACEMENT_3D ( 'NONE', #30467, #21272, #38230 ) ;
#39345=EDGE_CURVE ( 'NONE', #28038, #22999, #11052, .T. ) ;
#39356=AXIS2_PLACEMENT_3D ( 'NONE', #24597, #37635, #7544 ) ;
#39359=AXIS2_PLACEMENT_3D ( 'NONE', #34363, #24588, #38487 ) ;
#39364=ORIENTED_EDGE ( 'NONE', *, *, #24830, .T. ) ;
#39377=DIRECTION ( 'NONE',  ( -1.000000000000000000, 0.000000000000000000, -0.000000000000000000 ) ) ;
#39384=DIRECTION ( 'NONE',  ( -1.000000000000000000, 0.000000000000000000, 0.000000000000000000 ) ) ;
#39388=DIRECTION ( 'NONE',  ( 0.000000000000000000, -0.4817536741017223179, 0.8763066800438596982 ) ) ;
#39396=EDGE_LOOP ( 'NONE', ( #20481, #34836, #11289, #23900 ) ) ;
#39397=CARTESIAN_POINT ( 'NONE',  ( 18.00000000000000355, -46.19362259308827845, -8.585149169758995669 ) ) ;
#39408=EDGE_CURVE ( 'NONE', #16293, #38951, #40897, .T. ) ;
#39421=DIRECTION ( 'NONE',  ( 0.000000000000000000, 0.000000000000000000, 1.000000000000000000 ) ) ;
#39427=VERTEX_POINT ( 'NONE', #36769 ) ;
#39444=EDGE_LOOP ( 'NONE', ( #21957, #38351, #41716, #38574 ) ) ;
#39452=VERTEX_POINT ( 'NONE', #307 ) ;
#39455=ORIENTED_EDGE ( 'NONE', *, *, #13580, .F. ) ;
#39476=DIRECTION ( 'NONE',  ( -1.000000000000000000, 0.000000000000000000, -0.000000000000000000 ) ) ;
#39479=DIRECTION ( 'NONE',  ( 0.000000000000000000, -0.4817536741017036661, -0.8763066800438700232 ) ) ;
#39482=CIRCLE ( 'NONE', #12376, 20.00000000000000711 ) ;
#39486=CARTESIAN_POINT ( 'NONE',  ( 18.00000000000000355, -46.11014828289837197, -9.022736828081200144 ) ) ;
#39496=LINE ( 'NONE', #39704, #4261 ) ;
#39498=LINE ( 'NONE', #39270, #29622 ) ;
#39500=ORIENTED_EDGE ( 'NONE', *, *, #15192, .F. ) ;
#39511=ORIENTED_EDGE ( 'NONE', *, *, #40753, .F. ) ;
#39522=VECTOR ( 'NONE', #12508, 1000.000000000000000 ) ;
#39529=ADVANCED_FACE ( 'NONE', ( #31974 ), #28286, .T. ) ;
#39541=VERTEX_POINT ( 'NONE', #4458 ) ;
#39544=CARTESIAN_POINT ( 'NONE',  ( 0.000000000000000000, 0.000000000000000000, 0.000000000000000000 ) ) ;
#39545=EDGE_CURVE ( 'NONE', #41964, #8913, #8453, .T. ) ;
#39547=CARTESIAN_POINT ( 'NONE',  ( 0.000000000000000000, 46.19362259308835661, 8.585149169758654608 ) ) ;
#39559=AXIS2_PLACEMENT_3D ( 'NONE', #39083, #25400, #25617 ) ;
#39562=FACE_OUTER_BOUND ( 'NONE', #19760, .T. ) ;
#39569=DIRECTION ( 'NONE',  ( -1.000000000000000000, 0.000000000000000000, 0.000000000000000000 ) ) ;
#39570=DIRECTION ( 'NONE',  ( 1.000000000000000000, 0.000000000000000000, 0.000000000000000000 ) ) ;
#39577=ORIENTED_EDGE ( 'NONE', *, *, #9955, .T. ) ;
#39578=CARTESIAN_POINT ( 'NONE',  ( 18.00000000000000355, 0.000000000000000000, 0.000000000000000000 ) ) ;
#39591=ORIENTED_EDGE ( 'NONE', *, *, #28694, .F. ) ;
#39596=CARTESIAN_POINT ( 'NONE',  ( 0.000000000000000000, 29.60891106212788415, 37.14118181634774629 ) ) ;
#39601=EDGE_CURVE ( 'NONE', #39427, #10641, #1194, .T. ) ;
#39603=ADVANCED_FACE ( 'NONE', ( #1624 ), #24587, .T. ) ;
#39604=LINE ( 'NONE', #42449, #35710 ) ;
#39608=VERTEX_POINT ( 'NONE', #22821 ) ;
#39621=FACE_BOUND ( 'NONE', #9486, .T. ) ;
#39629=ADVANCED_FACE ( 'NONE', ( #12759 ), #22602, .T. ) ;
#39644=VERTEX_POINT ( 'NONE', #23033 ) ;
#39648=CARTESIAN_POINT ( 'NONE',  ( 9.000000000000001776, -39.64889472655706015, -33.64468972902550092 ) ) ;
#39651=DIRECTION ( 'NONE',  ( 0.000000000000000000, 0.000000000000000000, 1.000000000000000000 ) ) ;
#39660=ORIENTED_EDGE ( 'NONE', *, *, #39760, .F. ) ;
#39666=ORIENTED_EDGE ( 'NONE', *, *, #13058, .F. ) ;
#39692=DIRECTION ( 'NONE',  ( 0.000000000000000000, -0.1253332335642904638, -0.9921147013144796523 ) ) ;
#39704=CARTESIAN_POINT ( 'NONE',  ( 9.000000000000001776, 51.19683565102444334, 9.104066087303641197 ) ) ;
#39709=CARTESIAN_POINT ( 'NONE',  ( 18.00000000000000355, 30.03615769709733740, 42.44795908868999135 ) ) ;
#39713=DIRECTION ( 'NONE',  ( 0.000000000000000000, 0.000000000000000000, 1.000000000000000000 ) ) ;
#39714=DIRECTION ( 'NONE',  ( 0.000000000000000000, 0.000000000000000000, 1.000000000000000000 ) ) ;
#39716=DIRECTION ( 'NONE',  ( -1.000000000000000000, 0.000000000000000000, 0.000000000000000000 ) ) ;
#39717=ORIENTED_EDGE ( 'NONE', *, *, #39192, .T. ) ;
#39726=ORIENTED_EDGE ( 'NONE', *, *, #39207, .F. ) ;
#39734=DIRECTION ( 'NONE',  ( 0.000000000000000000, 0.000000000000000000, 1.000000000000000000 ) ) ;
#39738=DIRECTION ( 'NONE',  ( 0.000000000000000000, 0.9980267284282716700, -0.06279051952930995995 ) ) ;
#39750=CIRCLE ( 'NONE', #21015, 47.49900000000000233 ) ;
#39751=DIRECTION ( 'NONE',  ( -1.000000000000000000, -0.000000000000000000, 0.000000000000000000 ) ) ;
#39753=VERTEX_POINT ( 'NONE', #13627 ) ;
#39760=EDGE_CURVE ( 'NONE', #42037, #38673, #24101, .T. ) ;
#39771=CIRCLE ( 'NONE', #16851, 20.00000000000000355 ) ;
#39781=ORIENTED_EDGE ( 'NONE', *, *, #22685, .F. ) ;
#39782=EDGE_CURVE ( 'NONE', #14255, #9587, #4194, .T. ) ;
#39788=EDGE_CURVE ( 'NONE', #9587, #31709, #23834, .T. ) ;
#39801=VERTEX_POINT ( 'NONE', #20851 ) ;
#39803=EDGE_CURVE ( 'NONE', #6408, #23271, #2868, .T. ) ;
#39804=CARTESIAN_POINT ( 'NONE',  ( 18.00000000000000355, 0.000000000000000000, 0.000000000000000000 ) ) ;
#39805=DIRECTION ( 'NONE',  ( -1.000000000000000000, -0.000000000000000000, -0.000000000000000000 ) ) ;
#39807=ORIENTED_EDGE ( 'NONE', *, *, #34347, .F. ) ;
#39811=CARTESIAN_POINT ( 'NONE',  ( 18.00000000000000355, 46.19362259308845609, -8.585149169757988474 ) ) ;
#39812=VERTEX_POINT ( 'NONE', #36717 ) ;
#39813=ORIENTED_EDGE ( 'NONE', *, *, #21172, .T. ) ;
#39819=CIRCLE ( 'NONE', #9164, 20.00000000000000355 ) ;
#39822=EDGE_CURVE ( 'NONE', #36818, #14078, #10570, .T. ) ;
#39823=CARTESIAN_POINT ( 'NONE',  ( 18.00000000000000355, 22.43957647427220081, -41.27978878573604504 ) ) ;
#39831=LINE ( 'NONE', #23526, #25348 ) ;
#39834=CYLINDRICAL_SURFACE ( 'NONE', #23358, 20.00000000000000355 ) ;
#39835=ORIENTED_EDGE ( 'NONE', *, *, #16812, .F. ) ;
#39848=DIRECTION ( 'NONE',  ( 0.000000000000000000, 0.000000000000000000, 1.000000000000000000 ) ) ;
#39854=ORIENTED_EDGE ( 'NONE', *, *, #2795, .F. ) ;
#39858=CARTESIAN_POINT ( 'NONE',  ( 18.00000000000000355, 42.03146605346817921, -22.12489237027272893 ) ) ;
#39859=VECTOR ( 'NONE', #21664, 1000.000000000000000 ) ;
#39873=FACE_OUTER_BOUND ( 'NONE', #25592, .T. ) ;
#39875=CARTESIAN_POINT ( 'NONE',  ( 0.000000000000000000, 51.85248208264517444, 3.914090171286374265 ) ) ;
#39876=ORIENTED_EDGE ( 'NONE', *, *, #9111, .T. ) ;
#39882=AXIS2_PLACEMENT_3D ( 'NONE', #26593, #2344, #6079 ) ;
#39887=AXIS2_PLACEMENT_3D ( 'NONE', #17029, #33143, #6953 ) ;
#39890=ORIENTED_EDGE ( 'NONE', *, *, #43076, .F. ) ;
#39893=ADVANCED_FACE ( 'NONE', ( #27806 ), #25189, .T. ) ;
#39895=DIRECTION ( 'NONE',  ( -1.000000000000000000, 0.000000000000000000, -0.000000000000000000 ) ) ;
#39905=VERTEX_POINT ( 'NONE', #14924 ) ;
#39906=DIRECTION ( 'NONE',  ( -1.000000000000000000, 0.000000000000000000, -0.000000000000000000 ) ) ;
#39909=DIRECTION ( 'NONE',  ( -1.000000000000000000, 0.000000000000000000, -0.000000000000000000 ) ) ;
#39913=ORIENTED_EDGE ( 'NONE', *, *, #30448, .F. ) ;
#39941=EDGE_CURVE ( 'NONE', #14485, #4058, #5672, .T. ) ;
#39942=AXIS2_PLACEMENT_3D ( 'NONE', #3347, #37547, #9906 ) ;
#39943=ORIENTED_EDGE ( 'NONE', *, *, #11194, .T. ) ;
#39944=VERTEX_POINT ( 'NONE', #41495 ) ;
#39949=ORIENTED_EDGE ( 'NONE', *, *, #28659, .F. ) ;
#39957=AXIS2_PLACEMENT_3D ( 'NONE', #41450, #11601, #24942 ) ;
#39961=VERTEX_POINT ( 'NONE', #38232 ) ;
#39962=CARTESIAN_POINT ( 'NONE',  ( 0.000000000000000000, 0.000000000000000000, 0.000000000000000000 ) ) ;
#39963=AXIS2_PLACEMENT_3D ( 'NONE', #24252, #30560, #40763 ) ;
#39980=DIRECTION ( 'NONE',  ( -1.000000000000000000, 0.000000000000000000, -0.000000000000000000 ) ) ;
#39982=ORIENTED_EDGE ( 'NONE', *, *, #23798, .T. ) ;
#40005=DIRECTION ( 'NONE',  ( 0.000000000000000000, 0.000000000000000000, 1.000000000000000000 ) ) ;
#40008=DIRECTION ( 'NONE',  ( 0.000000000000000000, 0.000000000000000000, 1.000000000000000000 ) ) ;
#40009=EDGE_LOOP ( 'NONE', ( #33881, #26500, #40442, #20210 ) ) ;
#40013=DIRECTION ( 'NONE',  ( -1.000000000000000000, 0.000000000000000000, 0.000000000000000000 ) ) ;
#40026=ADVANCED_FACE ( 'NONE', ( #12285 ), #12707, .T. ) ;
#40027=DIRECTION ( 'NONE',  ( 0.000000000000000000, 0.000000000000000000, 1.000000000000000000 ) ) ;
#40029=CARTESIAN_POINT ( 'NONE',  ( 18.00000000000000355, -35.20873326984057883, -31.88259874184068465 ) ) ;
#40031=CYLINDRICAL_SURFACE ( 'NONE', #29713, 7.500000000000000000 ) ;
#40045=CIRCLE ( 'NONE', #33092, 7.500000000000000000 ) ;
#40053=ORIENTED_EDGE ( 'NONE', *, *, #9275, .T. ) ;
#40054=ORIENTED_EDGE ( 'NONE', *, *, #1711, .T. ) ;
#40057=CARTESIAN_POINT ( 'NONE',  ( -10.00000000000000000, 0.000000000000000000, 0.000000000000000000 ) ) ;
#40065=LINE ( 'NONE', #3631, #15271 ) ;
#40069=FACE_OUTER_BOUND ( 'NONE', #6814, .T. ) ;
#40077=EDGE_CURVE ( 'NONE', #31266, #2932, #13362, .T. ) ;
#40080=DIRECTION ( 'NONE',  ( 0.000000000000000000, 0.6845471059286846183, 0.7289686274214153272 ) ) ;
#40083=ADVANCED_FACE ( 'NONE', ( #15995 ), #12500, .T. ) ;
#40100=CYLINDRICAL_SURFACE ( 'NONE', #2334, 47.49900000000000233 ) ;
#40102=CIRCLE ( 'NONE', #10159, 20.00000000000000711 ) ;
#40103=ORIENTED_EDGE ( 'NONE', *, *, #7327, .F. ) ;
#40106=AXIS2_PLACEMENT_3D ( 'NONE', #15516, #32275, #29238 ) ;
#40123=DIRECTION ( 'NONE',  ( -1.000000000000000000, -0.000000000000000000, 0.000000000000000000 ) ) ;
#40130=ORIENTED_EDGE ( 'NONE', *, *, #20256, .F. ) ;
#40136=ADVANCED_FACE ( 'NONE', ( #42761 ), #16412, .T. ) ;
#40142=AXIS2_PLACEMENT_3D ( 'NONE', #41827, #11980, #41618 ) ;
#40146=DIRECTION ( 'NONE',  ( -1.000000000000000000, 0.000000000000000000, -0.000000000000000000 ) ) ;
#40156=DIRECTION ( 'NONE',  ( 0.000000000000000000, 0.000000000000000000, 1.000000000000000000 ) ) ;
#40167=EDGE_CURVE ( 'NONE', #8333, #37461, #9871, .T. ) ;
#40168=CIRCLE ( 'NONE', #42263, 20.00000000000000711 ) ;
#40171=VERTEX_POINT ( 'NONE', #10763 ) ;
#40180=DIRECTION ( 'NONE',  ( 0.000000000000000000, -0.9980267284282723361, 0.06279051952930260472 ) ) ;
#40198=VERTEX_POINT ( 'NONE', #36887 ) ;
#40199=CARTESIAN_POINT ( 'NONE',  ( 9.000000000000001776, -7.162210897276081845, 51.50439529848825515 ) ) ;
#40202=VERTEX_POINT ( 'NONE', #39709 ) ;
#40207=CARTESIAN_POINT ( 'NONE',  ( 18.00000000000000355, 0.000000000000000000, 0.000000000000000000 ) ) ;
#40213=CYLINDRICAL_SURFACE ( 'NONE', #35915, 47.49900000000000233 ) ;
#40223=DIRECTION ( 'NONE',  ( -1.000000000000000000, 0.000000000000000000, -0.000000000000000000 ) ) ;
#40231=ORIENTED_EDGE ( 'NONE', *, *, #13562, .F. ) ;
#40233=CIRCLE ( 'NONE', #2604, 20.00000000000000711 ) ;
#40239=VECTOR ( 'NONE', #9377, 1000.000000000000000 ) ;
#40242=CYLINDRICAL_SURFACE ( 'NONE', #43135, 47.49900000000000233 ) ;
#40252=ORIENTED_EDGE ( 'NONE', *, *, #36054, .F. ) ;
#40259=DIRECTION ( 'NONE',  ( 0.000000000000000000, 0.000000000000000000, 1.000000000000000000 ) ) ;
#40261=DIRECTION ( 'NONE',  ( 0.000000000000000000, 0.000000000000000000, -1.000000000000000000 ) ) ;
#40270=ORIENTED_EDGE ( 'NONE', *, *, #35383, .F. ) ;
#40277=CYLINDRICAL_SURFACE ( 'NONE', #7527, 20.00000000000000355 ) ;
#40286=LINE ( 'NONE', #27666, #22128 ) ;
#40289=ORIENTED_EDGE ( 'NONE', *, *, #31413, .T. ) ;
#40292=CARTESIAN_POINT ( 'NONE',  ( 18.00000000000000355, 0.000000000000000000, 0.000000000000000000 ) ) ;
#40295=ORIENTED_EDGE ( 'NONE', *, *, #1644, .F. ) ;
#40298=DIRECTION ( 'NONE',  ( -1.000000000000000000, 0.000000000000000000, 0.000000000000000000 ) ) ;
#40299=AXIS2_PLACEMENT_3D ( 'NONE', #37885, #18103, #40505 ) ;
#40302=AXIS2_PLACEMENT_3D ( 'NONE', #24788, #18046, #1176 ) ;
#40304=CARTESIAN_POINT ( 'NONE',  ( 18.00000000000000355, 8.053585752062561554, -46.81126742072013514 ) ) ;
#40309=DIRECTION ( 'NONE',  ( -1.000000000000000000, -0.000000000000000000, -0.000000000000000000 ) ) ;
#40310=CYLINDRICAL_SURFACE ( 'NONE', #9466, 47.49900000000000233 ) ;
#40311=DIRECTION ( 'NONE',  ( -1.000000000000000000, 0.000000000000000000, -0.000000000000000000 ) ) ;
#40314=CARTESIAN_POINT ( 'NONE',  ( 0.000000000000000000, 42.41764978026607480, -20.20639853260305685 ) ) ;
#40320=CARTESIAN_POINT ( 'NONE',  ( 0.000000000000000000, 5.871425383722279179, -51.66745943012274722 ) ) ;
#40322=CYLINDRICAL_SURFACE ( 'NONE', #6452, 20.00000000000001066 ) ;
#40329=CIRCLE ( 'NONE', #11792, 52.00000000000000000 ) ;
#40335=CARTESIAN_POINT ( 'NONE',  ( 18.00000000000000355, -3.840921266749491192, -47.34345070675175293 ) ) ;
#40336=EDGE_CURVE ( 'NONE', #19113, #35135, #37958, .T. ) ;
#40342=DIRECTION ( 'NONE',  ( -1.000000000000000000, -0.000000000000000000, 0.000000000000000000 ) ) ;
#40345=CARTESIAN_POINT ( 'NONE',  ( 0.000000000000000000, -38.92705108641749945, 27.21837053747784552 ) ) ;
#40356=ORIENTED_EDGE ( 'NONE', *, *, #10593, .F. ) ;
#40365=ADVANCED_FACE ( 'NONE', ( #25142 ), #21449, .T. ) ;
#40375=VERTEX_POINT ( 'NONE', #17955 ) ;
#40377=FACE_OUTER_BOUND ( 'NONE', #2392, .T. ) ;
#40387=EDGE_CURVE ( 'NONE', #31578, #27751, #8511, .T. ) ;
#40389=CARTESIAN_POINT ( 'NONE',  ( 9.000000000000001776, 35.11945359308163717, -38.34871548465978464 ) ) ;
#40394=DIRECTION ( 'NONE',  ( 0.000000000000000000, -0.4817536741017223179, 0.8763066800438598092 ) ) ;
#40397=DIRECTION ( 'NONE',  ( 1.000000000000000000, -0.000000000000000000, 0.000000000000000000 ) ) ;
#40400=ORIENTED_EDGE ( 'NONE', *, *, #7050, .T. ) ;
#40403=EDGE_CURVE ( 'NONE', #17987, #19733, #21660, .T. ) ;
#40409=CARTESIAN_POINT ( 'NONE',  ( -132.0000507999999968, 0.000000000000000000, 0.000000000000000000 ) ) ;
#40416=AXIS2_PLACEMENT_3D ( 'NONE', #30037, #34146, #3583 ) ;
#40417=EDGE_CURVE ( 'NONE', #23271, #26141, #27334, .T. ) ;
#40425=ORIENTED_EDGE ( 'NONE', *, *, #38912, .F. ) ;
#40441=CIRCLE ( 'NONE', #13300, 47.49899999999999523 ) ;
#40442=ORIENTED_EDGE ( 'NONE', *, *, #21797, .F. ) ;
#40443=DIRECTION ( 'NONE',  ( -1.000000000000000000, -0.000000000000000000, 0.000000000000000000 ) ) ;
#40453=ORIENTED_EDGE ( 'NONE', *, *, #28716, .T. ) ;
#40464=VERTEX_POINT ( 'NONE', #25770 ) ;
#40468=CARTESIAN_POINT ( 'NONE',  ( 18.00000000000000355, 39.78933988720149273, -24.98727647984960498 ) ) ;
#40481=DIRECTION ( 'NONE',  ( 1.000000000000000000, 0.000000000000000000, -0.000000000000000000 ) ) ;
#40492=FACE_OUTER_BOUND ( 'NONE', #40009, .T. ) ;
#40496=VERTEX_POINT ( 'NONE', #29031 ) ;
#40498=FACE_OUTER_BOUND ( 'NONE', #35797, .T. ) ;
#40500=ORIENTED_EDGE ( 'NONE', *, *, #19004, .F. ) ;
#40501=CARTESIAN_POINT ( 'NONE',  ( 0.000000000000000000, 5.871425383721554425, 51.66745943012284670 ) ) ;
#40503=DIRECTION ( 'NONE',  ( 0.000000000000000000, 0.000000000000000000, 1.000000000000000000 ) ) ;
#40505=DIRECTION ( 'NONE',  ( 0.000000000000000000, -0.3681245526846854133, 0.9297764858882485717 ) ) ;
#40509=EDGE_CURVE ( 'NONE', #36319, #15350, #12028, .T. ) ;
#40516=DIRECTION ( 'NONE',  ( 0.000000000000000000, 0.000000000000000000, 1.000000000000000000 ) ) ;
#40517=ORIENTED_EDGE ( 'NONE', *, *, #8687, .T. ) ;
#40520=CARTESIAN_POINT ( 'NONE',  ( 0.000000000000000000, -44.25018368420722936, -27.31155879685226395 ) ) ;
#40539=AXIS2_PLACEMENT_3D ( 'NONE', #12646, #19852, #22489 ) ;
#40551=ORIENTED_EDGE ( 'NONE', *, *, #30393, .T. ) ;
#40556=ADVANCED_FACE ( 'NONE', ( #15319 ), #25347, .T. ) ;
#40569=CIRCLE ( 'NONE', #42684, 20.00000000000001066 ) ;
#40572=EDGE_LOOP ( 'NONE', ( #12902, #30984, #38436, #5946 ) ) ;
#40575=CIRCLE ( 'NONE', #5742, 51.99999999999999289 ) ;
#40581=DIRECTION ( 'NONE',  ( 0.000000000000000000, -0.6845471059286792892, -0.7289686274214203232 ) ) ;
#40584=DIRECTION ( 'NONE',  ( -1.000000000000000000, 0.000000000000000000, -0.000000000000000000 ) ) ;
#40586=ORIENTED_EDGE ( 'NONE', *, *, #2149, .T. ) ;
#40589=EDGE_CURVE ( 'NONE', #11369, #27530, #22714, .T. ) ;
#40596=EDGE_CURVE ( 'NONE', #35106, #30536, #11252, .T. ) ;
#40603=ORIENTED_EDGE ( 'NONE', *, *, #32844, .F. ) ;
#40605=CARTESIAN_POINT ( 'NONE',  ( 18.00000000000000355, 42.60732521687599217, -19.80331771201614544 ) ) ;
#40606=EDGE_LOOP ( 'NONE', ( #1338, #36585, #34651, #20860 ) ) ;
#40607=DIRECTION ( 'NONE',  ( 0.000000000000000000, 0.9048270524660175784, 0.4257792915650767673 ) ) ;
#40623=EDGE_CURVE ( 'NONE', #23910, #14276, #36182, .T. ) ;
#40626=CARTESIAN_POINT ( 'NONE',  ( 18.00000000000000355, 0.000000000000000000, 0.000000000000000000 ) ) ;
#40629=VERTEX_POINT ( 'NONE', #3867 ) ;
#40636=EDGE_LOOP ( 'NONE', ( #14358, #1217, #18812, #7984 ) ) ;
#40637=AXIS2_PLACEMENT_3D ( 'NONE', #1305, #27085, #638 ) ;
#40641=ORIENTED_EDGE ( 'NONE', *, *, #20669, .T. ) ;
#40650=CARTESIAN_POINT ( 'NONE',  ( 18.00000000000000355, 0.000000000000000000, 0.000000000000000000 ) ) ;
#40654=CARTESIAN_POINT ( 'NONE',  ( 18.00000000000000355, -51.19683565102437228, -9.104066087303984034 ) ) ;
#40664=CARTESIAN_POINT ( 'NONE',  ( 18.00000000000000355, -0.2227391519119825691, 46.98410307550729215 ) ) ;
#40665=ORIENTED_EDGE ( 'NONE', *, *, #36948, .F. ) ;
#40670=ORIENTED_EDGE ( 'NONE', *, *, #7350, .T. ) ;
#40672=CARTESIAN_POINT ( 'NONE',  ( 0.000000000000000000, -30.93515269692088765, -36.04401931830283701 ) ) ;
#40680=CARTESIAN_POINT ( 'NONE',  ( 0.000000000000000000, -46.87740477351715640, 16.82754413119429771 ) ) ;
#40683=ORIENTED_EDGE ( 'NONE', *, *, #23392, .T. ) ;
#40685=DIRECTION ( 'NONE',  ( -1.000000000000000000, -0.000000000000000000, 0.000000000000000000 ) ) ;
#40688=CARTESIAN_POINT ( 'NONE',  ( 18.00000000000000355, -27.79676263918213763, 37.88001506494759241 ) ) ;
#40692=VERTEX_POINT ( 'NONE', #39875 ) ;
#40700=DIRECTION ( 'NONE',  ( 0.000000000000000000, 0.9048270524660205760, -0.4257792915650702170 ) ) ;
#40702=AXIS2_PLACEMENT_3D ( 'NONE', #20093, #9353, #151 ) ;
#40706=ORIENTED_EDGE ( 'NONE', *, *, #19605, .T. ) ;
#40712=CARTESIAN_POINT ( 'NONE',  ( 18.00000000000000355, -46.11014828289837197, -9.022736828081200144 ) ) ;
#40713=ORIENTED_EDGE ( 'NONE', *, *, #40740, .F. ) ;
#40726=DIRECTION ( 'NONE',  ( -1.000000000000000000, -0.000000000000000000, 0.000000000000000000 ) ) ;
#40730=ADVANCED_FACE ( 'NONE', ( #29669 ), #20097, .T. ) ;
#40736=CIRCLE ( 'NONE', #332, 51.99999999999999289 ) ;
#40738=CARTESIAN_POINT ( 'NONE',  ( -10.00000000000000000, 0.000000000000000000, 0.000000000000000000 ) ) ;
#40740=EDGE_CURVE ( 'NONE', #27094, #9333, #30743, .T. ) ;
#40743=CARTESIAN_POINT ( 'NONE',  ( 18.00000000000000355, -46.90537658765328644, -2.727856614654796452 ) ) ;
#40753=EDGE_CURVE ( 'NONE', #31904, #25141, #38385, .T. ) ;
#40760=AXIS2_PLACEMENT_3D ( 'NONE', #2058, #32178, #14986 ) ;
#40763=DIRECTION ( 'NONE',  ( 0.000000000000000000, 0.000000000000000000, 1.000000000000000000 ) ) ;
#40764=CIRCLE ( 'NONE', #27570, 47.49900000000000233 ) ;
#40767=VERTEX_POINT ( 'NONE', #41386 ) ;
#40802=EDGE_LOOP ( 'NONE', ( #43042, #6983, #7005, #29507 ) ) ;
#40807=VECTOR ( 'NONE', #24824, 1000.000000000000000 ) ;
#40808=DIRECTION ( 'NONE',  ( 0.000000000000000000, 0.9048270524660175784, 0.4257792915650768784 ) ) ;
#40810=VECTOR ( 'NONE', #41522, 1000.000000000000000 ) ;
#40819=DIRECTION ( 'NONE',  ( -1.000000000000000000, 0.000000000000000000, 0.000000000000000000 ) ) ;
#40824=DIRECTION ( 'NONE',  ( 0.000000000000000000, -0.3681245526846654292, -0.9297764858882562322 ) ) ;
#40833=AXIS2_PLACEMENT_3D ( 'NONE', #2310, #28975, #18771 ) ;
#40836=COLOUR_RGB ( '', 0.72549020, 0.75294118, 0.79215686) ;
#40838=ORIENTED_EDGE ( 'NONE', *, *, #33933, .T. ) ;
#40841=ORIENTED_EDGE ( 'NONE', *, *, #24981, .F. ) ;
#40868=ORIENTED_EDGE ( 'NONE', *, *, #24741, .T. ) ;
#40871=CIRCLE ( 'NONE', #30440, 20.00000000000000711 ) ;
#40876=ORIENTED_EDGE ( 'NONE', *, *, #16727, .F. ) ;
#40878=EDGE_CURVE ( 'NONE', #2459, #42969, #26566, .T. ) ;
#40886=FACE_OUTER_BOUND ( 'NONE', #21465, .T. ) ;
#40891=EDGE_LOOP ( 'NONE', ( #18011, #9505, #10096, #33764 ) ) ;
#40897=LINE ( 'NONE', #966, #33516 ) ;
#40899=ORIENTED_EDGE ( 'NONE', *, *, #11919, .T. ) ;
#40911=DIRECTION ( 'NONE',  ( -1.000000000000000000, 0.000000000000000000, 0.000000000000000000 ) ) ;
#40913=AXIS2_PLACEMENT_3D ( 'NONE', #33665, #3750, #17133 ) ;
#40918=CARTESIAN_POINT ( 'NONE',  ( 0.000000000000000000, -15.49408907645202937, 44.90087086784588166 ) ) ;
#40928=EDGE_LOOP ( 'NONE', ( #37146, #11883, #41566, #15821 ) ) ;
#40929=CARTESIAN_POINT ( 'NONE',  ( 18.00000000000000355, -44.75336757549769118, -14.30704879393654316 ) ) ;
#40933=DIRECTION ( 'NONE',  ( -1.000000000000000000, 0.000000000000000000, 0.000000000000000000 ) ) ;
#40957=FACE_OUTER_BOUND ( 'NONE', #7036, .T. ) ;
#40958=DIRECTION ( 'NONE',  ( -1.000000000000000000, 0.000000000000000000, 0.000000000000000000 ) ) ;
#40968=ADVANCED_FACE ( 'NONE', ( #17460 ), #27463, .T. ) ;
#40977=ORIENTED_EDGE ( 'NONE', *, *, #39760, .T. ) ;
#40985=ADVANCED_FACE ( 'NONE', ( #36287 ), #9254, .T. ) ;
#40986=EDGE_CURVE ( 'NONE', #42969, #38699, #28702, .T. ) ;
#40997=CARTESIAN_POINT ( 'NONE',  ( 0.000000000000000000, -46.11014828289837197, -9.022736828081200144 ) ) ;
#41005=ORIENTED_EDGE ( 'NONE', *, *, #25557, .F. ) ;
#41011=ORIENTED_EDGE ( 'NONE', *, *, #40878, .T. ) ;
#41017=AXIS2_PLACEMENT_3D ( 'NONE', #38419, #31900, #29269 ) ;
#41023=CARTESIAN_POINT ( 'NONE',  ( 9.000000000000001776, 18.53613841426857434, -48.58406706613883586 ) ) ;
#41033=EDGE_CURVE ( 'NONE', #16426, #41981, #28018, .T. ) ;
#41034=CARTESIAN_POINT ( 'NONE',  ( 0.000000000000000000, 19.44205635905601426, -43.33776004284588623 ) ) ;
#41042=ORIENTED_EDGE ( 'NONE', *, *, #15339, .T. ) ;
#41045=DIRECTION ( 'NONE',  ( -1.000000000000000000, 0.000000000000000000, -0.000000000000000000 ) ) ;
#41072=CIRCLE ( 'NONE', #14653, 47.49900000000000233 ) ;
#41077=ORIENTED_EDGE ( 'NONE', *, *, #34010, .F. ) ;
#41082=EDGE_CURVE ( 'NONE', #17739, #3818, #26599, .T. ) ;
#41089=EDGE_CURVE ( 'NONE', #2260, #12961, #25669, .T. ) ;
#41096=ADVANCED_FACE ( 'NONE', ( #39562 ), #2684, .T. ) ;
#41104=AXIS2_PLACEMENT_3D ( 'NONE', #15091, #1307, #8074 ) ;
#41105=FACE_OUTER_BOUND ( 'NONE', #15794, .T. ) ;
#41106=DIRECTION ( 'NONE',  ( -1.000000000000000000, 0.000000000000000000, 0.000000000000000000 ) ) ;
#41109=DIRECTION ( 'NONE',  ( -1.000000000000000000, -0.000000000000000000, -0.000000000000000000 ) ) ;
#41121=AXIS2_PLACEMENT_3D ( 'NONE', #17732, #14664, #27524 ) ;
#41125=VERTEX_POINT ( 'NONE', #17783 ) ;
#41127=VERTEX_POINT ( 'NONE', #4201 ) ;
#41131=ORIENTED_EDGE ( 'NONE', *, *, #1278, .T. ) ;
#41133=CYLINDRICAL_SURFACE ( 'NONE', #5287, 20.00000000000000711 ) ;
#41139=VERTEX_POINT ( 'NONE', #6844 ) ;
#41145=ORIENTED_EDGE ( 'NONE', *, *, #29593, .T. ) ;
#41148=DIRECTION ( 'NONE',  ( -1.000000000000000000, 0.000000000000000000, 0.000000000000000000 ) ) ;
#41154=DIRECTION ( 'NONE',  ( 0.000000000000000000, -0.9048270524660235736, 0.4257792915650639998 ) ) ;
#41155=CIRCLE ( 'NONE', #762, 47.49900000000000233 ) ;
#41157=DIRECTION ( 'NONE',  ( 0.000000000000000000, -0.9822872507286865007, -0.1873813145857355367 ) ) ;
#41166=CARTESIAN_POINT ( 'NONE',  ( 18.00000000000000355, -45.78515115856051665, 12.64416602183649374 ) ) ;
#41171=DIRECTION ( 'NONE',  ( 0.000000000000000000, 0.000000000000000000, -1.000000000000000000 ) ) ;
#41174=AXIS2_PLACEMENT_3D ( 'NONE', #3651, #17020, #16601 ) ;
#41179=VERTEX_POINT ( 'NONE', #7259 ) ;
#41180=DIRECTION ( 'NONE',  ( 0.000000000000000000, 0.000000000000000000, -1.000000000000000000 ) ) ;
#41190=EDGE_CURVE ( 'NONE', #16540, #36319, #14065, .T. ) ;
#41192=CIRCLE ( 'NONE', #38407, 52.00000000000000000 ) ;
#41198=CARTESIAN_POINT ( 'NONE',  ( 18.00000000000000355, 18.53613841426857434, -48.58406706613882875 ) ) ;
#41207=DIRECTION ( 'NONE',  ( -1.000000000000000000, -0.000000000000000000, 0.000000000000000000 ) ) ;
#41210=CARTESIAN_POINT ( 'NONE',  ( 18.00000000000000355, 51.93417535146740960, -2.615612846549368431 ) ) ;
#41220=ORIENTED_EDGE ( 'NONE', *, *, #41715, .F. ) ;
#41227=EDGE_CURVE ( 'NONE', #4417, #15422, #11985, .T. ) ;
#41232=CIRCLE ( 'NONE', #23188, 20.00000000000000711 ) ;
#41236=DIRECTION ( 'NONE',  ( 1.000000000000000000, -0.000000000000000000, 0.000000000000000000 ) ) ;
#41247=CARTESIAN_POINT ( 'NONE',  ( 18.00000000000000355, 46.21320724403663860, -10.97699764141904843 ) ) ;
#41248=DIRECTION ( 'NONE',  ( 0.000000000000000000, 0.2486898871648482723, 0.9685831611286327414 ) ) ;
#41249=CARTESIAN_POINT ( 'NONE',  ( 18.00000000000000355, 38.92705108641770551, -27.21837053747755419 ) ) ;
#41256=LINE ( 'NONE', #7891, #22984 ) ;
#41258=AXIS2_PLACEMENT_3D ( 'NONE', #19725, #16021, #29522 ) ;
#41269=CARTESIAN_POINT ( 'NONE',  ( 0.000000000000000000, 0.000000000000000000, 0.000000000000000000 ) ) ;
#41275=DIRECTION ( 'NONE',  ( -1.000000000000000000, -0.000000000000000000, -0.000000000000000000 ) ) ;
#41283=CARTESIAN_POINT ( 'NONE',  ( 9.000000000000001776, 24.47917365150009061, -45.87777302070909258 ) ) ;
#41292=CARTESIAN_POINT ( 'NONE',  ( 18.00000000000000355, 5.871425383722275626, -51.66745943012274722 ) ) ;
#41298=EDGE_CURVE ( 'NONE', #26596, #36818, #38016, .T. ) ;
#41303=DIRECTION ( 'NONE',  ( -1.000000000000000000, -0.000000000000000000, 0.000000000000000000 ) ) ;
#41304=ORIENTED_EDGE ( 'NONE', *, *, #11419, .T. ) ;
#41309=DIRECTION ( 'NONE',  ( 0.000000000000000000, 0.000000000000000000, 1.000000000000000000 ) ) ;
#41318=DIRECTION ( 'NONE',  ( 0.000000000000000000, 0.000000000000000000, -1.000000000000000000 ) ) ;
#41323=CARTESIAN_POINT ( 'NONE',  ( 18.00000000000000355, -27.43636312076294814, -38.14186064215179073 ) ) ;
#41338=AXIS2_PLACEMENT_3D ( 'NONE', #8790, #32139, #35802 ) ;
#41347=ORIENTED_EDGE ( 'NONE', *, *, #42719, .F. ) ;
#41362=DIRECTION ( 'NONE',  ( -1.000000000000000000, 0.000000000000000000, 0.000000000000000000 ) ) ;
#41370=ORIENTED_EDGE ( 'NONE', *, *, #21188, .F. ) ;
#41371=CARTESIAN_POINT ( 'NONE',  ( 18.00000000000000355, 0.000000000000000000, 0.000000000000000000 ) ) ;
#41373=AXIS2_PLACEMENT_3D ( 'NONE', #8956, #5670, #22305 ) ;
#41386=CARTESIAN_POINT ( 'NONE',  ( 18.00000000000000355, 13.56094713063641244, -50.20060470671726449 ) ) ;
#41390=ORIENTED_EDGE ( 'NONE', *, *, #39601, .F. ) ;
#41392=DIRECTION ( 'NONE',  ( 1.000000000000000000, -0.000000000000000000, -0.000000000000000000 ) ) ;
#41395=ORIENTED_EDGE ( 'NONE', *, *, #1278, .F. ) ;
#41406=VECTOR ( 'NONE', #38778, 1000.000000000000000 ) ;
#41414=CARTESIAN_POINT ( 'NONE',  ( 0.000000000000000000, 0.000000000000000000, 0.000000000000000000 ) ) ;
#41429=ORIENTED_EDGE ( 'NONE', *, *, #39159, .F. ) ;
#41432=ORIENTED_EDGE ( 'NONE', *, *, #13797, .T. ) ;
#41438=DIRECTION ( 'NONE',  ( -1.000000000000000000, -0.000000000000000000, -0.000000000000000000 ) ) ;
#41443=AXIS2_PLACEMENT_3D ( 'NONE', #3141, #3573, #16516 ) ;
#41445=ORIENTED_EDGE ( 'NONE', *, *, #19734, .F. ) ;
#41446=DIRECTION ( 'NONE',  ( 0.000000000000000000, 0.000000000000000000, 1.000000000000000000 ) ) ;
#41450=CARTESIAN_POINT ( 'NONE',  ( 18.00000000000000355, -17.50309955389642269, 43.60271849949357659 ) ) ;
#41454=DIRECTION ( 'NONE',  ( 0.000000000000000000, 0.000000000000000000, 1.000000000000000000 ) ) ;
#41457=EDGE_CURVE ( 'NONE', #28923, #13830, #3601, .T. ) ;
#41469=LINE ( 'NONE', #11187, #21884 ) ;
#41494=AXIS2_PLACEMENT_3D ( 'NONE', #10849, #23957, #33322 ) ;
#41495=CARTESIAN_POINT ( 'NONE',  ( 18.00000000000000355, -36.06787431788703913, 37.45808914225474950 ) ) ;
#41496=EDGE_LOOP ( 'NONE', ( #13674, #28506, #19137, #2729 ) ) ;
#41508=VECTOR ( 'NONE', #23554, 1000.000000000000000 ) ;
#41522=DIRECTION ( 'NONE',  ( -1.000000000000000000, -0.000000000000000000, 0.000000000000000000 ) ) ;
#41524=VECTOR ( 'NONE', #24436, 1000.000000000000000 ) ;
#41537=ADVANCED_FACE ( 'NONE', ( #42995 ), #15779, .T. ) ;
#41541=EDGE_LOOP ( 'NONE', ( #39030, #1824, #20086, #34095 ) ) ;
#41566=ORIENTED_EDGE ( 'NONE', *, *, #33457, .F. ) ;
#41583=ORIENTED_EDGE ( 'NONE', *, *, #2075, .T. ) ;
#41587=DIRECTION ( 'NONE',  ( 0.000000000000000000, 0.3681245526846786964, -0.9297764858882511252 ) ) ;
#41589=CARTESIAN_POINT ( 'NONE',  ( 18.00000000000000355, -44.47301969247432396, -16.68249143361957465 ) ) ;
#41595=VECTOR ( 'NONE', #33391, 1000.000000000000000 ) ;
#41601=ORIENTED_EDGE ( 'NONE', *, *, #22669, .F. ) ;
#41604=CIRCLE ( 'NONE', #19347, 51.99999999999999289 ) ;
#41606=AXIS2_PLACEMENT_3D ( 'NONE', #33191, #29290, #26657 ) ;
#41610=CARTESIAN_POINT ( 'NONE',  ( 18.00000000000000355, 31.08872492059957793, 41.68322423723109438 ) ) ;
#41618=DIRECTION ( 'NONE',  ( 0.000000000000000000, 0.9510565162951544194, -0.3090169943749448422 ) ) ;
#41625=AXIS2_PLACEMENT_3D ( 'NONE', #30662, #10140, #76 ) ;
#41633=CIRCLE ( 'NONE', #33972, 20.00000000000000711 ) ;
#41643=FACE_OUTER_BOUND ( 'NONE', #7286, .T. ) ;
#41646=ADVANCED_FACE ( 'NONE', ( #26658 ), #653, .T. ) ;
#41647=CYLINDRICAL_SURFACE ( 'NONE', #22625, 20.00000000000000711 ) ;
#41654=AXIS2_PLACEMENT_3D ( 'NONE', #36699, #23017, #33646 ) ;
#41655=CARTESIAN_POINT ( 'NONE',  ( 18.00000000000000355, 0.000000000000000000, 0.000000000000000000 ) ) ;
#41657=DIRECTION ( 'NONE',  ( -1.000000000000000000, 0.000000000000000000, 0.000000000000000000 ) ) ;
#41665=AXIS2_PLACEMENT_3D ( 'NONE', #22857, #70, #13441 ) ;
#41667=FACE_OUTER_BOUND ( 'NONE', #688, .T. ) ;
#41671=DIRECTION ( 'NONE',  ( 0.000000000000000000, 0.000000000000000000, 1.000000000000000000 ) ) ;
#41674=DIRECTION ( 'NONE',  ( 1.000000000000000000, -0.000000000000000000, -0.000000000000000000 ) ) ;
#41686=FACE_OUTER_BOUND ( 'NONE', #40636, .T. ) ;
#41688=VECTOR ( 'NONE', #12059, 1000.000000000000000 ) ;
#41698=CARTESIAN_POINT ( 'NONE',  ( 18.00000000000000355, 26.17370628620709638, -39.63700417846136048 ) ) ;
#41707=CARTESIAN_POINT ( 'NONE',  ( 0.000000000000000000, -47.49120266317494554, -0.8606222198180160099 ) ) ;
#41712=VERTEX_POINT ( 'NONE', #16657 ) ;
#41715=EDGE_CURVE ( 'NONE', #16239, #25951, #40575, .T. ) ;
#41716=ORIENTED_EDGE ( 'NONE', *, *, #5330, .F. ) ;
#41722=ORIENTED_EDGE ( 'NONE', *, *, #27984, .F. ) ;
#41724=DIRECTION ( 'NONE',  ( -1.000000000000000000, 0.000000000000000000, 0.000000000000000000 ) ) ;
#41729=CYLINDRICAL_SURFACE ( 'NONE', #20818, 51.99999999999999289 ) ;
#41733=DIRECTION ( 'NONE',  ( 0.000000000000000000, 0.000000000000000000, 1.000000000000000000 ) ) ;
#41739=ORIENTED_EDGE ( 'NONE', *, *, #6752, .T. ) ;
#41744=CARTESIAN_POINT ( 'NONE',  ( 18.00000000000000355, 0.000000000000000000, 0.000000000000000000 ) ) ;
#41748=EDGE_CURVE ( 'NONE', #1441, #30171, #32226, .T. ) ;
#41752=EDGE_LOOP ( 'NONE', ( #21565, #16041, #36291, #9579 ) ) ;
#41756=FACE_OUTER_BOUND ( 'NONE', #22779, .T. ) ;
#41778=CARTESIAN_POINT ( 'NONE',  ( 0.000000000000000000, 13.85708833600031298, -45.43276465116649376 ) ) ;
#41784=EDGE_CURVE ( 'NONE', #2747, #8333, #34475, .T. ) ;
#41788=ORIENTED_EDGE ( 'NONE', *, *, #7271, .T. ) ;
#41790=EDGE_CURVE ( 'NONE', #12306, #2405, #5061, .T. ) ;
#41791=CARTESIAN_POINT ( 'NONE',  ( 0.000000000000000000, -35.20873326984102647, 31.88259874184018372 ) ) ;
#41794=DIRECTION ( 'NONE',  ( 0.000000000000000000, 0.000000000000000000, 1.000000000000000000 ) ) ;
#41805=AXIS2_PLACEMENT_3D ( 'NONE', #10487, #6544, #42982 ) ;
#41807=VERTEX_POINT ( 'NONE', #34917 ) ;
#41808=CARTESIAN_POINT ( 'NONE',  ( 0.000000000000000000, 39.55064067543099071, -25.36340625197318488 ) ) ;
#41810=DIRECTION ( 'NONE',  ( 0.000000000000000000, 0.9822872507286879440, 0.1873813145857285145 ) ) ;
#41817=CARTESIAN_POINT ( 'NONE',  ( 0.000000000000000000, 0.000000000000000000, 0.000000000000000000 ) ) ;
#41821=EDGE_LOOP ( 'NONE', ( #8376, #31632, #5903, #23816 ) ) ;
#41827=CARTESIAN_POINT ( 'NONE',  ( 18.00000000000000355, -6.109652351742118626, 46.58570277113506819 ) ) ;
#41828=VERTEX_POINT ( 'NONE', #5029 ) ;
#41831=CIRCLE ( 'NONE', #6321, 47.49900000000000233 ) ;
#41832=CARTESIAN_POINT ( 'NONE',  ( 18.00000000000000355, -32.00046193115174731, 34.40241257139675923 ) ) ;
#41837=DIRECTION ( 'NONE',  ( 0.000000000000000000, 0.000000000000000000, 1.000000000000000000 ) ) ;
#41855=ORIENTED_EDGE ( 'NONE', *, *, #15432, .F. ) ;
#41856=DIRECTION ( 'NONE',  ( -1.000000000000000000, 0.000000000000000000, 0.000000000000000000 ) ) ;
#41880=DIRECTION ( 'NONE',  ( 0.000000000000000000, 0.000000000000000000, 1.000000000000000000 ) ) ;
#41882=DIRECTION ( 'NONE',  ( 0.000000000000000000, 0.000000000000000000, 1.000000000000000000 ) ) ;
#41884=CARTESIAN_POINT ( 'NONE',  ( 18.00000000000000355, 0.000000000000000000, 0.000000000000000000 ) ) ;
#41891=AXIS2_PLACEMENT_3D ( 'NONE', #9194, #12069, #15768 ) ;
#41894=CIRCLE ( 'NONE', #37690, 20.00000000000000711 ) ;
#41898=AXIS2_PLACEMENT_3D ( 'NONE', #23461, #3543, #17132 ) ;
#41901=CYLINDRICAL_SURFACE ( 'NONE', #36070, 51.99999999999999289 ) ;
#41903=CARTESIAN_POINT ( 'NONE',  ( 9.000000000000001776, -19.74581912682808849, -48.10512059033413834 ) ) ;
#41906=ORIENTED_EDGE ( 'NONE', *, *, #15135, .F. ) ;
#41911=EDGE_LOOP ( 'NONE', ( #21995, #18692, #31682, #33462 ) ) ;
#41921=CARTESIAN_POINT ( 'NONE',  ( 0.000000000000000000, -37.91532898920940653, 28.61088654061626357 ) ) ;
#41925=DIRECTION ( 'NONE',  ( 0.000000000000000000, 0.000000000000000000, 1.000000000000000000 ) ) ;
#41933=ADVANCED_FACE ( 'NONE', ( #5874 ), #42517, .T. ) ;
#41945=AXIS2_PLACEMENT_3D ( 'NONE', #2999, #29672, #25772 ) ;
#41946=AXIS2_PLACEMENT_3D ( 'NONE', #20348, #40146, #4144 ) ;
#41949=ORIENTED_EDGE ( 'NONE', *, *, #26526, .T. ) ;
#41960=DIRECTION ( 'NONE',  ( 0.000000000000000000, 0.000000000000000000, -1.000000000000000000 ) ) ;
#41963=DIRECTION ( 'NONE',  ( 0.000000000000000000, 0.000000000000000000, 1.000000000000000000 ) ) ;
#41964=VERTEX_POINT ( 'NONE', #29038 ) ;
#41978=CARTESIAN_POINT ( 'NONE',  ( 0.000000000000000000, 44.25018368420743542, 27.31155879685196552 ) ) ;
#41981=VERTEX_POINT ( 'NONE', #26184 ) ;
#41991=CARTESIAN_POINT ( 'NONE',  ( -10.00000000000000000, 0.000000000000000000, 0.000000000000000000 ) ) ;
#41992=EDGE_CURVE ( 'NONE', #28304, #15576, #12772, .T. ) ;
#42000=EDGE_CURVE ( 'NONE', #33321, #36878, #3001, .T. ) ;
#42012=FACE_OUTER_BOUND ( 'NONE', #15952, .T. ) ;
#42024=DIRECTION ( 'NONE',  ( -1.000000000000000000, 0.000000000000000000, 0.000000000000000000 ) ) ;
#42035=LINE ( 'NONE', #12190, #9423 ) ;
#42037=VERTEX_POINT ( 'NONE', #43166 ) ;
#42044=EDGE_CURVE ( 'NONE', #27751, #42728, #35051, .T. ) ;
#42064=CARTESIAN_POINT ( 'NONE',  ( 0.000000000000000000, 0.000000000000000000, 0.000000000000000000 ) ) ;
#42070=EDGE_LOOP ( 'NONE', ( #22155, #31040, #31095, #39364 ) ) ;
#42071=CARTESIAN_POINT ( 'NONE',  ( 18.00000000000000355, -2.123073309834832667, -47.45152853935337589 ) ) ;
#42073=VERTEX_POINT ( 'NONE', #30107 ) ;
#42076=CARTESIAN_POINT ( 'NONE',  ( -10.00000000000000000, 0.000000000000000000, 0.000000000000000000 ) ) ;
#42077=DIRECTION ( 'NONE',  ( -1.000000000000000000, -0.000000000000000000, -0.000000000000000000 ) ) ;
#42078=CIRCLE ( 'NONE', #15650, 47.49900000000000233 ) ;
#42079=ORIENTED_EDGE ( 'NONE', *, *, #14431, .T. ) ;
#42097=ADVANCED_FACE ( 'NONE', ( #13530 ), #40322, .T. ) ;
#42100=DIRECTION ( 'NONE',  ( -1.000000000000000000, 0.000000000000000000, -0.000000000000000000 ) ) ;
#42109=VECTOR ( 'NONE', #13978, 1000.000000000000000 ) ;
#42119=DIRECTION ( 'NONE',  ( 0.000000000000000000, 0.000000000000000000, 1.000000000000000000 ) ) ;
#42123=CYLINDRICAL_SURFACE ( 'NONE', #26136, 20.00000000000000355 ) ;
#42126=DIRECTION ( 'NONE',  ( -1.000000000000000000, 0.000000000000000000, 0.000000000000000000 ) ) ;
#42135=CARTESIAN_POINT ( 'NONE',  ( 18.00000000000000355, 8.053585752061904302, 46.81126742072025593 ) ) ;
#42150=VERTEX_POINT ( 'NONE', #23581 ) ;
#42167=VERTEX_POINT ( 'NONE', #37915 ) ;
#42169=EDGE_CURVE ( 'NONE', #22999, #1479, #42689, .T. ) ;
#42177=CARTESIAN_POINT ( 'NONE',  ( 18.00000000000000355, -47.49120266317495975, 0.8606222198173691940 ) ) ;
#42181=AXIS2_PLACEMENT_3D ( 'NONE', #14694, #11407, #11197 ) ;
#42191=ORIENTED_EDGE ( 'NONE', *, *, #34321, .F. ) ;
#42199=AXIS2_PLACEMENT_3D ( 'NONE', #2098, #34408, #41157 ) ;
#42200=CIRCLE ( 'NONE', #29684, 47.49899999999999523 ) ;
#42208=FACE_OUTER_BOUND ( 'NONE', #8711, .T. ) ;
#42210=AXIS2_PLACEMENT_3D ( 'NONE', #8275, #25117, #15493 ) ;
#42215=ORIENTED_EDGE ( 'NONE', *, *, #41190, .F. ) ;
#42227=ORIENTED_EDGE ( 'NONE', *, *, #35064, .T. ) ;
#42234=EDGE_CURVE ( 'NONE', #952, #18374, #32952, .T. ) ;
#42235=DIRECTION ( 'NONE',  ( 0.000000000000000000, -0.4817536741017036661, -0.8763066800438700232 ) ) ;
#42239=DIRECTION ( 'NONE',  ( 0.000000000000000000, 0.000000000000000000, 1.000000000000000000 ) ) ;
#42248=ORIENTED_EDGE ( 'NONE', *, *, #37767, .F. ) ;
#42252=DIRECTION ( 'NONE',  ( 0.000000000000000000, 0.000000000000000000, -1.000000000000000000 ) ) ;
#42253=CARTESIAN_POINT ( 'NONE',  ( 0.000000000000000000, 0.000000000000000000, 0.000000000000000000 ) ) ;
#42257=ORIENTED_EDGE ( 'NONE', *, *, #30693, .F. ) ;
#42263=AXIS2_PLACEMENT_3D ( 'NONE', #11746, #15248, #18952 ) ;
#42272=AXIS2_PLACEMENT_3D ( 'NONE', #4338, #8649, #37724 ) ;
#42276=CARTESIAN_POINT ( 'NONE',  ( 18.00000000000000355, 0.6505223195690489346, -51.99593080916756804 ) ) ;
#42278=FACE_OUTER_BOUND ( 'NONE', #26387, .T. ) ;
#42280=DIRECTION ( 'NONE',  ( 0.000000000000000000, 0.000000000000000000, 1.000000000000000000 ) ) ;
#42281=AXIS2_PLACEMENT_3D ( 'NONE', #8402, #41109, #38070 ) ;
#42289=VERTEX_POINT ( 'NONE', #20964 ) ;
#42291=ORIENTED_EDGE ( 'NONE', *, *, #22685, .T. ) ;
#42305=CARTESIAN_POINT ( 'NONE',  ( 0.000000000000000000, 39.55064067543064965, 25.36340625197373555 ) ) ;
#42310=CARTESIAN_POINT ( 'NONE',  ( 18.00000000000000355, 0.000000000000000000, 0.000000000000000000 ) ) ;
#42316=EDGE_CURVE ( 'NONE', #10423, #17165, #42717, .T. ) ;
#42318=ADVANCED_FACE ( 'NONE', ( #34428 ), #22461, .T. ) ;
#42323=AXIS2_PLACEMENT_3D ( 'NONE', #29532, #35627, #42803 ) ;
#42343=CARTESIAN_POINT ( 'NONE',  ( -10.00000000000000000, 0.000000000000000000, 0.000000000000000000 ) ) ;
#42354=CIRCLE ( 'NONE', #33311, 47.49900000000000233 ) ;
#42366=CIRCLE ( 'NONE', #22938, 51.99999999999999289 ) ;
#42371=EDGE_LOOP ( 'NONE', ( #40295, #27195, #11555, #4964 ) ) ;
#42376=ADVANCED_FACE ( 'NONE', ( #15480 ), #22038, .T. ) ;
#42380=CARTESIAN_POINT ( 'NONE',  ( 0.000000000000000000, 0.000000000000000000, 0.000000000000000000 ) ) ;
#42393=FACE_OUTER_BOUND ( 'NONE', #41821, .T. ) ;
#42422=ORIENTED_EDGE ( 'NONE', *, *, #18277, .F. ) ;
#42432=CARTESIAN_POINT ( 'NONE',  ( 0.000000000000000000, 51.85248208264521708, -3.914090171285657949 ) ) ;
#42434=ORIENTED_EDGE ( 'NONE', *, *, #20110, .F. ) ;
#42443=LINE ( 'NONE', #35889, #6064 ) ;
#42447=DIRECTION ( 'NONE',  ( -1.000000000000000000, 0.000000000000000000, 0.000000000000000000 ) ) ;
#42449=CARTESIAN_POINT ( 'NONE',  ( 9.000000000000001776, -5.871425383721900815, 51.66745943012280406 ) ) ;
#42452=EDGE_CURVE ( 'NONE', #2287, #4247, #39831, .T. ) ;
#42453=CYLINDRICAL_SURFACE ( 'NONE', #18224, 20.00000000000000355 ) ;
#42466=ORIENTED_EDGE ( 'NONE', *, *, #23969, .F. ) ;
#42471=ORIENTED_EDGE ( 'NONE', *, *, #30393, .F. ) ;
#42473=CARTESIAN_POINT ( 'NONE',  ( 18.00000000000000355, 19.44205635905542096, 43.33776004284615624 ) ) ;
#42490=DIRECTION ( 'NONE',  ( 1.000000000000000000, -0.000000000000000000, -0.000000000000000000 ) ) ;
#42491=CARTESIAN_POINT ( 'NONE',  ( 18.00000000000000355, 0.000000000000000000, 0.000000000000000000 ) ) ;
#42505=CIRCLE ( 'NONE', #34866, 47.49900000000000944 ) ;
#42510=AXIS2_PLACEMENT_3D ( 'NONE', #23372, #17276, #3669 ) ;
#42515=FACE_OUTER_BOUND ( 'NONE', #29376, .T. ) ;
#42517=CYLINDRICAL_SURFACE ( 'NONE', #28761, 20.00000000000000355 ) ;
#42520=DIRECTION ( 'NONE',  ( 0.000000000000000000, 0.000000000000000000, 1.000000000000000000 ) ) ;
#42532=CIRCLE ( 'NONE', #2148, 47.49900000000000233 ) ;
#42538=DIRECTION ( 'NONE',  ( 1.000000000000000000, 0.000000000000000000, -0.000000000000000000 ) ) ;
#42539=ORIENTED_EDGE ( 'NONE', *, *, #14566, .F. ) ;
#42541=DIRECTION ( 'NONE',  ( -1.000000000000000000, 0.000000000000000000, -0.000000000000000000 ) ) ;
#42542=AXIS2_PLACEMENT_3D ( 'NONE', #23848, #37113, #30161 ) ;
#42543=ORIENTED_EDGE ( 'NONE', *, *, #13058, .T. ) ;
#42547=CYLINDRICAL_SURFACE ( 'NONE', #6263, 47.49900000000000233 ) ;
#42552=EDGE_CURVE ( 'NONE', #32639, #25151, #26768, .T. ) ;
#42553=ADVANCED_FACE ( 'NONE', ( #36557 ), #6686, .T. ) ;
#42557=DIRECTION ( 'NONE',  ( 0.000000000000000000, 0.000000000000000000, 1.000000000000000000 ) ) ;
#42567=CARTESIAN_POINT ( 'NONE',  ( 18.00000000000000355, -30.03615769709762517, 42.44795908868979950 ) ) ;
#42572=DIRECTION ( 'NONE',  ( 0.000000000000000000, 0.000000000000000000, 1.000000000000000000 ) ) ;
#42588=DIRECTION ( 'NONE',  ( 0.000000000000000000, 0.000000000000000000, 1.000000000000000000 ) ) ;
#42605=DIRECTION ( 'NONE',  ( 0.000000000000000000, 0.000000000000000000, 1.000000000000000000 ) ) ;
#42607=ADVANCED_FACE ( 'NONE', ( #37858 ), #24826, .T. ) ;
#42620=CIRCLE ( 'NONE', #17619, 20.00000000000000711 ) ;
#42623=CARTESIAN_POINT ( 'NONE',  ( 0.000000000000000000, -17.08890430202718491, -43.76671000081963570 ) ) ;
#42631=DIRECTION ( 'NONE',  ( 1.000000000000000000, -0.000000000000000000, -0.000000000000000000 ) ) ;
#42639=CARTESIAN_POINT ( 'NONE',  ( 18.00000000000000355, 0.000000000000000000, 0.000000000000000000 ) ) ;
#42640=ORIENTED_EDGE ( 'NONE', *, *, #11798, .F. ) ;
#42645=CARTESIAN_POINT ( 'NONE',  ( 0.000000000000000000, -19.44205635905570873, 43.33776004284602124 ) ) ;
#42646=DIRECTION ( 'NONE',  ( 1.000000000000000000, -0.000000000000000000, 0.000000000000000000 ) ) ;
#42648=DIRECTION ( 'NONE',  ( 0.000000000000000000, 0.000000000000000000, 1.000000000000000000 ) ) ;
#42661=ORIENTED_EDGE ( 'NONE', *, *, #35849, .F. ) ;
#42663=DIRECTION ( 'NONE',  ( 0.000000000000000000, -0.9510565162951500895, -0.3090169943749581649 ) ) ;
#42666=DIRECTION ( 'NONE',  ( 0.000000000000000000, -0.2486898871648622888, 0.9685831611286290777 ) ) ;
#42668=ORIENTED_EDGE ( 'NONE', *, *, #27910, .F. ) ;
#42670=EDGE_CURVE ( 'NONE', #17165, #17334, #32308, .T. ) ;
#42672=FACE_OUTER_BOUND ( 'NONE', #5861, .T. ) ;
#42674=EDGE_CURVE ( 'NONE', #41139, #27343, #28163, .T. ) ;
#42684=AXIS2_PLACEMENT_3D ( 'NONE', #11097, #1672, #15026 ) ;
#42687=ORIENTED_EDGE ( 'NONE', *, *, #32355, .T. ) ;
#42689=CIRCLE ( 'NONE', #21871, 20.00000000000000711 ) ;
#42690=DIRECTION ( 'NONE',  ( -1.000000000000000000, -0.000000000000000000, -0.000000000000000000 ) ) ;
#42701=CARTESIAN_POINT ( 'NONE',  ( 0.000000000000000000, 0.000000000000000000, 0.000000000000000000 ) ) ;
#42704=ADVANCED_FACE ( 'NONE', ( #983 ), #14334, .T. ) ;
#42709=FACE_OUTER_BOUND ( 'NONE', #17372, .T. ) ;
#42710=DIRECTION ( 'NONE',  ( -1.000000000000000000, 0.000000000000000000, -0.000000000000000000 ) ) ;
#42714=CARTESIAN_POINT ( 'NONE',  ( 18.00000000000000355, -35.20873326984102647, 31.88259874184018372 ) ) ;
#42717=CIRCLE ( 'NONE', #35743, 20.00000000000000711 ) ;
#42719=EDGE_CURVE ( 'NONE', #24437, #36472, #19117, .T. ) ;
#42723=CIRCLE ( 'NONE', #25382, 11.00000000000000000 ) ;
#42728=VERTEX_POINT ( 'NONE', #12359 ) ;
#42744=ORIENTED_EDGE ( 'NONE', *, *, #8051, .F. ) ;
#42745=CARTESIAN_POINT ( 'NONE',  ( 0.000000000000000000, 0.000000000000000000, 0.000000000000000000 ) ) ;
#42748=DIRECTION ( 'NONE',  ( -1.000000000000000000, 0.000000000000000000, 0.000000000000000000 ) ) ;
#42761=FACE_OUTER_BOUND ( 'NONE', #41496, .T. ) ;
#42786=ORIENTED_EDGE ( 'NONE', *, *, #16669, .F. ) ;
#42793=AXIS2_PLACEMENT_3D ( 'NONE', #20468, #13479, #30487 ) ;
#42799=CARTESIAN_POINT ( 'NONE',  ( -10.00000000000000000, 0.000000000000000000, 0.000000000000000000 ) ) ;
#42803=DIRECTION ( 'NONE',  ( 0.000000000000000000, 0.000000000000000000, 1.000000000000000000 ) ) ;
#42813=VERTEX_POINT ( 'NONE', #11933 ) ;
#42817=VECTOR ( 'NONE', #20560, 1000.000000000000000 ) ;
#42818=ORIENTED_EDGE ( 'NONE', *, *, #20357, .T. ) ;
#42819=CARTESIAN_POINT ( 'NONE',  ( 18.00000000000000355, 17.50309955389612426, 43.60271849949370448 ) ) ;
#42825=CARTESIAN_POINT ( 'NONE',  ( 18.00000000000000355, -24.47917365149913849, -45.87777302070959706 ) ) ;
#42827=DIRECTION ( 'NONE',  ( 0.000000000000000000, -0.1253332335643113082, 0.9921147013144769877 ) ) ;
#42830=EDGE_LOOP ( 'NONE', ( #20099, #25728, #19134, #35429 ) ) ;
#42836=CYLINDRICAL_SURFACE ( 'NONE', #17749, 20.00000000000000355 ) ;
#42839=DIRECTION ( 'NONE',  ( 0.000000000000000000, -0.6845471059286791782, -0.7289686274214204342 ) ) ;
#42841=ORIENTED_EDGE ( 'NONE', *, *, #28768, .T. ) ;
#42844=ADVANCED_FACE ( 'NONE', ( #5775 ), #32397, .T. ) ;
#42856=DIRECTION ( 'NONE',  ( 0.000000000000000000, 0.000000000000000000, 1.000000000000000000 ) ) ;
#42862=DIRECTION ( 'NONE',  ( -1.000000000000000000, 0.000000000000000000, 0.000000000000000000 ) ) ;
#42874=DIRECTION ( 'NONE',  ( 0.000000000000000000, 0.000000000000000000, 1.000000000000000000 ) ) ;
#42889=VERTEX_POINT ( 'NONE', #876 ) ;
#42891=CARTESIAN_POINT ( 'NONE',  ( 0.000000000000000000, 0.000000000000000000, 0.000000000000000000 ) ) ;
#42916=ORIENTED_EDGE ( 'NONE', *, *, #18395, .F. ) ;
#42922=ADVANCED_FACE ( 'NONE', ( #30801 ), #13426, .T. ) ;
#42925=LINE ( 'NONE', #3200, #1286 ) ;
#42931=VECTOR ( 'NONE', #33332, 1000.000000000000000 ) ;
#42932=ORIENTED_EDGE ( 'NONE', *, *, #25200, .F. ) ;
#42933=AXIS2_PLACEMENT_3D ( 'NONE', #14158, #3428, #27447 ) ;
#42934=ORIENTED_EDGE ( 'NONE', *, *, #28659, .T. ) ;
#42963=EDGE_CURVE ( 'NONE', #10641, #24221, #11435, .T. ) ;
#42968=DIRECTION ( 'NONE',  ( -1.000000000000000000, -0.000000000000000000, -0.000000000000000000 ) ) ;
#42969=VERTEX_POINT ( 'NONE', #13212 ) ;
#42976=DIRECTION ( 'NONE',  ( -1.000000000000000000, 0.000000000000000000, -0.000000000000000000 ) ) ;
#42982=DIRECTION ( 'NONE',  ( 0.000000000000000000, 0.000000000000000000, 1.000000000000000000 ) ) ;
#42987=DIRECTION ( 'NONE',  ( -1.000000000000000000, -0.000000000000000000, -0.000000000000000000 ) ) ;
#42988=CARTESIAN_POINT ( 'NONE',  ( 0.000000000000000000, -24.47917365149977087, 45.87777302070925600 ) ) ;
#42994=ADVANCED_FACE ( 'NONE', ( #16269 ), #42836, .T. ) ;
#42995=FACE_OUTER_BOUND ( 'NONE', #21690, .T. ) ;
#43005=ORIENTED_EDGE ( 'NONE', *, *, #1747, .F. ) ;
#43011=AXIS2_PLACEMENT_3D ( 'NONE', #35325, #38172, #14860 ) ;
#43013=AXIS2_PLACEMENT_3D ( 'NONE', #6224, #3133, #32840 ) ;
#43015=ORIENTED_EDGE ( 'NONE', *, *, #26800, .T. ) ;
#43024=CARTESIAN_POINT ( 'NONE',  ( 18.00000000000000355, -9.744342220503709129, 46.48873837489794880 ) ) ;
#43034=ORIENTED_EDGE ( 'NONE', *, *, #26346, .T. ) ;
#43042=ORIENTED_EDGE ( 'NONE', *, *, #792, .F. ) ;
#43046=AXIS2_PLACEMENT_3D ( 'NONE', #32197, #28310, #34823 ) ;
#43052=VECTOR ( 'NONE', #9386, 1000.000000000000000 ) ;
#43054=DIRECTION ( 'NONE',  ( 0.000000000000000000, 0.000000000000000000, -1.000000000000000000 ) ) ;
#43057=ORIENTED_EDGE ( 'NONE', *, *, #11020, .T. ) ;
#43059=EDGE_LOOP ( 'NONE', ( #41739, #29361, #13017, #40899 ) ) ;
#43065=ORIENTED_EDGE ( 'NONE', *, *, #9955, .F. ) ;
#43070=CARTESIAN_POINT ( 'NONE',  ( 18.00000000000000355, 37.91532898920961969, -28.61088654061597936 ) ) ;
#43073=AXIS2_PLACEMENT_3D ( 'NONE', #5008, #5439, #5215 ) ;
#43074=DIRECTION ( 'NONE',  ( 0.000000000000000000, -0.2486898871648622611, 0.9685831611286290777 ) ) ;
#43076=EDGE_CURVE ( 'NONE', #22654, #21903, #8314, .T. ) ;
#43085=DIRECTION ( 'NONE',  ( -1.000000000000000000, -0.000000000000000000, -0.000000000000000000 ) ) ;
#43093=DIRECTION ( 'NONE',  ( -1.000000000000000000, -0.000000000000000000, -0.000000000000000000 ) ) ;
#43098=DIRECTION ( 'NONE',  ( -1.000000000000000000, 0.000000000000000000, 0.000000000000000000 ) ) ;
#43102=EDGE_CURVE ( 'NONE', #4953, #31904, #18392, .T. ) ;
#43106=CARTESIAN_POINT ( 'NONE',  ( 0.000000000000000000, -42.03146605346801579, 22.12489237027304512 ) ) ;
#43122=ORIENTED_EDGE ( 'NONE', *, *, #6434, .T. ) ;
#43134=CIRCLE ( 'NONE', #6916, 52.00000000000000000 ) ;
#43135=AXIS2_PLACEMENT_3D ( 'NONE', #30879, #30456, #536 ) ;
#43146=DIRECTION ( 'NONE',  ( 0.000000000000000000, 0.9048270524660205760, -0.4257792915650704391 ) ) ;
#43147=ORIENTED_EDGE ( 'NONE', *, *, #32703, .F. ) ;
#43149=LINE ( 'NONE', #16802, #33024 ) ;
#43152=DIRECTION ( 'NONE',  ( 0.000000000000000000, -0.9048270524660235736, 0.4257792915650641663 ) ) ;
#43153=CARTESIAN_POINT ( 'NONE',  ( 0.000000000000000000, 44.25018368420781911, -27.31155879685132959 ) ) ;
#43155=EDGE_CURVE ( 'NONE', #19720, #35521, #1691, .T. ) ;
#43159=DIRECTION ( 'NONE',  ( -1.000000000000000000, -0.000000000000000000, -0.000000000000000000 ) ) ;
#43166=CARTESIAN_POINT ( 'NONE',  ( 18.00000000000000355, -7.162210897276081845, 51.50439529848825515 ) ) ;
#43172=ORIENTED_EDGE ( 'NONE', *, *, #17310, .T. ) ;
#43178=CARTESIAN_POINT ( 'NONE',  ( 9.000000000000001776, -39.64889472655755753, 33.64468972902493960 ) ) ;
#43180=ORIENTED_EDGE ( 'NONE', *, *, #30693, .T. ) ;
ENDSEC;
END-ISO-10303-21;
